ISO-10303-21;
HEADER;
/* Generated by software containing ST-Developer
 * from STEP Tools, Inc. (www.steptools.com) 
 */

FILE_DESCRIPTION(
/* description */ ('STEP AP214'),
/* implementation_level */ '2;1');

FILE_NAME(
/* name */ 'Class 8.8 Steel Hex Head Screw.step',
/* time_stamp */ '2026-11-14T06:34:07-08:00',
/* author */ (''),
/* organization */ (''),
/* preprocessor_version */ 'ST-DEVELOPER v20.2',
/* originating_system */ 'Autodesk Translation Framework v15.17.0.0',
/* authorisation */ '');

FILE_SCHEMA (('AUTOMOTIVE_DESIGN { 1 0 10303 214 3 1 1 }'));
ENDSEC;

DATA;
#10=MECHANICAL_DESIGN_GEOMETRIC_PRESENTATION_REPRESENTATION('',(#7322),#310623);
#984=B_SPLINE_SURFACE_WITH_KNOTS('',3,1,((#306944,#306945),(#306946,#306947),
(#306948,#306949),(#306950,#306951),(#306952,#306953),(#306954,#306955),
(#306956,#306957),(#306958,#306959),(#306960,#306961),(#306962,#306963),
(#306964,#306965),(#306966,#306967),(#306968,#306969),(#306970,#306971),
(#306972,#306973),(#306974,#306975),(#306976,#306977),(#306978,#306979),
(#306980,#306981)),.UNSPECIFIED.,.F.,.F.,.F.,(4,1,1,1,1,1,1,1,1,1,1,1,1,
1,1,1,4),(2,2),(0.,0.0580692684342556,0.114001303445375,0.169772099070702,
0.224674954494909,0.280054150165824,0.336957215314267,0.395112576113712,
0.456649482459617,0.519182398591372,0.582165728137028,0.645753825355143,
0.710908012329458,0.778341319290106,0.848949505917864,0.922850140892551,
1.),(0.,0.024),.UNSPECIFIED.);
#985=B_SPLINE_SURFACE_WITH_KNOTS('',3,1,((#307005,#307006),(#307007,#307008),
(#307009,#307010),(#307011,#307012),(#307013,#307014),(#307015,#307016),
(#307017,#307018),(#307019,#307020),(#307021,#307022),(#307023,#307024),
(#307025,#307026),(#307027,#307028),(#307029,#307030),(#307031,#307032),
(#307033,#307034),(#307035,#307036),(#307037,#307038),(#307039,#307040),
(#307041,#307042)),.UNSPECIFIED.,.F.,.F.,.F.,(4,1,1,1,1,1,1,1,1,1,1,1,1,
1,1,1,4),(2,2),(0.,0.0766164418639844,0.150101977842741,0.220268821680907,
0.287483908975341,0.35290178839726,0.417338409308383,0.480866360224848,
0.543808187325834,0.605854592868513,0.665047756996982,0.722013651121557,
0.777789178028364,0.832724479504672,0.887128050755955,0.942855781853261,
1.),(0.,0.024),.UNSPECIFIED.);
#986=B_SPLINE_SURFACE_WITH_KNOTS('',3,1,((#307064,#307065),(#307066,#307067),
(#307068,#307069),(#307070,#307071),(#307072,#307073),(#307074,#307075),
(#307076,#307077),(#307078,#307079),(#307080,#307081),(#307082,#307083),
(#307084,#307085),(#307086,#307087),(#307088,#307089),(#307090,#307091),
(#307092,#307093),(#307094,#307095),(#307096,#307097),(#307098,#307099),
(#307100,#307101)),.UNSPECIFIED.,.F.,.F.,.F.,(4,1,1,1,1,1,1,1,1,1,1,1,1,
1,1,1,4),(2,2),(0.,0.0577170366867072,0.113994474768008,0.16893758423175,
0.224179487123504,0.279968804571931,0.337633163696686,0.397092193126611,
0.459041827583877,0.522525900750905,0.586121573329079,0.650102352916103,
0.71540731027663,0.782762550840158,0.852275272320573,0.924507298607219,
1.),(0.,0.024),.UNSPECIFIED.);
#987=B_SPLINE_SURFACE_WITH_KNOTS('',3,1,((#307123,#307124),(#307125,#307126),
(#307127,#307128),(#307129,#307130),(#307131,#307132),(#307133,#307134),
(#307135,#307136),(#307137,#307138),(#307139,#307140),(#307141,#307142),
(#307143,#307144),(#307145,#307146),(#307147,#307148),(#307149,#307150),
(#307151,#307152),(#307153,#307154),(#307155,#307156),(#307157,#307158),
(#307159,#307160)),.UNSPECIFIED.,.F.,.F.,.F.,(4,1,1,1,1,1,1,1,1,1,1,1,1,
1,1,1,4),(2,2),(0.,0.0768723536038944,0.150603343572851,0.220876273582275,
0.288315870518755,0.35395225660761,0.418604106617997,0.481972048717606,
0.545247561534372,0.606993813632933,0.665860906234417,0.723420981486814,
0.778433488719744,0.833552283298071,0.88813757158342,0.943362448943921,
1.),(0.,0.024),.UNSPECIFIED.);
#988=B_SPLINE_SURFACE_WITH_KNOTS('',3,1,((#307180,#307181),(#307182,#307183),
(#307184,#307185),(#307186,#307187),(#307188,#307189),(#307190,#307191),
(#307192,#307193),(#307194,#307195),(#307196,#307197),(#307198,#307199),
(#307200,#307201)),.UNSPECIFIED.,.F.,.F.,.F.,(4,1,1,1,1,1,1,1,4),(2,2),
(0.,0.113008663357688,0.223447121007772,0.335763095333029,0.457240997711765,
0.584219963833153,0.714811315114105,0.851997802140335,1.),(0.,0.024),
 .UNSPECIFIED.);
#989=B_SPLINE_SURFACE_WITH_KNOTS('',3,1,((#307217,#307218),(#307219,#307220),
(#307221,#307222),(#307223,#307224),(#307225,#307226),(#307227,#307228),
(#307229,#307230),(#307231,#307232),(#307233,#307234),(#307235,#307236),
(#307237,#307238)),.UNSPECIFIED.,.F.,.F.,.F.,(4,1,1,1,1,1,1,1,4),(2,2),
(0.,0.149379665294656,0.288273014687601,0.418942648167458,0.547753389590675,
0.670496533301504,0.782663672045753,0.890203158268387,1.),(0.,0.024),
 .UNSPECIFIED.);
#990=B_SPLINE_SURFACE_WITH_KNOTS('',3,1,((#307252,#307253),(#307254,#307255),
(#307256,#307257),(#307258,#307259),(#307260,#307261),(#307262,#307263),
(#307264,#307265),(#307266,#307267),(#307268,#307269),(#307270,#307271),
(#307272,#307273)),.UNSPECIFIED.,.F.,.F.,.F.,(4,1,1,1,1,1,1,1,4),(2,2),
(0.,0.113035127206385,0.22352787461649,0.337812984577189,0.462304974001557,
0.590889524052717,0.720496476039469,0.855414628911259,1.),(0.,0.024),
 .UNSPECIFIED.);
#991=B_SPLINE_SURFACE_WITH_KNOTS('',3,1,((#307287,#307288),(#307289,#307290),
(#307291,#307292),(#307293,#307294),(#307295,#307296),(#307297,#307298),
(#307299,#307300),(#307301,#307302),(#307303,#307304),(#307305,#307306),
(#307307,#307308)),.UNSPECIFIED.,.F.,.F.,.F.,(4,1,1,1,1,1,1,1,4),(2,2),
(0.,0.153975786043391,0.294620990206987,0.425952943236339,0.551063084753368,
0.669883873511439,0.780296648018842,0.888858324162197,1.),(0.,0.024),
 .UNSPECIFIED.);
#992=B_SPLINE_SURFACE_WITH_KNOTS('',3,1,((#307320,#307321),(#307322,#307323),
(#307324,#307325),(#307326,#307327),(#307328,#307329),(#307330,#307331),
(#307332,#307333),(#307334,#307335),(#307336,#307337),(#307338,#307339),
(#307340,#307341),(#307342,#307343),(#307344,#307345),(#307346,#307347),
(#307348,#307349),(#307350,#307351),(#307352,#307353),(#307354,#307355),
(#307356,#307357)),.UNSPECIFIED.,.F.,.F.,.F.,(4,1,1,1,1,1,1,1,1,1,1,1,1,
1,1,1,4),(2,2),(0.,0.0580692684342556,0.114001303445375,0.169772099070702,
0.224674954494909,0.280054150165824,0.336957215314267,0.395112576113712,
0.456649482459617,0.519182398591372,0.582165728137028,0.645753825355143,
0.710908012329458,0.778341319290106,0.848949505917864,0.922850140892551,
1.),(0.,0.024),.UNSPECIFIED.);
#993=B_SPLINE_SURFACE_WITH_KNOTS('',3,1,((#307381,#307382),(#307383,#307384),
(#307385,#307386),(#307387,#307388),(#307389,#307390),(#307391,#307392),
(#307393,#307394),(#307395,#307396),(#307397,#307398),(#307399,#307400),
(#307401,#307402),(#307403,#307404),(#307405,#307406),(#307407,#307408),
(#307409,#307410),(#307411,#307412),(#307413,#307414),(#307415,#307416),
(#307417,#307418)),.UNSPECIFIED.,.F.,.F.,.F.,(4,1,1,1,1,1,1,1,1,1,1,1,1,
1,1,1,4),(2,2),(0.,0.0766164418639844,0.150101977842741,0.220268821680907,
0.287483908975341,0.35290178839726,0.417338409308383,0.480866360224848,
0.543808187325834,0.605854592868513,0.665047756996982,0.722013651121557,
0.777789178028364,0.832724479504672,0.887128050755955,0.942855781853261,
1.),(0.,0.024),.UNSPECIFIED.);
#994=B_SPLINE_SURFACE_WITH_KNOTS('',3,1,((#307440,#307441),(#307442,#307443),
(#307444,#307445),(#307446,#307447),(#307448,#307449),(#307450,#307451),
(#307452,#307453),(#307454,#307455),(#307456,#307457),(#307458,#307459),
(#307460,#307461),(#307462,#307463),(#307464,#307465),(#307466,#307467),
(#307468,#307469),(#307470,#307471),(#307472,#307473),(#307474,#307475),
(#307476,#307477)),.UNSPECIFIED.,.F.,.F.,.F.,(4,1,1,1,1,1,1,1,1,1,1,1,1,
1,1,1,4),(2,2),(0.,0.0577170366867072,0.113994474768008,0.16893758423175,
0.224179487123505,0.279968804571931,0.337633163696686,0.397092193126611,
0.459041827583877,0.522525900750905,0.586121573329079,0.650102352916103,
0.71540731027663,0.782762550840158,0.852275272320572,0.924507298607219,
1.),(0.,0.024),.UNSPECIFIED.);
#995=B_SPLINE_SURFACE_WITH_KNOTS('',3,1,((#307499,#307500),(#307501,#307502),
(#307503,#307504),(#307505,#307506),(#307507,#307508),(#307509,#307510),
(#307511,#307512),(#307513,#307514),(#307515,#307516),(#307517,#307518),
(#307519,#307520),(#307521,#307522),(#307523,#307524),(#307525,#307526),
(#307527,#307528),(#307529,#307530),(#307531,#307532),(#307533,#307534),
(#307535,#307536)),.UNSPECIFIED.,.F.,.F.,.F.,(4,1,1,1,1,1,1,1,1,1,1,1,1,
1,1,1,4),(2,2),(0.,0.0768723536038944,0.150603343572851,0.220876273582275,
0.288315870518755,0.35395225660761,0.418604106617997,0.481972048717605,
0.545247561534372,0.606993813632933,0.665860906234417,0.723420981486814,
0.778433488719744,0.833552283298071,0.88813757158342,0.943362448943921,
1.),(0.,0.024),.UNSPECIFIED.);
#996=B_SPLINE_SURFACE_WITH_KNOTS('',3,1,((#307556,#307557),(#307558,#307559),
(#307560,#307561),(#307562,#307563),(#307564,#307565),(#307566,#307567),
(#307568,#307569),(#307570,#307571),(#307572,#307573),(#307574,#307575),
(#307576,#307577)),.UNSPECIFIED.,.F.,.F.,.F.,(4,1,1,1,1,1,1,1,4),(2,2),
(0.,0.113008663357688,0.223447121007772,0.335763095333029,0.457240997711765,
0.584219963833153,0.714811315114105,0.851997802140335,1.),(0.,0.024),
 .UNSPECIFIED.);
#997=B_SPLINE_SURFACE_WITH_KNOTS('',3,1,((#307593,#307594),(#307595,#307596),
(#307597,#307598),(#307599,#307600),(#307601,#307602),(#307603,#307604),
(#307605,#307606),(#307607,#307608),(#307609,#307610),(#307611,#307612),
(#307613,#307614)),.UNSPECIFIED.,.F.,.F.,.F.,(4,1,1,1,1,1,1,1,4),(2,2),
(0.,0.149379665294656,0.288273014687601,0.418942648167458,0.547753389590675,
0.670496533301504,0.782663672045753,0.890203158268387,1.),(0.,0.024),
 .UNSPECIFIED.);
#998=B_SPLINE_SURFACE_WITH_KNOTS('',3,1,((#307628,#307629),(#307630,#307631),
(#307632,#307633),(#307634,#307635),(#307636,#307637),(#307638,#307639),
(#307640,#307641),(#307642,#307643),(#307644,#307645),(#307646,#307647),
(#307648,#307649)),.UNSPECIFIED.,.F.,.F.,.F.,(4,1,1,1,1,1,1,1,4),(2,2),
(0.,0.113035127206385,0.22352787461649,0.337812984577189,0.462304974001557,
0.590889524052717,0.720496476039469,0.855414628911259,1.),(0.,0.024),
 .UNSPECIFIED.);
#999=B_SPLINE_SURFACE_WITH_KNOTS('',3,1,((#307663,#307664),(#307665,#307666),
(#307667,#307668),(#307669,#307670),(#307671,#307672),(#307673,#307674),
(#307675,#307676),(#307677,#307678),(#307679,#307680),(#307681,#307682),
(#307683,#307684)),.UNSPECIFIED.,.F.,.F.,.F.,(4,1,1,1,1,1,1,1,4),(2,2),
(0.,0.153975786043391,0.294620990206987,0.42595294323634,0.551063084753368,
0.669883873511439,0.780296648018842,0.888858324162197,1.),(0.,0.024),
 .UNSPECIFIED.);
#1000=B_SPLINE_SURFACE_WITH_KNOTS('',3,1,((#307995,#307996),(#307997,#307998),
(#307999,#308000),(#308001,#308002),(#308003,#308004),(#308005,#308006),
(#308007,#308008),(#308009,#308010),(#308011,#308012),(#308013,#308014),
(#308015,#308016),(#308017,#308018),(#308019,#308020),(#308021,#308022),
(#308023,#308024),(#308025,#308026),(#308027,#308028),(#308029,#308030),
(#308031,#308032)),.UNSPECIFIED.,.F.,.F.,.F.,(4,1,1,1,1,1,1,1,1,1,1,1,1,
1,1,1,4),(2,2),(0.,0.0624074292203441,0.123580758253191,0.183030548059535,
0.241487894622227,0.299476288588136,0.357776621678218,0.416397215359044,
0.475293297309649,0.535174551555035,0.596373380100883,0.65843295832835,
0.722087328991003,0.787866252937039,0.856053064935337,0.926280127267363,
1.),(0.,0.024),.UNSPECIFIED.);
#1001=B_SPLINE_SURFACE_WITH_KNOTS('',3,1,((#308056,#308057),(#308058,#308059),
(#308060,#308061),(#308062,#308063),(#308064,#308065),(#308066,#308067),
(#308068,#308069),(#308070,#308071),(#308072,#308073),(#308074,#308075),
(#308076,#308077)),.UNSPECIFIED.,.F.,.F.,.F.,(4,1,1,1,1,1,1,1,4),(2,2),
(0.,0.140786050719229,0.271192292477146,0.394820533419766,0.51366840541228,
0.630249521887138,0.748635241534156,0.870539222318192,1.),(0.,0.024),
 .UNSPECIFIED.);
#1002=B_SPLINE_SURFACE_WITH_KNOTS('',3,1,((#308091,#308092),(#308093,#308094),
(#308095,#308096),(#308097,#308098),(#308099,#308100),(#308101,#308102),
(#308103,#308104),(#308105,#308106),(#308107,#308108),(#308109,#308110),
(#308111,#308112),(#308113,#308114),(#308115,#308116),(#308117,#308118),
(#308119,#308120),(#308121,#308122),(#308123,#308124),(#308125,#308126),
(#308127,#308128)),.UNSPECIFIED.,.F.,.F.,.F.,(4,1,1,1,1,1,1,1,1,1,1,1,1,
1,1,1,4),(2,2),(0.,0.061579283211466,0.121651367349155,0.179800294989198,
0.237201673292092,0.294780234992934,0.353324880649131,0.412515530286399,
0.474433538402357,0.537108068033057,0.599269077379891,0.66175044463838,
0.725142484567205,0.790290611404277,0.857751363050287,0.927508428952717,
1.),(0.,0.024),.UNSPECIFIED.);
#1003=B_SPLINE_SURFACE_WITH_KNOTS('',3,1,((#308150,#308151),(#308152,#308153),
(#308154,#308155),(#308156,#308157),(#308158,#308159),(#308160,#308161),
(#308162,#308163),(#308164,#308165),(#308166,#308167),(#308168,#308169),
(#308170,#308171),(#308172,#308173),(#308174,#308175),(#308176,#308177),
(#308178,#308179),(#308180,#308181),(#308182,#308183),(#308184,#308185),
(#308186,#308187)),.UNSPECIFIED.,.F.,.F.,.F.,(4,1,1,1,1,1,1,1,1,1,1,1,1,
1,1,1,4),(2,2),(0.,0.0728455592253727,0.142402257701936,0.209648156853246,
0.274427985226561,0.337611609749171,0.399896985087157,0.462371952688158,
0.524655094094133,0.586203391626632,0.645775819776357,0.704006503444922,
0.762043319649332,0.81964939871453,0.877994662833982,0.938199028971844,
1.),(0.,0.024),.UNSPECIFIED.);
#1004=B_SPLINE_SURFACE_WITH_KNOTS('',3,1,((#308209,#308210),(#308211,#308212),
(#308213,#308214),(#308215,#308216),(#308217,#308218),(#308219,#308220),
(#308221,#308222),(#308223,#308224),(#308225,#308226),(#308227,#308228),
(#308229,#308230)),.UNSPECIFIED.,.F.,.F.,.F.,(4,1,1,1,1,1,1,1,4),(2,2),
(0.,0.126037809173243,0.24590192439148,0.362706754432767,0.479405225937116,
0.59860340945283,0.723279815939465,0.85618139156474,1.),(0.,0.024),
 .UNSPECIFIED.);
#1005=B_SPLINE_SURFACE_WITH_KNOTS('',3,1,((#308244,#308245),(#308246,#308247),
(#308248,#308249),(#308250,#308251),(#308252,#308253),(#308254,#308255),
(#308256,#308257),(#308258,#308259),(#308260,#308261),(#308262,#308263),
(#308264,#308265),(#308266,#308267),(#308268,#308269),(#308270,#308271),
(#308272,#308273),(#308274,#308275),(#308276,#308277),(#308278,#308279),
(#308280,#308281)),.UNSPECIFIED.,.F.,.F.,.F.,(4,1,1,1,1,1,1,1,1,1,1,1,1,
1,1,1,4),(2,2),(0.,0.0756779287595513,0.148475385165302,0.218686839383758,
0.285894163869826,0.350394511043543,0.41333034849776,0.475131662182092,
0.535395707628871,0.595069793647295,0.653190706601446,0.71022527848224,
0.767064167323289,0.824126149789293,0.882061797546221,0.940276800846585,
1.),(0.,0.024),.UNSPECIFIED.);
#1006=B_SPLINE_SURFACE_WITH_KNOTS('',3,1,((#308303,#308304),(#308305,#308306),
(#308307,#308308),(#308309,#308310),(#308311,#308312),(#308313,#308314),
(#308315,#308316),(#308317,#308318),(#308319,#308320),(#308321,#308322),
(#308323,#308324),(#308325,#308326),(#308327,#308328),(#308329,#308330),
(#308331,#308332),(#308333,#308334),(#308335,#308336),(#308337,#308338),
(#308339,#308340)),.UNSPECIFIED.,.F.,.F.,.F.,(4,1,1,1,1,1,1,1,1,1,1,1,1,
1,1,1,4),(2,2),(0.,0.061560808552986,0.120975543465591,0.179004419802313,
0.236102291207156,0.293686508428115,0.351514938997191,0.410728891353352,
0.472160594099565,0.534227146274051,0.596384774286223,0.658759168877887,
0.722544817104037,0.787964999387698,0.855593119477614,0.926440609783223,
1.),(0.,0.024),.UNSPECIFIED.);
#1007=B_SPLINE_SURFACE_WITH_KNOTS('',3,1,((#308362,#308363),(#308364,#308365),
(#308366,#308367),(#308368,#308369),(#308370,#308371),(#308372,#308373),
(#308374,#308375),(#308376,#308377),(#308378,#308379),(#308380,#308381),
(#308382,#308383),(#308384,#308385),(#308386,#308387),(#308388,#308389),
(#308390,#308391),(#308392,#308393),(#308394,#308395),(#308396,#308397),
(#308398,#308399)),.UNSPECIFIED.,.F.,.F.,.F.,(4,1,1,1,1,1,1,1,1,1,1,1,1,
1,1,1,4),(2,2),(0.,0.0724843729385586,0.142190024778259,0.209247943639616,
0.274447923967761,0.33802582267117,0.400406532440542,0.463046285981066,
0.525723189050567,0.587758999700955,0.647207274703619,0.705604379270503,
0.76335494041328,0.821014301633402,0.879178712895835,0.938732443992665,
1.),(0.,0.024),.UNSPECIFIED.);
#1008=B_SPLINE_SURFACE_WITH_KNOTS('',3,1,((#308419,#308420),(#308421,#308422),
(#308423,#308424),(#308425,#308426),(#308427,#308428),(#308429,#308430),
(#308431,#308432),(#308433,#308434),(#308435,#308436),(#308437,#308438),
(#308439,#308440),(#308441,#308442),(#308443,#308444),(#308445,#308446),
(#308447,#308448),(#308449,#308450),(#308451,#308452),(#308453,#308454),
(#308455,#308456)),.UNSPECIFIED.,.F.,.F.,.F.,(4,1,1,1,1,1,1,1,1,1,1,1,1,
1,1,1,4),(2,2),(0.,0.0624074292203441,0.123580758253191,0.183030548059535,
0.241487894622227,0.299476288588135,0.357776621678218,0.416397215359044,
0.475293297309649,0.535174551555035,0.596373380100883,0.65843295832835,
0.722087328991003,0.787866252937039,0.856053064935338,0.926280127267363,
1.),(0.,0.024),.UNSPECIFIED.);
#1009=B_SPLINE_SURFACE_WITH_KNOTS('',3,1,((#308480,#308481),(#308482,#308483),
(#308484,#308485),(#308486,#308487),(#308488,#308489),(#308490,#308491),
(#308492,#308493),(#308494,#308495),(#308496,#308497),(#308498,#308499),
(#308500,#308501)),.UNSPECIFIED.,.F.,.F.,.F.,(4,1,1,1,1,1,1,1,4),(2,2),
(0.,0.140786050719229,0.271192292477146,0.394820533419766,0.51366840541228,
0.630249521887138,0.748635241534156,0.870539222318192,1.),(0.,0.024),
 .UNSPECIFIED.);
#1010=B_SPLINE_SURFACE_WITH_KNOTS('',3,1,((#308515,#308516),(#308517,#308518),
(#308519,#308520),(#308521,#308522),(#308523,#308524),(#308525,#308526),
(#308527,#308528),(#308529,#308530),(#308531,#308532),(#308533,#308534),
(#308535,#308536),(#308537,#308538),(#308539,#308540),(#308541,#308542),
(#308543,#308544),(#308545,#308546),(#308547,#308548),(#308549,#308550),
(#308551,#308552)),.UNSPECIFIED.,.F.,.F.,.F.,(4,1,1,1,1,1,1,1,1,1,1,1,1,
1,1,1,4),(2,2),(0.,0.061579283211466,0.121651367349155,0.179800294989198,
0.237201673292092,0.294780234992934,0.353324880649131,0.412515530286399,
0.474433538402357,0.537108068033057,0.599269077379891,0.66175044463838,
0.725142484567205,0.790290611404277,0.857751363050287,0.927508428952717,
1.),(0.,0.024),.UNSPECIFIED.);
#1011=B_SPLINE_SURFACE_WITH_KNOTS('',3,1,((#308574,#308575),(#308576,#308577),
(#308578,#308579),(#308580,#308581),(#308582,#308583),(#308584,#308585),
(#308586,#308587),(#308588,#308589),(#308590,#308591),(#308592,#308593),
(#308594,#308595),(#308596,#308597),(#308598,#308599),(#308600,#308601),
(#308602,#308603),(#308604,#308605),(#308606,#308607),(#308608,#308609),
(#308610,#308611)),.UNSPECIFIED.,.F.,.F.,.F.,(4,1,1,1,1,1,1,1,1,1,1,1,1,
1,1,1,4),(2,2),(0.,0.0728455592253727,0.142402257701936,0.209648156853246,
0.274427985226561,0.337611609749171,0.399896985087157,0.462371952688158,
0.524655094094133,0.586203391626633,0.645775819776357,0.704006503444922,
0.762043319649332,0.81964939871453,0.877994662833982,0.938199028971844,
1.),(0.,0.024),.UNSPECIFIED.);
#1012=B_SPLINE_SURFACE_WITH_KNOTS('',3,1,((#308633,#308634),(#308635,#308636),
(#308637,#308638),(#308639,#308640),(#308641,#308642),(#308643,#308644),
(#308645,#308646),(#308647,#308648),(#308649,#308650),(#308651,#308652),
(#308653,#308654)),.UNSPECIFIED.,.F.,.F.,.F.,(4,1,1,1,1,1,1,1,4),(2,2),
(0.,0.126037809173244,0.24590192439148,0.362706754432767,0.479405225937116,
0.59860340945283,0.723279815939465,0.85618139156474,1.),(0.,0.024),
 .UNSPECIFIED.);
#1013=B_SPLINE_SURFACE_WITH_KNOTS('',3,1,((#308668,#308669),(#308670,#308671),
(#308672,#308673),(#308674,#308675),(#308676,#308677),(#308678,#308679),
(#308680,#308681),(#308682,#308683),(#308684,#308685),(#308686,#308687),
(#308688,#308689),(#308690,#308691),(#308692,#308693),(#308694,#308695),
(#308696,#308697),(#308698,#308699),(#308700,#308701),(#308702,#308703),
(#308704,#308705)),.UNSPECIFIED.,.F.,.F.,.F.,(4,1,1,1,1,1,1,1,1,1,1,1,1,
1,1,1,4),(2,2),(0.,0.0756779287595513,0.148475385165302,0.218686839383758,
0.285894163869826,0.350394511043543,0.41333034849776,0.475131662182092,
0.535395707628871,0.595069793647295,0.653190706601445,0.71022527848224,
0.767064167323289,0.824126149789293,0.882061797546221,0.940276800846584,
1.),(0.,0.024),.UNSPECIFIED.);
#1014=B_SPLINE_SURFACE_WITH_KNOTS('',3,1,((#308727,#308728),(#308729,#308730),
(#308731,#308732),(#308733,#308734),(#308735,#308736),(#308737,#308738),
(#308739,#308740),(#308741,#308742),(#308743,#308744),(#308745,#308746),
(#308747,#308748),(#308749,#308750),(#308751,#308752),(#308753,#308754),
(#308755,#308756),(#308757,#308758),(#308759,#308760),(#308761,#308762),
(#308763,#308764)),.UNSPECIFIED.,.F.,.F.,.F.,(4,1,1,1,1,1,1,1,1,1,1,1,1,
1,1,1,4),(2,2),(0.,0.061560808552986,0.120975543465591,0.179004419802313,
0.236102291207156,0.293686508428115,0.351514938997191,0.410728891353352,
0.472160594099565,0.534227146274051,0.596384774286223,0.658759168877887,
0.722544817104037,0.787964999387698,0.855593119477614,0.926440609783223,
1.),(0.,0.024),.UNSPECIFIED.);
#1015=B_SPLINE_SURFACE_WITH_KNOTS('',3,1,((#308786,#308787),(#308788,#308789),
(#308790,#308791),(#308792,#308793),(#308794,#308795),(#308796,#308797),
(#308798,#308799),(#308800,#308801),(#308802,#308803),(#308804,#308805),
(#308806,#308807),(#308808,#308809),(#308810,#308811),(#308812,#308813),
(#308814,#308815),(#308816,#308817),(#308818,#308819),(#308820,#308821),
(#308822,#308823)),.UNSPECIFIED.,.F.,.F.,.F.,(4,1,1,1,1,1,1,1,1,1,1,1,1,
1,1,1,4),(2,2),(0.,0.0724843729385586,0.142190024778259,0.209247943639616,
0.274447923967761,0.33802582267117,0.400406532440542,0.463046285981066,
0.525723189050567,0.587758999700955,0.647207274703619,0.705604379270503,
0.76335494041328,0.821014301633402,0.879178712895835,0.938732443992665,
1.),(0.,0.024),.UNSPECIFIED.);
#1692=(
BOUNDED_CURVE()
B_SPLINE_CURVE(2,(#304329,#304330,#304331),.UNSPECIFIED.,.F.,.F.)
B_SPLINE_CURVE_WITH_KNOTS((3,3),(0.868421052631579,0.871442538302458),
 .UNSPECIFIED.)
CURVE()
GEOMETRIC_REPRESENTATION_ITEM()
RATIONAL_B_SPLINE_CURVE((1.,0.971902413407548,0.976065479819744))
REPRESENTATION_ITEM('')
);
#1693=(
BOUNDED_CURVE()
B_SPLINE_CURVE(2,(#304336,#304337,#304338,#304339,#304340,#304341,#304342,
#304343,#304344,#304345,#304346,#304347,#304348,#304349,#304350,#304351,
#304352,#304353,#304354,#304355,#304356),.UNSPECIFIED.,.F.,.F.)
B_SPLINE_CURVE_WITH_KNOTS((3,2,2,2,2,2,2,2,2,2,3),(0.815789473684211,0.821052631578947,
0.826315789473684,0.831578947368421,0.836842105263158,0.842105263157895,
0.847368421052632,0.852631578947368,0.857894736842105,0.863157894736842,
0.868421052631579),.UNSPECIFIED.)
CURVE()
GEOMETRIC_REPRESENTATION_ITEM()
RATIONAL_B_SPLINE_CURVE((1.,0.951056516295154,1.,0.951056516295154,1.,0.951056516295154,
1.,0.951056516295154,1.,0.951056516295154,1.,0.951056516295154,1.,0.951056516295154,
1.,0.951056516295154,1.,0.951056516295154,1.,0.951056516295154,1.))
REPRESENTATION_ITEM('')
);
#1694=(
BOUNDED_CURVE()
B_SPLINE_CURVE(2,(#304357,#304358,#304359,#304360,#304361,#304362,#304363,
#304364,#304365,#304366,#304367,#304368,#304369,#304370,#304371,#304372,
#304373,#304374,#304375,#304376,#304377),.UNSPECIFIED.,.F.,.F.)
B_SPLINE_CURVE_WITH_KNOTS((3,2,2,2,2,2,2,2,2,2,3),(0.815789473684211,0.821052631578947,
0.826315789473684,0.831578947368421,0.836842105263158,0.842105263157895,
0.847368421052632,0.852631578947368,0.857894736842105,0.863157894736842,
0.864892973551299),.UNSPECIFIED.)
CURVE()
GEOMETRIC_REPRESENTATION_ITEM()
RATIONAL_B_SPLINE_CURVE((1.,0.951056516295154,1.,0.951056516295154,1.,0.951056516295154,
1.,0.951056516295154,1.,0.951056516295154,1.,0.951056516295154,1.,0.951056516295154,
1.,0.951056516295154,1.,0.951056516295154,1.,0.983865047680423,0.978368352658793))
REPRESENTATION_ITEM('')
);
#1695=(
BOUNDED_CURVE()
B_SPLINE_CURVE(2,(#304382,#304383,#304384,#304385,#304386,#304387,#304388,
#304389,#304390,#304391,#304392,#304393,#304394,#304395,#304396,#304397,
#304398,#304399,#304400,#304401,#304402),.UNSPECIFIED.,.F.,.F.)
B_SPLINE_CURVE_WITH_KNOTS((3,2,2,2,2,2,2,2,2,2,3),(0.763157894736842,0.768421052631579,
0.773684210526316,0.778947368421053,0.78421052631579,0.789473684210526,
0.794736842105263,0.8,0.805263157894737,0.810526315789474,0.815789473684211),
 .UNSPECIFIED.)
CURVE()
GEOMETRIC_REPRESENTATION_ITEM()
RATIONAL_B_SPLINE_CURVE((1.,0.951056516295154,1.,0.951056516295154,1.,0.951056516295154,
1.,0.951056516295154,1.,0.951056516295154,1.,0.951056516295154,1.,0.951056516295154,
1.,0.951056516295154,1.,0.951056516295154,1.,0.951056516295154,1.))
REPRESENTATION_ITEM('')
);
#1696=(
BOUNDED_CURVE()
B_SPLINE_CURVE(2,(#304403,#304404,#304405,#304406,#304407,#304408,#304409,
#304410,#304411,#304412,#304413,#304414,#304415,#304416,#304417,#304418,
#304419,#304420,#304421,#304422,#304423),.UNSPECIFIED.,.F.,.F.)
B_SPLINE_CURVE_WITH_KNOTS((3,2,2,2,2,2,2,2,2,2,3),(0.763157894736842,0.768421052631579,
0.773684210526316,0.778947368421053,0.78421052631579,0.789473684210526,
0.794736842105263,0.8,0.805263157894737,0.810526315789474,0.815789473684211),
 .UNSPECIFIED.)
CURVE()
GEOMETRIC_REPRESENTATION_ITEM()
RATIONAL_B_SPLINE_CURVE((1.,0.951056516295154,1.,0.951056516295154,1.,0.951056516295154,
1.,0.951056516295154,1.,0.951056516295154,1.,0.951056516295154,1.,0.951056516295154,
1.,0.951056516295154,1.,0.951056516295154,1.,0.951056516295154,1.))
REPRESENTATION_ITEM('')
);
#1697=(
BOUNDED_CURVE()
B_SPLINE_CURVE(2,(#304428,#304429,#304430,#304431,#304432,#304433,#304434,
#304435,#304436,#304437,#304438,#304439,#304440,#304441,#304442,#304443,
#304444,#304445,#304446,#304447,#304448),.UNSPECIFIED.,.F.,.F.)
B_SPLINE_CURVE_WITH_KNOTS((3,2,2,2,2,2,2,2,2,2,3),(0.710526315789474,0.715789473684211,
0.721052631578947,0.726315789473684,0.731578947368421,0.736842105263158,
0.742105263157895,0.747368421052632,0.752631578947368,0.757894736842105,
0.763157894736842),.UNSPECIFIED.)
CURVE()
GEOMETRIC_REPRESENTATION_ITEM()
RATIONAL_B_SPLINE_CURVE((1.,0.951056516295154,1.,0.951056516295154,1.,0.951056516295154,
1.,0.951056516295154,1.,0.951056516295154,1.,0.951056516295154,1.,0.951056516295154,
1.,0.951056516295154,1.,0.951056516295154,1.,0.951056516295154,1.))
REPRESENTATION_ITEM('')
);
#1698=(
BOUNDED_CURVE()
B_SPLINE_CURVE(2,(#304449,#304450,#304451,#304452,#304453,#304454,#304455,
#304456,#304457,#304458,#304459,#304460,#304461,#304462,#304463,#304464,
#304465,#304466,#304467,#304468,#304469),.UNSPECIFIED.,.F.,.F.)
B_SPLINE_CURVE_WITH_KNOTS((3,2,2,2,2,2,2,2,2,2,3),(0.710526315789474,0.715789473684211,
0.721052631578947,0.726315789473684,0.731578947368421,0.736842105263158,
0.742105263157895,0.747368421052632,0.752631578947368,0.757894736842105,
0.763157894736842),.UNSPECIFIED.)
CURVE()
GEOMETRIC_REPRESENTATION_ITEM()
RATIONAL_B_SPLINE_CURVE((1.,0.951056516295154,1.,0.951056516295154,1.,0.951056516295154,
1.,0.951056516295154,1.,0.951056516295154,1.,0.951056516295154,1.,0.951056516295154,
1.,0.951056516295154,1.,0.951056516295154,1.,0.951056516295154,1.))
REPRESENTATION_ITEM('')
);
#1699=(
BOUNDED_CURVE()
B_SPLINE_CURVE(2,(#304474,#304475,#304476,#304477,#304478,#304479,#304480,
#304481,#304482,#304483,#304484,#304485,#304486,#304487,#304488,#304489,
#304490,#304491,#304492,#304493,#304494),.UNSPECIFIED.,.F.,.F.)
B_SPLINE_CURVE_WITH_KNOTS((3,2,2,2,2,2,2,2,2,2,3),(0.657894736842105,0.663157894736842,
0.668421052631579,0.673684210526316,0.678947368421053,0.68421052631579,
0.689473684210526,0.694736842105263,0.7,0.705263157894737,0.710526315789474),
 .UNSPECIFIED.)
CURVE()
GEOMETRIC_REPRESENTATION_ITEM()
RATIONAL_B_SPLINE_CURVE((1.,0.951056516295154,1.,0.951056516295154,1.,0.951056516295154,
1.,0.951056516295154,1.,0.951056516295154,1.,0.951056516295154,1.,0.951056516295154,
1.,0.951056516295154,1.,0.951056516295154,1.,0.951056516295154,1.))
REPRESENTATION_ITEM('')
);
#1700=(
BOUNDED_CURVE()
B_SPLINE_CURVE(2,(#304495,#304496,#304497,#304498,#304499,#304500,#304501,
#304502,#304503,#304504,#304505,#304506,#304507,#304508,#304509,#304510,
#304511,#304512,#304513,#304514,#304515),.UNSPECIFIED.,.F.,.F.)
B_SPLINE_CURVE_WITH_KNOTS((3,2,2,2,2,2,2,2,2,2,3),(0.657894736842105,0.663157894736842,
0.668421052631579,0.673684210526316,0.678947368421053,0.68421052631579,
0.689473684210526,0.694736842105263,0.7,0.705263157894737,0.710526315789474),
 .UNSPECIFIED.)
CURVE()
GEOMETRIC_REPRESENTATION_ITEM()
RATIONAL_B_SPLINE_CURVE((1.,0.951056516295154,1.,0.951056516295154,1.,0.951056516295154,
1.,0.951056516295154,1.,0.951056516295154,1.,0.951056516295154,1.,0.951056516295154,
1.,0.951056516295154,1.,0.951056516295154,1.,0.951056516295154,1.))
REPRESENTATION_ITEM('')
);
#1701=(
BOUNDED_CURVE()
B_SPLINE_CURVE(2,(#304520,#304521,#304522,#304523,#304524,#304525,#304526,
#304527,#304528,#304529,#304530,#304531,#304532,#304533,#304534,#304535,
#304536,#304537,#304538,#304539,#304540),.UNSPECIFIED.,.F.,.F.)
B_SPLINE_CURVE_WITH_KNOTS((3,2,2,2,2,2,2,2,2,2,3),(0.605263157894737,0.610526315789474,
0.615789473684211,0.621052631578947,0.626315789473684,0.631578947368421,
0.636842105263158,0.642105263157895,0.647368421052632,0.652631578947369,
0.657894736842105),.UNSPECIFIED.)
CURVE()
GEOMETRIC_REPRESENTATION_ITEM()
RATIONAL_B_SPLINE_CURVE((1.,0.951056516295154,1.,0.951056516295154,1.,0.951056516295154,
1.,0.951056516295154,1.,0.951056516295154,1.,0.951056516295154,1.,0.951056516295154,
1.,0.951056516295154,1.,0.951056516295154,1.,0.951056516295154,1.))
REPRESENTATION_ITEM('')
);
#1702=(
BOUNDED_CURVE()
B_SPLINE_CURVE(2,(#304541,#304542,#304543,#304544,#304545,#304546,#304547,
#304548,#304549,#304550,#304551,#304552,#304553,#304554,#304555,#304556,
#304557,#304558,#304559,#304560,#304561),.UNSPECIFIED.,.F.,.F.)
B_SPLINE_CURVE_WITH_KNOTS((3,2,2,2,2,2,2,2,2,2,3),(0.605263157894737,0.610526315789474,
0.615789473684211,0.621052631578947,0.626315789473684,0.631578947368421,
0.636842105263158,0.642105263157895,0.647368421052632,0.652631578947369,
0.657894736842105),.UNSPECIFIED.)
CURVE()
GEOMETRIC_REPRESENTATION_ITEM()
RATIONAL_B_SPLINE_CURVE((1.,0.951056516295154,1.,0.951056516295154,1.,0.951056516295154,
1.,0.951056516295154,1.,0.951056516295154,1.,0.951056516295154,1.,0.951056516295154,
1.,0.951056516295154,1.,0.951056516295154,1.,0.951056516295154,1.))
REPRESENTATION_ITEM('')
);
#1703=(
BOUNDED_CURVE()
B_SPLINE_CURVE(2,(#304566,#304567,#304568,#304569,#304570,#304571,#304572,
#304573,#304574,#304575,#304576,#304577,#304578,#304579,#304580,#304581,
#304582,#304583,#304584,#304585,#304586),.UNSPECIFIED.,.F.,.F.)
B_SPLINE_CURVE_WITH_KNOTS((3,2,2,2,2,2,2,2,2,2,3),(0.552631578947369,0.557894736842105,
0.563157894736842,0.568421052631579,0.573684210526316,0.578947368421053,
0.58421052631579,0.589473684210526,0.594736842105263,0.6,0.605263157894737),
 .UNSPECIFIED.)
CURVE()
GEOMETRIC_REPRESENTATION_ITEM()
RATIONAL_B_SPLINE_CURVE((1.,0.951056516295154,1.,0.951056516295154,1.,0.951056516295154,
1.,0.951056516295154,1.,0.951056516295154,1.,0.951056516295154,1.,0.951056516295154,
1.,0.951056516295154,1.,0.951056516295154,1.,0.951056516295154,1.))
REPRESENTATION_ITEM('')
);
#1704=(
BOUNDED_CURVE()
B_SPLINE_CURVE(2,(#304587,#304588,#304589,#304590,#304591,#304592,#304593,
#304594,#304595,#304596,#304597,#304598,#304599,#304600,#304601,#304602,
#304603,#304604,#304605,#304606,#304607),.UNSPECIFIED.,.F.,.F.)
B_SPLINE_CURVE_WITH_KNOTS((3,2,2,2,2,2,2,2,2,2,3),(0.552631578947369,0.557894736842105,
0.563157894736842,0.568421052631579,0.573684210526316,0.578947368421053,
0.58421052631579,0.589473684210526,0.594736842105263,0.6,0.605263157894737),
 .UNSPECIFIED.)
CURVE()
GEOMETRIC_REPRESENTATION_ITEM()
RATIONAL_B_SPLINE_CURVE((1.,0.951056516295154,1.,0.951056516295154,1.,0.951056516295154,
1.,0.951056516295154,1.,0.951056516295154,1.,0.951056516295154,1.,0.951056516295154,
1.,0.951056516295154,1.,0.951056516295154,1.,0.951056516295154,1.))
REPRESENTATION_ITEM('')
);
#1705=(
BOUNDED_CURVE()
B_SPLINE_CURVE(2,(#304612,#304613,#304614,#304615,#304616,#304617,#304618,
#304619,#304620,#304621,#304622,#304623,#304624,#304625,#304626,#304627,
#304628,#304629,#304630,#304631,#304632),.UNSPECIFIED.,.F.,.F.)
B_SPLINE_CURVE_WITH_KNOTS((3,2,2,2,2,2,2,2,2,2,3),(0.5,0.505263157894737,
0.510526315789474,0.515789473684211,0.521052631578947,0.526315789473684,
0.531578947368421,0.536842105263158,0.542105263157895,0.547368421052632,
0.552631578947369),.UNSPECIFIED.)
CURVE()
GEOMETRIC_REPRESENTATION_ITEM()
RATIONAL_B_SPLINE_CURVE((1.,0.951056516295154,1.,0.951056516295154,1.,0.951056516295154,
1.,0.951056516295154,1.,0.951056516295154,1.,0.951056516295154,1.,0.951056516295154,
1.,0.951056516295154,1.,0.951056516295154,1.,0.951056516295154,1.))
REPRESENTATION_ITEM('')
);
#1706=(
BOUNDED_CURVE()
B_SPLINE_CURVE(2,(#304633,#304634,#304635,#304636,#304637,#304638,#304639,
#304640,#304641,#304642,#304643,#304644,#304645,#304646,#304647,#304648,
#304649,#304650,#304651,#304652,#304653),.UNSPECIFIED.,.F.,.F.)
B_SPLINE_CURVE_WITH_KNOTS((3,2,2,2,2,2,2,2,2,2,3),(0.5,0.505263157894737,
0.510526315789474,0.515789473684211,0.521052631578947,0.526315789473684,
0.531578947368421,0.536842105263158,0.542105263157895,0.547368421052632,
0.552631578947369),.UNSPECIFIED.)
CURVE()
GEOMETRIC_REPRESENTATION_ITEM()
RATIONAL_B_SPLINE_CURVE((1.,0.951056516295154,1.,0.951056516295154,1.,0.951056516295154,
1.,0.951056516295154,1.,0.951056516295154,1.,0.951056516295154,1.,0.951056516295154,
1.,0.951056516295154,1.,0.951056516295154,1.,0.951056516295154,1.))
REPRESENTATION_ITEM('')
);
#1707=(
BOUNDED_CURVE()
B_SPLINE_CURVE(2,(#304658,#304659,#304660,#304661,#304662,#304663,#304664,
#304665,#304666,#304667,#304668,#304669,#304670,#304671,#304672,#304673,
#304674,#304675,#304676,#304677,#304678),.UNSPECIFIED.,.F.,.F.)
B_SPLINE_CURVE_WITH_KNOTS((3,2,2,2,2,2,2,2,2,2,3),(0.447368421052632,0.452631578947368,
0.457894736842105,0.463157894736842,0.468421052631579,0.473684210526316,
0.478947368421053,0.48421052631579,0.489473684210526,0.494736842105263,
0.5),.UNSPECIFIED.)
CURVE()
GEOMETRIC_REPRESENTATION_ITEM()
RATIONAL_B_SPLINE_CURVE((1.,0.951056516295154,1.,0.951056516295154,1.,0.951056516295154,
1.,0.951056516295154,1.,0.951056516295154,1.,0.951056516295154,1.,0.951056516295154,
1.,0.951056516295154,1.,0.951056516295154,1.,0.951056516295154,1.))
REPRESENTATION_ITEM('')
);
#1708=(
BOUNDED_CURVE()
B_SPLINE_CURVE(2,(#304679,#304680,#304681,#304682,#304683,#304684,#304685,
#304686,#304687,#304688,#304689,#304690,#304691,#304692,#304693,#304694,
#304695,#304696,#304697,#304698,#304699),.UNSPECIFIED.,.F.,.F.)
B_SPLINE_CURVE_WITH_KNOTS((3,2,2,2,2,2,2,2,2,2,3),(0.447368421052631,0.452631578947369,
0.457894736842105,0.463157894736842,0.468421052631579,0.473684210526316,
0.478947368421053,0.48421052631579,0.489473684210526,0.494736842105263,
0.5),.UNSPECIFIED.)
CURVE()
GEOMETRIC_REPRESENTATION_ITEM()
RATIONAL_B_SPLINE_CURVE((1.,0.951056516295154,1.,0.951056516295154,1.,0.951056516295154,
1.,0.951056516295154,1.,0.951056516295154,1.,0.951056516295154,1.,0.951056516295154,
1.,0.951056516295154,1.,0.951056516295154,1.,0.951056516295154,1.))
REPRESENTATION_ITEM('')
);
#1709=(
BOUNDED_CURVE()
B_SPLINE_CURVE(2,(#304704,#304705,#304706,#304707,#304708,#304709,#304710,
#304711,#304712,#304713,#304714,#304715,#304716,#304717,#304718,#304719,
#304720,#304721,#304722,#304723,#304724),.UNSPECIFIED.,.F.,.F.)
B_SPLINE_CURVE_WITH_KNOTS((3,2,2,2,2,2,2,2,2,2,3),(0.394736842105263,0.4,
0.405263157894737,0.410526315789473,0.415789473684211,0.421052631578948,
0.426315789473684,0.431578947368421,0.436842105263158,0.442105263157895,
0.447368421052632),.UNSPECIFIED.)
CURVE()
GEOMETRIC_REPRESENTATION_ITEM()
RATIONAL_B_SPLINE_CURVE((1.,0.951056516295154,1.,0.951056516295154,1.,0.951056516295154,
1.,0.951056516295154,1.,0.951056516295154,1.,0.951056516295154,1.,0.951056516295154,
1.,0.951056516295154,1.,0.951056516295154,1.,0.951056516295154,1.))
REPRESENTATION_ITEM('')
);
#1710=(
BOUNDED_CURVE()
B_SPLINE_CURVE(2,(#304725,#304726,#304727,#304728,#304729,#304730,#304731,
#304732,#304733,#304734,#304735,#304736,#304737,#304738,#304739,#304740,
#304741,#304742,#304743,#304744,#304745),.UNSPECIFIED.,.F.,.F.)
B_SPLINE_CURVE_WITH_KNOTS((3,2,2,2,2,2,2,2,2,2,3),(0.394736842105263,0.4,
0.405263157894737,0.410526315789473,0.415789473684211,0.421052631578948,
0.426315789473684,0.431578947368421,0.436842105263158,0.442105263157894,
0.447368421052631),.UNSPECIFIED.)
CURVE()
GEOMETRIC_REPRESENTATION_ITEM()
RATIONAL_B_SPLINE_CURVE((1.,0.951056516295154,1.,0.951056516295154,1.,0.951056516295154,
1.,0.951056516295154,1.,0.951056516295154,1.,0.951056516295154,1.,0.951056516295154,
1.,0.951056516295154,1.,0.951056516295154,1.,0.951056516295154,1.))
REPRESENTATION_ITEM('')
);
#1711=(
BOUNDED_CURVE()
B_SPLINE_CURVE(2,(#304750,#304751,#304752,#304753,#304754,#304755,#304756,
#304757,#304758,#304759,#304760,#304761,#304762,#304763,#304764,#304765,
#304766,#304767,#304768,#304769,#304770),.UNSPECIFIED.,.F.,.F.)
B_SPLINE_CURVE_WITH_KNOTS((3,2,2,2,2,2,2,2,2,2,3),(0.342105263157895,0.347368421052631,
0.352631578947369,0.357894736842105,0.363157894736842,0.368421052631579,
0.373684210526316,0.378947368421053,0.38421052631579,0.389473684210526,
0.394736842105263),.UNSPECIFIED.)
CURVE()
GEOMETRIC_REPRESENTATION_ITEM()
RATIONAL_B_SPLINE_CURVE((1.,0.951056516295154,1.,0.951056516295154,1.,0.951056516295154,
1.,0.951056516295154,1.,0.951056516295154,1.,0.951056516295154,1.,0.951056516295154,
1.,0.951056516295154,1.,0.951056516295154,1.,0.951056516295154,1.))
REPRESENTATION_ITEM('')
);
#1712=(
BOUNDED_CURVE()
B_SPLINE_CURVE(2,(#304771,#304772,#304773,#304774,#304775,#304776,#304777,
#304778,#304779,#304780,#304781,#304782,#304783,#304784,#304785,#304786,
#304787,#304788,#304789,#304790,#304791),.UNSPECIFIED.,.F.,.F.)
B_SPLINE_CURVE_WITH_KNOTS((3,2,2,2,2,2,2,2,2,2,3),(0.342105263157895,0.347368421052632,
0.352631578947369,0.357894736842105,0.363157894736842,0.368421052631579,
0.373684210526316,0.378947368421053,0.38421052631579,0.389473684210527,
0.394736842105263),.UNSPECIFIED.)
CURVE()
GEOMETRIC_REPRESENTATION_ITEM()
RATIONAL_B_SPLINE_CURVE((1.,0.951056516295154,1.,0.951056516295154,1.,0.951056516295154,
1.,0.951056516295154,1.,0.951056516295154,1.,0.951056516295154,1.,0.951056516295154,
1.,0.951056516295154,1.,0.951056516295154,1.,0.951056516295154,1.))
REPRESENTATION_ITEM('')
);
#1713=(
BOUNDED_CURVE()
B_SPLINE_CURVE(2,(#304796,#304797,#304798,#304799,#304800,#304801,#304802,
#304803,#304804,#304805,#304806,#304807,#304808,#304809,#304810,#304811,
#304812,#304813,#304814,#304815,#304816),.UNSPECIFIED.,.F.,.F.)
B_SPLINE_CURVE_WITH_KNOTS((3,2,2,2,2,2,2,2,2,2,3),(0.289473684210526,0.294736842105263,
0.3,0.305263157894737,0.310526315789473,0.315789473684211,0.321052631578947,
0.326315789473685,0.331578947368421,0.336842105263158,0.342105263157895),
 .UNSPECIFIED.)
CURVE()
GEOMETRIC_REPRESENTATION_ITEM()
RATIONAL_B_SPLINE_CURVE((1.,0.951056516295154,1.,0.951056516295154,1.,0.951056516295154,
1.,0.951056516295154,1.,0.951056516295154,1.,0.951056516295154,1.,0.951056516295154,
1.,0.951056516295154,1.,0.951056516295154,1.,0.951056516295154,1.))
REPRESENTATION_ITEM('')
);
#1714=(
BOUNDED_CURVE()
B_SPLINE_CURVE(2,(#304817,#304818,#304819,#304820,#304821,#304822,#304823,
#304824,#304825,#304826,#304827,#304828,#304829,#304830,#304831,#304832,
#304833,#304834,#304835,#304836,#304837),.UNSPECIFIED.,.F.,.F.)
B_SPLINE_CURVE_WITH_KNOTS((3,2,2,2,2,2,2,2,2,2,3),(0.289473684210526,0.294736842105263,
0.3,0.305263157894737,0.310526315789473,0.315789473684211,0.321052631578947,
0.326315789473685,0.331578947368421,0.336842105263158,0.342105263157895),
 .UNSPECIFIED.)
CURVE()
GEOMETRIC_REPRESENTATION_ITEM()
RATIONAL_B_SPLINE_CURVE((1.,0.951056516295154,1.,0.951056516295154,1.,0.951056516295154,
1.,0.951056516295154,1.,0.951056516295154,1.,0.951056516295154,1.,0.951056516295154,
1.,0.951056516295154,1.,0.951056516295154,1.,0.951056516295154,1.))
REPRESENTATION_ITEM('')
);
#1715=(
BOUNDED_CURVE()
B_SPLINE_CURVE(2,(#304842,#304843,#304844,#304845,#304846,#304847,#304848,
#304849,#304850,#304851,#304852,#304853,#304854,#304855,#304856,#304857,
#304858,#304859,#304860,#304861,#304862),.UNSPECIFIED.,.F.,.F.)
B_SPLINE_CURVE_WITH_KNOTS((3,2,2,2,2,2,2,2,2,2,3),(0.236842105263158,0.242105263157895,
0.247368421052632,0.252631578947369,0.257894736842106,0.263157894736842,
0.268421052631579,0.273684210526316,0.278947368421052,0.28421052631579,
0.289473684210526),.UNSPECIFIED.)
CURVE()
GEOMETRIC_REPRESENTATION_ITEM()
RATIONAL_B_SPLINE_CURVE((1.,0.951056516295154,1.,0.951056516295154,1.,0.951056516295154,
1.,0.951056516295154,1.,0.951056516295154,1.,0.951056516295154,1.,0.951056516295154,
1.,0.951056516295154,1.,0.951056516295154,1.,0.951056516295154,1.))
REPRESENTATION_ITEM('')
);
#1716=(
BOUNDED_CURVE()
B_SPLINE_CURVE(2,(#304863,#304864,#304865,#304866,#304867,#304868,#304869,
#304870,#304871,#304872,#304873,#304874,#304875,#304876,#304877,#304878,
#304879,#304880,#304881,#304882,#304883),.UNSPECIFIED.,.F.,.F.)
B_SPLINE_CURVE_WITH_KNOTS((3,2,2,2,2,2,2,2,2,2,3),(0.236842105263158,0.242105263157895,
0.247368421052632,0.252631578947369,0.257894736842106,0.263157894736842,
0.268421052631579,0.273684210526316,0.278947368421052,0.28421052631579,
0.289473684210526),.UNSPECIFIED.)
CURVE()
GEOMETRIC_REPRESENTATION_ITEM()
RATIONAL_B_SPLINE_CURVE((1.,0.951056516295154,1.,0.951056516295154,1.,0.951056516295154,
1.,0.951056516295154,1.,0.951056516295154,1.,0.951056516295154,1.,0.951056516295154,
1.,0.951056516295154,1.,0.951056516295154,1.,0.951056516295154,1.))
REPRESENTATION_ITEM('')
);
#1717=(
BOUNDED_CURVE()
B_SPLINE_CURVE(2,(#304888,#304889,#304890,#304891,#304892,#304893,#304894,
#304895,#304896,#304897,#304898,#304899,#304900,#304901,#304902,#304903,
#304904,#304905,#304906,#304907,#304908),.UNSPECIFIED.,.F.,.F.)
B_SPLINE_CURVE_WITH_KNOTS((3,2,2,2,2,2,2,2,2,2,3),(0.18421052631579,0.189473684210526,
0.194736842105263,0.2,0.205263157894737,0.210526315789474,0.215789473684211,
0.221052631578948,0.226315789473684,0.231578947368421,0.236842105263158),
 .UNSPECIFIED.)
CURVE()
GEOMETRIC_REPRESENTATION_ITEM()
RATIONAL_B_SPLINE_CURVE((1.,0.951056516295154,1.,0.951056516295154,1.,0.951056516295154,
1.,0.951056516295154,1.,0.951056516295154,1.,0.951056516295154,1.,0.951056516295154,
1.,0.951056516295154,1.,0.951056516295154,1.,0.951056516295154,1.))
REPRESENTATION_ITEM('')
);
#1718=(
BOUNDED_CURVE()
B_SPLINE_CURVE(2,(#304909,#304910,#304911,#304912,#304913,#304914,#304915,
#304916,#304917,#304918,#304919,#304920,#304921,#304922,#304923,#304924,
#304925,#304926,#304927,#304928,#304929),.UNSPECIFIED.,.F.,.F.)
B_SPLINE_CURVE_WITH_KNOTS((3,2,2,2,2,2,2,2,2,2,3),(0.18421052631579,0.189473684210526,
0.194736842105263,0.2,0.205263157894737,0.210526315789474,0.215789473684211,
0.221052631578948,0.226315789473685,0.231578947368421,0.236842105263158),
 .UNSPECIFIED.)
CURVE()
GEOMETRIC_REPRESENTATION_ITEM()
RATIONAL_B_SPLINE_CURVE((1.,0.951056516295154,1.,0.951056516295154,1.,0.951056516295154,
1.,0.951056516295154,1.,0.951056516295154,1.,0.951056516295154,1.,0.951056516295154,
1.,0.951056516295154,1.,0.951056516295154,1.,0.951056516295154,1.))
REPRESENTATION_ITEM('')
);
#1719=(
BOUNDED_CURVE()
B_SPLINE_CURVE(2,(#304934,#304935,#304936,#304937,#304938,#304939,#304940,
#304941,#304942,#304943,#304944,#304945,#304946,#304947,#304948,#304949,
#304950,#304951,#304952,#304953,#304954),.UNSPECIFIED.,.F.,.F.)
B_SPLINE_CURVE_WITH_KNOTS((3,2,2,2,2,2,2,2,2,2,3),(0.131578947368421,0.136842105263158,
0.142105263157895,0.147368421052632,0.152631578947369,0.157894736842105,
0.163157894736842,0.168421052631579,0.173684210526316,0.178947368421052,
0.18421052631579),.UNSPECIFIED.)
CURVE()
GEOMETRIC_REPRESENTATION_ITEM()
RATIONAL_B_SPLINE_CURVE((1.,0.951056516295154,1.,0.951056516295154,1.,0.951056516295154,
1.,0.951056516295154,1.,0.951056516295154,1.,0.951056516295154,1.,0.951056516295154,
1.,0.951056516295154,1.,0.951056516295154,1.,0.951056516295154,1.))
REPRESENTATION_ITEM('')
);
#1720=(
BOUNDED_CURVE()
B_SPLINE_CURVE(2,(#304955,#304956,#304957,#304958,#304959,#304960,#304961,
#304962,#304963,#304964,#304965,#304966,#304967,#304968,#304969,#304970,
#304971,#304972,#304973,#304974,#304975),.UNSPECIFIED.,.F.,.F.)
B_SPLINE_CURVE_WITH_KNOTS((3,2,2,2,2,2,2,2,2,2,3),(0.131578947368421,0.136842105263158,
0.142105263157895,0.147368421052632,0.152631578947369,0.157894736842105,
0.163157894736842,0.168421052631579,0.173684210526316,0.178947368421053,
0.18421052631579),.UNSPECIFIED.)
CURVE()
GEOMETRIC_REPRESENTATION_ITEM()
RATIONAL_B_SPLINE_CURVE((1.,0.951056516295154,1.,0.951056516295154,1.,0.951056516295154,
1.,0.951056516295154,1.,0.951056516295154,1.,0.951056516295154,1.,0.951056516295154,
1.,0.951056516295154,1.,0.951056516295154,1.,0.951056516295154,1.))
REPRESENTATION_ITEM('')
);
#1721=(
BOUNDED_CURVE()
B_SPLINE_CURVE(2,(#304980,#304981,#304982,#304983,#304984,#304985,#304986,
#304987,#304988,#304989,#304990,#304991,#304992,#304993,#304994,#304995,
#304996,#304997,#304998,#304999,#305000),.UNSPECIFIED.,.F.,.F.)
B_SPLINE_CURVE_WITH_KNOTS((3,2,2,2,2,2,2,2,2,2,3),(0.0789473684210526,0.0842105263157895,
0.0894736842105263,0.0947368421052632,0.1,0.105263157894737,0.110526315789474,
0.11578947368421,0.121052631578947,0.126315789473684,0.131578947368421),
 .UNSPECIFIED.)
CURVE()
GEOMETRIC_REPRESENTATION_ITEM()
RATIONAL_B_SPLINE_CURVE((1.,0.951056516295154,1.,0.951056516295154,1.,0.951056516295154,
1.,0.951056516295154,1.,0.951056516295154,1.,0.951056516295154,1.,0.951056516295154,
1.,0.951056516295154,1.,0.951056516295154,1.,0.951056516295154,1.))
REPRESENTATION_ITEM('')
);
#1722=(
BOUNDED_CURVE()
B_SPLINE_CURVE(2,(#305001,#305002,#305003,#305004,#305005,#305006,#305007,
#305008,#305009,#305010,#305011,#305012,#305013,#305014,#305015,#305016,
#305017,#305018,#305019,#305020,#305021),.UNSPECIFIED.,.F.,.F.)
B_SPLINE_CURVE_WITH_KNOTS((3,2,2,2,2,2,2,2,2,2,3),(0.0789473684210526,0.0842105263157895,
0.0894736842105263,0.0947368421052632,0.1,0.105263157894737,0.110526315789474,
0.11578947368421,0.121052631578947,0.126315789473684,0.131578947368421),
 .UNSPECIFIED.)
CURVE()
GEOMETRIC_REPRESENTATION_ITEM()
RATIONAL_B_SPLINE_CURVE((1.,0.951056516295154,1.,0.951056516295154,1.,0.951056516295154,
1.,0.951056516295154,1.,0.951056516295154,1.,0.951056516295154,1.,0.951056516295154,
1.,0.951056516295154,1.,0.951056516295154,1.,0.951056516295154,1.))
REPRESENTATION_ITEM('')
);
#1723=(
BOUNDED_CURVE()
B_SPLINE_CURVE(2,(#305028,#305029,#305030,#305031,#305032,#305033,#305034,
#305035,#305036,#305037,#305038,#305039,#305040,#305041,#305042,#305043,
#305044,#305045,#305046),.UNSPECIFIED.,.F.,.F.)
B_SPLINE_CURVE_WITH_KNOTS((3,2,2,2,2,2,2,2,2,3),(0.0316055430258635,0.0368421052631579,
0.0421052631578947,0.0473684210526316,0.0526315789473684,0.0578947368421053,
0.0631578947368421,0.068421052631579,0.0736842105263158,0.0789473684210526),
 .UNSPECIFIED.)
CURVE()
GEOMETRIC_REPRESENTATION_ITEM()
RATIONAL_B_SPLINE_CURVE((0.999507859534149,0.951303836279218,1.,0.951056516295154,
1.,0.951056516295154,1.,0.951056516295154,1.,0.951056516295154,1.,0.951056516295154,
1.,0.951056516295154,1.,0.951056516295154,1.,0.951056516295154,1.))
REPRESENTATION_ITEM('')
);
#1724=(
BOUNDED_CURVE()
B_SPLINE_CURVE(2,(#305047,#305048,#305049,#305050,#305051,#305052,#305053,
#305054,#305055,#305056,#305057,#305058,#305059,#305060,#305061,#305062,
#305063,#305064,#305065,#305066,#305067),.UNSPECIFIED.,.F.,.F.)
B_SPLINE_CURVE_WITH_KNOTS((3,2,2,2,2,2,2,2,2,2,3),(0.0263157894736842,0.031578947368421,
0.0368421052631579,0.0421052631578947,0.0473684210526316,0.0526315789473684,
0.0578947368421053,0.0631578947368421,0.068421052631579,0.0736842105263158,
0.0789473684210526),.UNSPECIFIED.)
CURVE()
GEOMETRIC_REPRESENTATION_ITEM()
RATIONAL_B_SPLINE_CURVE((1.,0.951056516295154,1.,0.951056516295154,1.,0.951056516295154,
1.,0.951056516295154,1.,0.951056516295154,1.,0.951056516295154,1.,0.951056516295154,
1.,0.951056516295154,1.,0.951056516295154,1.,0.951056516295154,1.))
REPRESENTATION_ITEM('')
);
#1725=(
BOUNDED_CURVE()
B_SPLINE_CURVE(2,(#305900,#305901,#305902),.UNSPECIFIED.,.F.,.F.)
B_SPLINE_CURVE_WITH_KNOTS((3,3),(0.0250007074989804,0.0263157894736842),
 .UNSPECIFIED.)
CURVE()
GEOMETRIC_REPRESENTATION_ITEM()
RATIONAL_B_SPLINE_CURVE((0.981652774597819,0.987770708292104,1.))
REPRESENTATION_ITEM('')
);
#1726=(
BOUNDED_CURVE()
B_SPLINE_CURVE(2,(#308874,#308875,#308876),.UNSPECIFIED.,.F.,.F.)
B_SPLINE_CURVE_WITH_KNOTS((3,3),(-2.38479811603073,-1.41769287070735),
 .UNSPECIFIED.)
CURVE()
GEOMETRIC_REPRESENTATION_ITEM()
RATIONAL_B_SPLINE_CURVE((1.77486483496503,1.77486483496502,1.6474352731167))
REPRESENTATION_ITEM('')
);
#1727=(
BOUNDED_CURVE()
B_SPLINE_CURVE(2,(#308877,#308878,#308879),.UNSPECIFIED.,.F.,.F.)
B_SPLINE_CURVE_WITH_KNOTS((3,3),(-3.35190336135413,-2.38479811603074),
 .UNSPECIFIED.)
CURVE()
GEOMETRIC_REPRESENTATION_ITEM()
RATIONAL_B_SPLINE_CURVE((1.6474352731167,1.77486483496503,1.77486483496503))
REPRESENTATION_ITEM('')
);
#1728=(
BOUNDED_CURVE()
B_SPLINE_CURVE(2,(#308882,#308883,#308884),.UNSPECIFIED.,.F.,.F.)
B_SPLINE_CURVE_WITH_KNOTS((3,3),(-2.38479811603074,-1.41769287070735),
 .UNSPECIFIED.)
CURVE()
GEOMETRIC_REPRESENTATION_ITEM()
RATIONAL_B_SPLINE_CURVE((1.77486483496503,1.77486483496503,1.6474352731167))
REPRESENTATION_ITEM('')
);
#1729=(
BOUNDED_CURVE()
B_SPLINE_CURVE(2,(#308885,#308886,#308887),.UNSPECIFIED.,.F.,.F.)
B_SPLINE_CURVE_WITH_KNOTS((3,3),(-3.35190336135412,-2.38479811603073),
 .UNSPECIFIED.)
CURVE()
GEOMETRIC_REPRESENTATION_ITEM()
RATIONAL_B_SPLINE_CURVE((1.6474352731167,1.77486483496503,1.77486483496503))
REPRESENTATION_ITEM('')
);
#1730=(
BOUNDED_CURVE()
B_SPLINE_CURVE(2,(#308890,#308891,#308892),.UNSPECIFIED.,.F.,.F.)
B_SPLINE_CURVE_WITH_KNOTS((3,3),(-2.38479811603073,-1.41769287070735),
 .UNSPECIFIED.)
CURVE()
GEOMETRIC_REPRESENTATION_ITEM()
RATIONAL_B_SPLINE_CURVE((1.77486483496503,1.77486483496503,1.6474352731167))
REPRESENTATION_ITEM('')
);
#1731=(
BOUNDED_CURVE()
B_SPLINE_CURVE(2,(#308893,#308894,#308895),.UNSPECIFIED.,.F.,.F.)
B_SPLINE_CURVE_WITH_KNOTS((3,3),(-3.35190336135412,-2.38479811603073),
 .UNSPECIFIED.)
CURVE()
GEOMETRIC_REPRESENTATION_ITEM()
RATIONAL_B_SPLINE_CURVE((1.6474352731167,1.77486483496503,1.77486483496503))
REPRESENTATION_ITEM('')
);
#1732=(
BOUNDED_CURVE()
B_SPLINE_CURVE(2,(#308898,#308899,#308900),.UNSPECIFIED.,.F.,.F.)
B_SPLINE_CURVE_WITH_KNOTS((3,3),(-2.38479811603073,-1.41769287070735),
 .UNSPECIFIED.)
CURVE()
GEOMETRIC_REPRESENTATION_ITEM()
RATIONAL_B_SPLINE_CURVE((1.77486483496503,1.77486483496503,1.6474352731167))
REPRESENTATION_ITEM('')
);
#1733=(
BOUNDED_CURVE()
B_SPLINE_CURVE(2,(#308901,#308902,#308903),.UNSPECIFIED.,.F.,.F.)
B_SPLINE_CURVE_WITH_KNOTS((3,3),(-3.35190336135412,-2.38479811603073),
 .UNSPECIFIED.)
CURVE()
GEOMETRIC_REPRESENTATION_ITEM()
RATIONAL_B_SPLINE_CURVE((1.6474352731167,1.77486483496502,1.77486483496502))
REPRESENTATION_ITEM('')
);
#1734=(
BOUNDED_CURVE()
B_SPLINE_CURVE(2,(#308906,#308907,#308908),.UNSPECIFIED.,.F.,.F.)
B_SPLINE_CURVE_WITH_KNOTS((3,3),(-2.38479811603073,-1.41769287070735),
 .UNSPECIFIED.)
CURVE()
GEOMETRIC_REPRESENTATION_ITEM()
RATIONAL_B_SPLINE_CURVE((1.77486483496503,1.77486483496503,1.6474352731167))
REPRESENTATION_ITEM('')
);
#1735=(
BOUNDED_CURVE()
B_SPLINE_CURVE(2,(#308909,#308910,#308911),.UNSPECIFIED.,.F.,.F.)
B_SPLINE_CURVE_WITH_KNOTS((3,3),(-3.35190336135413,-2.38479811603073),
 .UNSPECIFIED.)
CURVE()
GEOMETRIC_REPRESENTATION_ITEM()
RATIONAL_B_SPLINE_CURVE((1.6474352731167,1.77486483496503,1.77486483496503))
REPRESENTATION_ITEM('')
);
#1736=(
BOUNDED_CURVE()
B_SPLINE_CURVE(2,(#308914,#308915,#308916),.UNSPECIFIED.,.F.,.F.)
B_SPLINE_CURVE_WITH_KNOTS((3,3),(-3.35190336135412,-2.38479811603073),
 .UNSPECIFIED.)
CURVE()
GEOMETRIC_REPRESENTATION_ITEM()
RATIONAL_B_SPLINE_CURVE((1.6474352731167,1.77486483496503,1.77486483496503))
REPRESENTATION_ITEM('')
);
#1737=(
BOUNDED_CURVE()
B_SPLINE_CURVE(2,(#308917,#308918,#308919),.UNSPECIFIED.,.F.,.F.)
B_SPLINE_CURVE_WITH_KNOTS((3,3),(-2.38479811603073,-1.41769287070735),
 .UNSPECIFIED.)
CURVE()
GEOMETRIC_REPRESENTATION_ITEM()
RATIONAL_B_SPLINE_CURVE((1.77486483496502,1.77486483496502,1.6474352731167))
REPRESENTATION_ITEM('')
);
#3202=(
BOUNDED_SURFACE()
B_SPLINE_SURFACE(1,2,((#305134,#305135,#305136,#305137,#305138,#305139,
#305140,#305141,#305142,#305143,#305144,#305145,#305146,#305147,#305148,
#305149,#305150,#305151,#305152,#305153,#305154,#305155,#305156,#305157,
#305158,#305159,#305160,#305161,#305162,#305163,#305164,#305165,#305166,
#305167,#305168,#305169,#305170,#305171,#305172,#305173,#305174,#305175,
#305176,#305177,#305178,#305179,#305180,#305181,#305182,#305183,#305184,
#305185,#305186,#305187,#305188,#305189,#305190,#305191,#305192,#305193,
#305194,#305195,#305196,#305197,#305198,#305199,#305200,#305201,#305202,
#305203,#305204,#305205,#305206,#305207,#305208,#305209,#305210,#305211,
#305212,#305213,#305214,#305215,#305216,#305217,#305218,#305219,#305220,
#305221,#305222,#305223,#305224,#305225,#305226,#305227,#305228,#305229,
#305230,#305231,#305232,#305233,#305234,#305235,#305236,#305237,#305238,
#305239,#305240,#305241,#305242,#305243,#305244,#305245,#305246,#305247,
#305248,#305249,#305250,#305251,#305252,#305253,#305254,#305255,#305256,
#305257,#305258,#305259,#305260,#305261,#305262,#305263,#305264,#305265,
#305266,#305267,#305268,#305269,#305270,#305271,#305272,#305273,#305274,
#305275,#305276,#305277,#305278,#305279,#305280,#305281,#305282,#305283,
#305284,#305285,#305286,#305287,#305288,#305289,#305290,#305291,#305292,
#305293,#305294,#305295,#305296,#305297,#305298,#305299,#305300,#305301,
#305302,#305303,#305304,#305305,#305306,#305307,#305308,#305309,#305310,
#305311,#305312,#305313,#305314,#305315,#305316,#305317,#305318,#305319,
#305320,#305321,#305322,#305323,#305324,#305325,#305326,#305327,#305328,
#305329,#305330,#305331,#305332,#305333,#305334,#305335,#305336,#305337,
#305338,#305339,#305340,#305341,#305342,#305343,#305344,#305345,#305346,
#305347,#305348,#305349,#305350,#305351,#305352,#305353,#305354,#305355,
#305356,#305357,#305358,#305359,#305360,#305361,#305362,#305363,#305364,
#305365,#305366,#305367,#305368,#305369,#305370,#305371,#305372,#305373,
#305374,#305375,#305376,#305377,#305378,#305379,#305380,#305381,#305382,
#305383,#305384,#305385,#305386,#305387,#305388,#305389,#305390,#305391,
#305392,#305393,#305394,#305395,#305396,#305397,#305398,#305399,#305400,
#305401,#305402,#305403,#305404,#305405,#305406,#305407,#305408,#305409,
#305410,#305411,#305412,#305413,#305414,#305415,#305416,#305417,#305418,
#305419,#305420,#305421,#305422,#305423,#305424,#305425,#305426,#305427,
#305428,#305429,#305430,#305431,#305432,#305433,#305434,#305435,#305436,
#305437,#305438,#305439,#305440,#305441,#305442,#305443,#305444,#305445,
#305446,#305447,#305448,#305449,#305450,#305451,#305452,#305453,#305454,
#305455,#305456,#305457,#305458,#305459,#305460,#305461,#305462,#305463,
#305464,#305465,#305466,#305467,#305468,#305469,#305470,#305471,#305472,
#305473,#305474,#305475,#305476,#305477,#305478,#305479,#305480,#305481,
#305482,#305483,#305484,#305485,#305486,#305487,#305488,#305489,#305490,
#305491,#305492,#305493,#305494,#305495,#305496,#305497,#305498),(#305499,
#305500,#305501,#305502,#305503,#305504,#305505,#305506,#305507,#305508,
#305509,#305510,#305511,#305512,#305513,#305514,#305515,#305516,#305517,
#305518,#305519,#305520,#305521,#305522,#305523,#305524,#305525,#305526,
#305527,#305528,#305529,#305530,#305531,#305532,#305533,#305534,#305535,
#305536,#305537,#305538,#305539,#305540,#305541,#305542,#305543,#305544,
#305545,#305546,#305547,#305548,#305549,#305550,#305551,#305552,#305553,
#305554,#305555,#305556,#305557,#305558,#305559,#305560,#305561,#305562,
#305563,#305564,#305565,#305566,#305567,#305568,#305569,#305570,#305571,
#305572,#305573,#305574,#305575,#305576,#305577,#305578,#305579,#305580,
#305581,#305582,#305583,#305584,#305585,#305586,#305587,#305588,#305589,
#305590,#305591,#305592,#305593,#305594,#305595,#305596,#305597,#305598,
#305599,#305600,#305601,#305602,#305603,#305604,#305605,#305606,#305607,
#305608,#305609,#305610,#305611,#305612,#305613,#305614,#305615,#305616,
#305617,#305618,#305619,#305620,#305621,#305622,#305623,#305624,#305625,
#305626,#305627,#305628,#305629,#305630,#305631,#305632,#305633,#305634,
#305635,#305636,#305637,#305638,#305639,#305640,#305641,#305642,#305643,
#305644,#305645,#305646,#305647,#305648,#305649,#305650,#305651,#305652,
#305653,#305654,#305655,#305656,#305657,#305658,#305659,#305660,#305661,
#305662,#305663,#305664,#305665,#305666,#305667,#305668,#305669,#305670,
#305671,#305672,#305673,#305674,#305675,#305676,#305677,#305678,#305679,
#305680,#305681,#305682,#305683,#305684,#305685,#305686,#305687,#305688,
#305689,#305690,#305691,#305692,#305693,#305694,#305695,#305696,#305697,
#305698,#305699,#305700,#305701,#305702,#305703,#305704,#305705,#305706,
#305707,#305708,#305709,#305710,#305711,#305712,#305713,#305714,#305715,
#305716,#305717,#305718,#305719,#305720,#305721,#305722,#305723,#305724,
#305725,#305726,#305727,#305728,#305729,#305730,#305731,#305732,#305733,
#305734,#305735,#305736,#305737,#305738,#305739,#305740,#305741,#305742,
#305743,#305744,#305745,#305746,#305747,#305748,#305749,#305750,#305751,
#305752,#305753,#305754,#305755,#305756,#305757,#305758,#305759,#305760,
#305761,#305762,#305763,#305764,#305765,#305766,#305767,#305768,#305769,
#305770,#305771,#305772,#305773,#305774,#305775,#305776,#305777,#305778,
#305779,#305780,#305781,#305782,#305783,#305784,#305785,#305786,#305787,
#305788,#305789,#305790,#305791,#305792,#305793,#305794,#305795,#305796,
#305797,#305798,#305799,#305800,#305801,#305802,#305803,#305804,#305805,
#305806,#305807,#305808,#305809,#305810,#305811,#305812,#305813,#305814,
#305815,#305816,#305817,#305818,#305819,#305820,#305821,#305822,#305823,
#305824,#305825,#305826,#305827,#305828,#305829,#305830,#305831,#305832,
#305833,#305834,#305835,#305836,#305837,#305838,#305839,#305840,#305841,
#305842,#305843,#305844,#305845,#305846,#305847,#305848,#305849,#305850,
#305851,#305852,#305853,#305854,#305855,#305856,#305857,#305858,#305859,
#305860,#305861,#305862,#305863)),.UNSPECIFIED.,.F.,.F.,.F.)
B_SPLINE_SURFACE_WITH_KNOTS((2,2),(3,2,2,2,2,2,2,2,2,2,2,2,2,2,2,2,2,2,
2,2,2,2,2,2,2,2,2,2,2,2,2,2,2,2,2,2,2,2,2,2,2,2,2,2,2,2,2,2,2,2,2,2,2,2,
2,2,2,2,2,2,2,2,2,2,2,2,2,2,2,2,2,2,2,2,2,2,2,2,2,2,2,2,2,2,2,2,2,2,2,2,
2,2,2,2,2,2,2,2,2,2,2,2,2,2,2,2,2,2,2,2,2,2,2,2,2,2,2,2,2,2,2,2,2,2,2,2,
2,2,2,2,2,2,2,2,2,2,2,2,2,2,2,2,2,2,2,2,2,2,2,2,2,2,2,2,2,2,2,2,2,2,2,2,
2,2,2,2,2,2,2,2,2,2,2,2,2,2,2,2,2,2,2,2,3),(0.,1.00001329281699),(0.,0.00526315789473684,
0.0105263157894737,0.0157894736842105,0.0210526315789474,0.0263157894736842,
0.031578947368421,0.0368421052631579,0.0421052631578947,0.0473684210526316,
0.0526315789473684,0.0578947368421053,0.0631578947368421,0.068421052631579,
0.0736842105263158,0.0789473684210526,0.0842105263157895,0.0894736842105263,
0.0947368421052632,0.1,0.105263157894737,0.110526315789474,0.11578947368421,
0.121052631578947,0.126315789473684,0.131578947368421,0.136842105263158,
0.142105263157895,0.147368421052632,0.152631578947369,0.157894736842105,
0.163157894736842,0.168421052631579,0.173684210526316,0.178947368421052,
0.18421052631579,0.189473684210526,0.194736842105263,0.2,0.205263157894737,
0.210526315789474,0.215789473684211,0.221052631578948,0.226315789473684,
0.231578947368421,0.236842105263158,0.242105263157895,0.247368421052632,
0.252631578947369,0.257894736842106,0.263157894736842,0.268421052631579,
0.273684210526316,0.278947368421052,0.28421052631579,0.289473684210526,
0.294736842105263,0.3,0.305263157894737,0.310526315789473,0.315789473684211,
0.321052631578947,0.326315789473685,0.331578947368421,0.336842105263158,
0.342105263157895,0.347368421052631,0.352631578947369,0.357894736842105,
0.363157894736842,0.368421052631579,0.373684210526316,0.378947368421053,
0.38421052631579,0.389473684210526,0.394736842105263,0.4,0.405263157894737,
0.410526315789473,0.415789473684211,0.421052631578948,0.426315789473684,
0.431578947368421,0.436842105263158,0.442105263157895,0.447368421052632,
0.452631578947369,0.457894736842105,0.463157894736842,0.468421052631579,
0.473684210526316,0.478947368421053,0.48421052631579,0.489473684210526,
0.494736842105263,0.5,0.505263157894737,0.510526315789474,0.515789473684211,
0.521052631578947,0.526315789473684,0.531578947368421,0.536842105263158,
0.542105263157895,0.547368421052632,0.552631578947369,0.557894736842105,
0.563157894736842,0.568421052631579,0.573684210526316,0.578947368421053,
0.58421052631579,0.589473684210526,0.594736842105263,0.6,0.605263157894737,
0.610526315789474,0.615789473684211,0.621052631578947,0.626315789473684,
0.631578947368421,0.636842105263158,0.642105263157895,0.647368421052632,
0.652631578947369,0.657894736842105,0.663157894736842,0.668421052631579,
0.673684210526316,0.678947368421053,0.68421052631579,0.689473684210526,
0.694736842105263,0.7,0.705263157894737,0.710526315789474,0.715789473684211,
0.721052631578947,0.726315789473684,0.731578947368421,0.736842105263158,
0.742105263157895,0.747368421052632,0.752631578947368,0.757894736842105,
0.763157894736842,0.768421052631579,0.773684210526316,0.778947368421053,
0.78421052631579,0.789473684210526,0.794736842105263,0.8,0.805263157894737,
0.810526315789474,0.815789473684211,0.821052631578947,0.826315789473684,
0.831578947368421,0.836842105263158,0.842105263157895,0.847368421052632,
0.852631578947368,0.857894736842105,0.863157894736842,0.868421052631579,
0.873684210526316,0.878947368421053,0.884210526315789,0.889473684210526,
0.894736842105263,0.9,0.905263157894737,0.910526315789474,0.91578947368421,
0.921052631578947,0.926315789473684,0.931578947368421,0.936842105263158,
0.942105263157895,0.947368421052632,0.952631578947368,0.954890265398446),
 .UNSPECIFIED.)
GEOMETRIC_REPRESENTATION_ITEM()
RATIONAL_B_SPLINE_SURFACE(((1.,0.951056516295154,1.,0.951056516295154,1.,
0.951056516295154,1.,0.951056516295154,1.,0.951056516295154,1.,0.951056516295154,
1.,0.951056516295154,1.,0.951056516295154,1.,0.951056516295154,1.,0.951056516295154,
1.,0.951056516295154,1.,0.951056516295154,1.,0.951056516295154,1.,0.951056516295154,
1.,0.951056516295154,1.,0.951056516295154,1.,0.951056516295154,1.,0.951056516295154,
1.,0.951056516295154,1.,0.951056516295154,1.,0.951056516295154,1.,0.951056516295154,
1.,0.951056516295154,1.,0.951056516295154,1.,0.951056516295154,1.,0.951056516295154,
1.,0.951056516295154,1.,0.951056516295154,1.,0.951056516295154,1.,0.951056516295154,
1.,0.951056516295154,1.,0.951056516295154,1.,0.951056516295154,1.,0.951056516295154,
1.,0.951056516295154,1.,0.951056516295154,1.,0.951056516295154,1.,0.951056516295154,
1.,0.951056516295154,1.,0.951056516295154,1.,0.951056516295154,1.,0.951056516295154,
1.,0.951056516295154,1.,0.951056516295154,1.,0.951056516295154,1.,0.951056516295154,
1.,0.951056516295154,1.,0.951056516295154,1.,0.951056516295154,1.,0.951056516295154,
1.,0.951056516295154,1.,0.951056516295154,1.,0.951056516295154,1.,0.951056516295154,
1.,0.951056516295154,1.,0.951056516295154,1.,0.951056516295154,1.,0.951056516295154,
1.,0.951056516295154,1.,0.951056516295154,1.,0.951056516295154,1.,0.951056516295154,
1.,0.951056516295154,1.,0.951056516295154,1.,0.951056516295154,1.,0.951056516295154,
1.,0.951056516295154,1.,0.951056516295154,1.,0.951056516295154,1.,0.951056516295154,
1.,0.951056516295154,1.,0.951056516295154,1.,0.951056516295154,1.,0.951056516295154,
1.,0.951056516295154,1.,0.951056516295154,1.,0.951056516295154,1.,0.951056516295154,
1.,0.951056516295154,1.,0.951056516295154,1.,0.951056516295154,1.,0.951056516295154,
1.,0.951056516295154,1.,0.951056516295154,1.,0.951056516295154,1.,0.951056516295154,
1.,0.951056516295154,1.,0.951056516295154,1.,0.951056516295154,1.,0.951056516295154,
1.,0.951056516295154,1.,0.951056516295154,1.,0.951056516295154,1.,0.951056516295154,
1.,0.951056516295154,1.,0.951056516295154,1.,0.951056516295154,1.,0.951056516295154,
1.,0.951056516295154,1.,0.951056516295154,1.,0.951056516295154,1.,0.951056516295154,
1.,0.951056516295154,1.,0.951056516295154,1.,0.951056516295154,1.,0.951056516295154,
1.,0.951056516295154,1.,0.951056516295154,1.,0.951056516295154,1.,0.951056516295154,
1.,0.951056516295154,1.,0.951056516295154,1.,0.951056516295154,1.,0.951056516295154,
1.,0.951056516295154,1.,0.951056516295154,1.,0.951056516295154,1.,0.951056516295154,
1.,0.951056516295154,1.,0.951056516295154,1.,0.951056516295154,1.,0.951056516295154,
1.,0.951056516295154,1.,0.951056516295154,1.,0.951056516295154,1.,0.951056516295154,
1.,0.951056516295154,1.,0.951056516295154,1.,0.951056516295154,1.,0.951056516295154,
1.,0.951056516295154,1.,0.951056516295154,1.,0.951056516295154,1.,0.951056516295154,
1.,0.951056516295154,1.,0.951056516295154,1.,0.951056516295154,1.,0.951056516295154,
1.,0.951056516295154,1.,0.951056516295154,1.,0.951056516295154,1.,0.951056516295154,
1.,0.951056516295154,1.,0.951056516295154,1.,0.951056516295154,1.,0.951056516295154,
1.,0.951056516295154,1.,0.951056516295154,1.,0.951056516295154,1.,0.951056516295154,
1.,0.951056516295154,1.,0.951056516295154,1.,0.951056516295154,1.,0.951056516295154,
1.,0.951056516295154,1.,0.951056516295154,1.,0.951056516295154,1.,0.951056516295154,
1.,0.951056516295154,1.,0.951056516295154,1.,0.951056516295154,1.,0.951056516295154,
1.,0.951056516295154,1.,0.951056516295154,1.,0.951056516295154,1.,0.951056516295154,
1.,0.951056516295154,1.,0.951056516295154,1.,0.951056516295154,1.,0.951056516295154,
1.,0.951056516295154,1.,0.951056516295154,1.,0.951056516295154,1.,0.951056516295154,
1.,0.951056516295154,1.,0.951056516295154,1.,0.951056516295154,1.,0.951056516295154,
1.,0.951056516295154,1.,0.951056516295154,1.,0.951056516295154,1.,0.978995883132586,
0.976019617655583),(1.,0.951056516295154,1.,0.951056516295154,1.,0.951056516295154,
1.,0.951056516295154,1.,0.951056516295154,1.,0.951056516295154,1.,0.951056516295154,
1.,0.951056516295154,1.,0.951056516295154,1.,0.951056516295154,1.,0.951056516295154,
1.,0.951056516295154,1.,0.951056516295154,1.,0.951056516295154,1.,0.951056516295154,
1.,0.951056516295154,1.,0.951056516295154,1.,0.951056516295154,1.,0.951056516295154,
1.,0.951056516295154,1.,0.951056516295154,1.,0.951056516295154,1.,0.951056516295154,
1.,0.951056516295154,1.,0.951056516295154,1.,0.951056516295154,1.,0.951056516295154,
1.,0.951056516295154,1.,0.951056516295154,1.,0.951056516295154,1.,0.951056516295154,
1.,0.951056516295154,1.,0.951056516295154,1.,0.951056516295154,1.,0.951056516295154,
1.,0.951056516295154,1.,0.951056516295154,1.,0.951056516295154,1.,0.951056516295154,
1.,0.951056516295154,1.,0.951056516295154,1.,0.951056516295154,1.,0.951056516295154,
1.,0.951056516295154,1.,0.951056516295154,1.,0.951056516295154,1.,0.951056516295154,
1.,0.951056516295154,1.,0.951056516295154,1.,0.951056516295154,1.,0.951056516295154,
1.,0.951056516295154,1.,0.951056516295154,1.,0.951056516295154,1.,0.951056516295154,
1.,0.951056516295154,1.,0.951056516295154,1.,0.951056516295154,1.,0.951056516295154,
1.,0.951056516295154,1.,0.951056516295154,1.,0.951056516295154,1.,0.951056516295154,
1.,0.951056516295154,1.,0.951056516295154,1.,0.951056516295154,1.,0.951056516295154,
1.,0.951056516295154,1.,0.951056516295154,1.,0.951056516295154,1.,0.951056516295154,
1.,0.951056516295154,1.,0.951056516295154,1.,0.951056516295154,1.,0.951056516295154,
1.,0.951056516295154,1.,0.951056516295154,1.,0.951056516295154,1.,0.951056516295154,
1.,0.951056516295154,1.,0.951056516295154,1.,0.951056516295154,1.,0.951056516295154,
1.,0.951056516295154,1.,0.951056516295154,1.,0.951056516295154,1.,0.951056516295154,
1.,0.951056516295154,1.,0.951056516295154,1.,0.951056516295154,1.,0.951056516295154,
1.,0.951056516295154,1.,0.951056516295154,1.,0.951056516295154,1.,0.951056516295154,
1.,0.951056516295154,1.,0.951056516295154,1.,0.951056516295154,1.,0.951056516295154,
1.,0.951056516295154,1.,0.951056516295154,1.,0.951056516295154,1.,0.951056516295154,
1.,0.951056516295154,1.,0.951056516295154,1.,0.951056516295154,1.,0.951056516295154,
1.,0.951056516295154,1.,0.951056516295154,1.,0.951056516295154,1.,0.951056516295154,
1.,0.951056516295154,1.,0.951056516295154,1.,0.951056516295154,1.,0.951056516295154,
1.,0.951056516295154,1.,0.951056516295154,1.,0.951056516295154,1.,0.951056516295154,
1.,0.951056516295154,1.,0.951056516295154,1.,0.951056516295154,1.,0.951056516295154,
1.,0.951056516295154,1.,0.951056516295154,1.,0.951056516295154,1.,0.951056516295154,
1.,0.951056516295154,1.,0.951056516295154,1.,0.951056516295154,1.,0.951056516295154,
1.,0.951056516295154,1.,0.951056516295154,1.,0.951056516295154,1.,0.951056516295154,
1.,0.951056516295154,1.,0.951056516295154,1.,0.951056516295154,1.,0.951056516295154,
1.,0.951056516295154,1.,0.951056516295154,1.,0.951056516295154,1.,0.951056516295154,
1.,0.951056516295154,1.,0.951056516295154,1.,0.951056516295154,1.,0.951056516295154,
1.,0.951056516295154,1.,0.951056516295154,1.,0.951056516295154,1.,0.951056516295154,
1.,0.951056516295154,1.,0.951056516295154,1.,0.951056516295154,1.,0.951056516295154,
1.,0.951056516295154,1.,0.951056516295154,1.,0.951056516295154,1.,0.951056516295154,
1.,0.951056516295154,1.,0.951056516295154,1.,0.951056516295154,1.,0.951056516295154,
1.,0.951056516295154,1.,0.951056516295154,1.,0.951056516295154,1.,0.951056516295154,
1.,0.951056516295154,1.,0.951056516295154,1.,0.951056516295154,1.,0.951056516295154,
1.,0.951056516295154,1.,0.951056516295154,1.,0.951056516295154,1.,0.951056516295154,
1.,0.951056516295154,1.,0.951056516295154,1.,0.951056516295154,1.,0.951056516295154,
1.,0.951056516295154,1.,0.951056516295154,1.,0.978995883132586,0.976019617655583)))
REPRESENTATION_ITEM('')
SURFACE()
);
#3203=(
BOUNDED_SURFACE()
B_SPLINE_SURFACE(1,2,((#305903,#305904,#305905,#305906,#305907,#305908,
#305909,#305910,#305911,#305912,#305913,#305914,#305915,#305916,#305917,
#305918,#305919,#305920,#305921,#305922,#305923,#305924,#305925,#305926,
#305927,#305928,#305929,#305930,#305931,#305932,#305933,#305934,#305935,
#305936,#305937,#305938,#305939,#305940,#305941,#305942,#305943,#305944,
#305945,#305946,#305947,#305948,#305949,#305950,#305951,#305952,#305953,
#305954,#305955,#305956,#305957,#305958,#305959,#305960,#305961,#305962,
#305963,#305964,#305965,#305966,#305967,#305968,#305969,#305970,#305971,
#305972,#305973,#305974,#305975,#305976,#305977,#305978,#305979,#305980,
#305981,#305982,#305983,#305984,#305985,#305986,#305987,#305988,#305989,
#305990,#305991,#305992,#305993,#305994,#305995,#305996,#305997,#305998,
#305999,#306000,#306001,#306002,#306003,#306004,#306005,#306006,#306007,
#306008,#306009,#306010,#306011,#306012,#306013,#306014,#306015,#306016,
#306017,#306018,#306019,#306020,#306021,#306022,#306023,#306024,#306025,
#306026,#306027,#306028,#306029,#306030,#306031,#306032,#306033,#306034,
#306035,#306036,#306037,#306038,#306039,#306040,#306041,#306042,#306043,
#306044,#306045,#306046,#306047,#306048,#306049,#306050,#306051,#306052,
#306053,#306054,#306055,#306056,#306057,#306058,#306059,#306060,#306061,
#306062,#306063,#306064,#306065,#306066,#306067,#306068,#306069,#306070,
#306071,#306072,#306073,#306074,#306075,#306076,#306077,#306078,#306079,
#306080,#306081,#306082,#306083,#306084,#306085,#306086,#306087,#306088,
#306089,#306090,#306091,#306092,#306093,#306094,#306095,#306096,#306097,
#306098,#306099,#306100,#306101,#306102,#306103,#306104,#306105,#306106,
#306107,#306108,#306109,#306110,#306111,#306112,#306113,#306114,#306115,
#306116,#306117,#306118,#306119,#306120,#306121,#306122,#306123,#306124,
#306125,#306126,#306127,#306128,#306129,#306130,#306131,#306132,#306133,
#306134,#306135,#306136,#306137,#306138,#306139,#306140,#306141,#306142,
#306143,#306144,#306145,#306146,#306147,#306148,#306149,#306150,#306151,
#306152,#306153,#306154,#306155,#306156,#306157,#306158,#306159,#306160,
#306161,#306162,#306163,#306164,#306165,#306166,#306167,#306168,#306169,
#306170,#306171,#306172,#306173,#306174,#306175,#306176,#306177,#306178,
#306179,#306180,#306181,#306182,#306183,#306184,#306185,#306186,#306187,
#306188,#306189,#306190,#306191,#306192,#306193,#306194,#306195,#306196,
#306197,#306198,#306199,#306200,#306201,#306202,#306203,#306204,#306205,
#306206,#306207,#306208,#306209,#306210,#306211,#306212,#306213,#306214,
#306215,#306216,#306217,#306218,#306219,#306220,#306221,#306222,#306223,
#306224,#306225,#306226,#306227,#306228,#306229,#306230,#306231,#306232,
#306233,#306234,#306235,#306236,#306237,#306238,#306239,#306240,#306241,
#306242,#306243,#306244,#306245,#306246,#306247,#306248,#306249,#306250,
#306251,#306252,#306253,#306254,#306255,#306256,#306257,#306258,#306259,
#306260,#306261,#306262,#306263,#306264,#306265,#306266,#306267),(#306268,
#306269,#306270,#306271,#306272,#306273,#306274,#306275,#306276,#306277,
#306278,#306279,#306280,#306281,#306282,#306283,#306284,#306285,#306286,
#306287,#306288,#306289,#306290,#306291,#306292,#306293,#306294,#306295,
#306296,#306297,#306298,#306299,#306300,#306301,#306302,#306303,#306304,
#306305,#306306,#306307,#306308,#306309,#306310,#306311,#306312,#306313,
#306314,#306315,#306316,#306317,#306318,#306319,#306320,#306321,#306322,
#306323,#306324,#306325,#306326,#306327,#306328,#306329,#306330,#306331,
#306332,#306333,#306334,#306335,#306336,#306337,#306338,#306339,#306340,
#306341,#306342,#306343,#306344,#306345,#306346,#306347,#306348,#306349,
#306350,#306351,#306352,#306353,#306354,#306355,#306356,#306357,#306358,
#306359,#306360,#306361,#306362,#306363,#306364,#306365,#306366,#306367,
#306368,#306369,#306370,#306371,#306372,#306373,#306374,#306375,#306376,
#306377,#306378,#306379,#306380,#306381,#306382,#306383,#306384,#306385,
#306386,#306387,#306388,#306389,#306390,#306391,#306392,#306393,#306394,
#306395,#306396,#306397,#306398,#306399,#306400,#306401,#306402,#306403,
#306404,#306405,#306406,#306407,#306408,#306409,#306410,#306411,#306412,
#306413,#306414,#306415,#306416,#306417,#306418,#306419,#306420,#306421,
#306422,#306423,#306424,#306425,#306426,#306427,#306428,#306429,#306430,
#306431,#306432,#306433,#306434,#306435,#306436,#306437,#306438,#306439,
#306440,#306441,#306442,#306443,#306444,#306445,#306446,#306447,#306448,
#306449,#306450,#306451,#306452,#306453,#306454,#306455,#306456,#306457,
#306458,#306459,#306460,#306461,#306462,#306463,#306464,#306465,#306466,
#306467,#306468,#306469,#306470,#306471,#306472,#306473,#306474,#306475,
#306476,#306477,#306478,#306479,#306480,#306481,#306482,#306483,#306484,
#306485,#306486,#306487,#306488,#306489,#306490,#306491,#306492,#306493,
#306494,#306495,#306496,#306497,#306498,#306499,#306500,#306501,#306502,
#306503,#306504,#306505,#306506,#306507,#306508,#306509,#306510,#306511,
#306512,#306513,#306514,#306515,#306516,#306517,#306518,#306519,#306520,
#306521,#306522,#306523,#306524,#306525,#306526,#306527,#306528,#306529,
#306530,#306531,#306532,#306533,#306534,#306535,#306536,#306537,#306538,
#306539,#306540,#306541,#306542,#306543,#306544,#306545,#306546,#306547,
#306548,#306549,#306550,#306551,#306552,#306553,#306554,#306555,#306556,
#306557,#306558,#306559,#306560,#306561,#306562,#306563,#306564,#306565,
#306566,#306567,#306568,#306569,#306570,#306571,#306572,#306573,#306574,
#306575,#306576,#306577,#306578,#306579,#306580,#306581,#306582,#306583,
#306584,#306585,#306586,#306587,#306588,#306589,#306590,#306591,#306592,
#306593,#306594,#306595,#306596,#306597,#306598,#306599,#306600,#306601,
#306602,#306603,#306604,#306605,#306606,#306607,#306608,#306609,#306610,
#306611,#306612,#306613,#306614,#306615,#306616,#306617,#306618,#306619,
#306620,#306621,#306622,#306623,#306624,#306625,#306626,#306627,#306628,
#306629,#306630,#306631,#306632)),.UNSPECIFIED.,.F.,.F.,.F.)
B_SPLINE_SURFACE_WITH_KNOTS((2,2),(3,2,2,2,2,2,2,2,2,2,2,2,2,2,2,2,2,2,
2,2,2,2,2,2,2,2,2,2,2,2,2,2,2,2,2,2,2,2,2,2,2,2,2,2,2,2,2,2,2,2,2,2,2,2,
2,2,2,2,2,2,2,2,2,2,2,2,2,2,2,2,2,2,2,2,2,2,2,2,2,2,2,2,2,2,2,2,2,2,2,2,
2,2,2,2,2,2,2,2,2,2,2,2,2,2,2,2,2,2,2,2,2,2,2,2,2,2,2,2,2,2,2,2,2,2,2,2,
2,2,2,2,2,2,2,2,2,2,2,2,2,2,2,2,2,2,2,2,2,2,2,2,2,2,2,2,2,2,2,2,2,2,2,2,
2,2,2,2,2,2,2,2,2,2,2,2,2,2,2,2,2,2,2,2,3),(-9.0530534475071E-6,1.),(0.,
0.00526315789473684,0.0105263157894737,0.0157894736842105,0.0210526315789474,
0.0263157894736842,0.031578947368421,0.0368421052631579,0.0421052631578947,
0.0473684210526316,0.0526315789473684,0.0578947368421053,0.0631578947368421,
0.068421052631579,0.0736842105263158,0.0789473684210526,0.0842105263157895,
0.0894736842105263,0.0947368421052632,0.1,0.105263157894737,0.110526315789474,
0.11578947368421,0.121052631578947,0.126315789473684,0.131578947368421,
0.136842105263158,0.142105263157895,0.147368421052632,0.152631578947369,
0.157894736842105,0.163157894736842,0.168421052631579,0.173684210526316,
0.178947368421052,0.18421052631579,0.189473684210526,0.194736842105263,
0.2,0.205263157894737,0.210526315789474,0.215789473684211,0.221052631578948,
0.226315789473684,0.231578947368421,0.236842105263158,0.242105263157895,
0.247368421052632,0.252631578947369,0.257894736842106,0.263157894736842,
0.268421052631579,0.273684210526316,0.278947368421052,0.28421052631579,
0.289473684210526,0.294736842105263,0.3,0.305263157894737,0.310526315789473,
0.315789473684211,0.321052631578947,0.326315789473685,0.331578947368421,
0.336842105263158,0.342105263157895,0.347368421052631,0.352631578947369,
0.357894736842105,0.363157894736842,0.368421052631579,0.373684210526316,
0.378947368421053,0.38421052631579,0.389473684210526,0.394736842105263,
0.4,0.405263157894737,0.410526315789473,0.415789473684211,0.421052631578948,
0.426315789473684,0.431578947368421,0.436842105263158,0.442105263157895,
0.447368421052632,0.452631578947369,0.457894736842105,0.463157894736842,
0.468421052631579,0.473684210526316,0.478947368421053,0.48421052631579,
0.489473684210526,0.494736842105263,0.5,0.505263157894737,0.510526315789474,
0.515789473684211,0.521052631578947,0.526315789473684,0.531578947368421,
0.536842105263158,0.542105263157895,0.547368421052632,0.552631578947369,
0.557894736842105,0.563157894736842,0.568421052631579,0.573684210526316,
0.578947368421053,0.58421052631579,0.589473684210526,0.594736842105263,
0.6,0.605263157894737,0.610526315789474,0.615789473684211,0.621052631578947,
0.626315789473684,0.631578947368421,0.636842105263158,0.642105263157895,
0.647368421052632,0.652631578947369,0.657894736842105,0.663157894736842,
0.668421052631579,0.673684210526316,0.678947368421053,0.68421052631579,
0.689473684210526,0.694736842105263,0.7,0.705263157894737,0.710526315789474,
0.715789473684211,0.721052631578947,0.726315789473684,0.731578947368421,
0.736842105263158,0.742105263157895,0.747368421052632,0.752631578947368,
0.757894736842105,0.763157894736842,0.768421052631579,0.773684210526316,
0.778947368421053,0.78421052631579,0.789473684210526,0.794736842105263,
0.8,0.805263157894737,0.810526315789474,0.815789473684211,0.821052631578947,
0.826315789473684,0.831578947368421,0.836842105263158,0.842105263157895,
0.847368421052632,0.852631578947368,0.857894736842105,0.863157894736842,
0.868421052631579,0.873684210526316,0.878947368421053,0.884210526315789,
0.889473684210526,0.894736842105263,0.9,0.905263157894737,0.910526315789474,
0.91578947368421,0.921052631578947,0.926315789473684,0.931578947368421,
0.936842105263158,0.942105263157895,0.947368421052632,0.952631578947368,
0.954890272715098),.UNSPECIFIED.)
GEOMETRIC_REPRESENTATION_ITEM()
RATIONAL_B_SPLINE_SURFACE(((1.,0.951056516295154,1.,0.951056516295154,1.,
0.951056516295154,1.,0.951056516295154,1.,0.951056516295154,1.,0.951056516295154,
1.,0.951056516295154,1.,0.951056516295154,1.,0.951056516295154,1.,0.951056516295154,
1.,0.951056516295154,1.,0.951056516295154,1.,0.951056516295154,1.,0.951056516295154,
1.,0.951056516295154,1.,0.951056516295154,1.,0.951056516295154,1.,0.951056516295154,
1.,0.951056516295154,1.,0.951056516295154,1.,0.951056516295154,1.,0.951056516295154,
1.,0.951056516295154,1.,0.951056516295154,1.,0.951056516295154,1.,0.951056516295154,
1.,0.951056516295154,1.,0.951056516295154,1.,0.951056516295154,1.,0.951056516295154,
1.,0.951056516295154,1.,0.951056516295154,1.,0.951056516295154,1.,0.951056516295154,
1.,0.951056516295154,1.,0.951056516295154,1.,0.951056516295154,1.,0.951056516295154,
1.,0.951056516295154,1.,0.951056516295154,1.,0.951056516295154,1.,0.951056516295154,
1.,0.951056516295154,1.,0.951056516295154,1.,0.951056516295154,1.,0.951056516295154,
1.,0.951056516295154,1.,0.951056516295154,1.,0.951056516295154,1.,0.951056516295154,
1.,0.951056516295154,1.,0.951056516295154,1.,0.951056516295154,1.,0.951056516295154,
1.,0.951056516295154,1.,0.951056516295154,1.,0.951056516295154,1.,0.951056516295154,
1.,0.951056516295154,1.,0.951056516295154,1.,0.951056516295154,1.,0.951056516295154,
1.,0.951056516295154,1.,0.951056516295154,1.,0.951056516295154,1.,0.951056516295154,
1.,0.951056516295154,1.,0.951056516295154,1.,0.951056516295154,1.,0.951056516295154,
1.,0.951056516295154,1.,0.951056516295154,1.,0.951056516295154,1.,0.951056516295154,
1.,0.951056516295154,1.,0.951056516295154,1.,0.951056516295154,1.,0.951056516295154,
1.,0.951056516295154,1.,0.951056516295154,1.,0.951056516295154,1.,0.951056516295154,
1.,0.951056516295154,1.,0.951056516295154,1.,0.951056516295154,1.,0.951056516295154,
1.,0.951056516295154,1.,0.951056516295154,1.,0.951056516295154,1.,0.951056516295154,
1.,0.951056516295154,1.,0.951056516295154,1.,0.951056516295154,1.,0.951056516295154,
1.,0.951056516295154,1.,0.951056516295154,1.,0.951056516295154,1.,0.951056516295154,
1.,0.951056516295154,1.,0.951056516295154,1.,0.951056516295154,1.,0.951056516295154,
1.,0.951056516295154,1.,0.951056516295154,1.,0.951056516295154,1.,0.951056516295154,
1.,0.951056516295154,1.,0.951056516295154,1.,0.951056516295154,1.,0.951056516295154,
1.,0.951056516295154,1.,0.951056516295154,1.,0.951056516295154,1.,0.951056516295154,
1.,0.951056516295154,1.,0.951056516295154,1.,0.951056516295154,1.,0.951056516295154,
1.,0.951056516295154,1.,0.951056516295154,1.,0.951056516295154,1.,0.951056516295154,
1.,0.951056516295154,1.,0.951056516295154,1.,0.951056516295154,1.,0.951056516295154,
1.,0.951056516295154,1.,0.951056516295154,1.,0.951056516295154,1.,0.951056516295154,
1.,0.951056516295154,1.,0.951056516295154,1.,0.951056516295154,1.,0.951056516295154,
1.,0.951056516295154,1.,0.951056516295154,1.,0.951056516295154,1.,0.951056516295154,
1.,0.951056516295154,1.,0.951056516295154,1.,0.951056516295154,1.,0.951056516295154,
1.,0.951056516295154,1.,0.951056516295154,1.,0.951056516295154,1.,0.951056516295154,
1.,0.951056516295154,1.,0.951056516295154,1.,0.951056516295154,1.,0.951056516295154,
1.,0.951056516295154,1.,0.951056516295154,1.,0.951056516295154,1.,0.951056516295154,
1.,0.951056516295154,1.,0.951056516295154,1.,0.951056516295154,1.,0.951056516295154,
1.,0.951056516295154,1.,0.951056516295154,1.,0.951056516295154,1.,0.951056516295154,
1.,0.951056516295154,1.,0.951056516295154,1.,0.951056516295154,1.,0.951056516295154,
1.,0.951056516295154,1.,0.951056516295154,1.,0.951056516295154,1.,0.951056516295154,
1.,0.951056516295154,1.,0.951056516295154,1.,0.951056516295154,1.,0.951056516295154,
1.,0.951056516295154,1.,0.951056516295154,1.,0.951056516295154,1.,0.951056516295154,
1.,0.951056516295154,1.,0.951056516295154,1.,0.951056516295154,1.,0.978995815093128,
0.976019598373506),(1.,0.951056516295154,1.,0.951056516295154,1.,0.951056516295154,
1.,0.951056516295154,1.,0.951056516295154,1.,0.951056516295154,1.,0.951056516295154,
1.,0.951056516295154,1.,0.951056516295154,1.,0.951056516295154,1.,0.951056516295154,
1.,0.951056516295154,1.,0.951056516295154,1.,0.951056516295154,1.,0.951056516295154,
1.,0.951056516295154,1.,0.951056516295154,1.,0.951056516295154,1.,0.951056516295154,
1.,0.951056516295154,1.,0.951056516295154,1.,0.951056516295154,1.,0.951056516295154,
1.,0.951056516295154,1.,0.951056516295154,1.,0.951056516295154,1.,0.951056516295154,
1.,0.951056516295154,1.,0.951056516295154,1.,0.951056516295154,1.,0.951056516295154,
1.,0.951056516295154,1.,0.951056516295154,1.,0.951056516295154,1.,0.951056516295154,
1.,0.951056516295154,1.,0.951056516295154,1.,0.951056516295154,1.,0.951056516295154,
1.,0.951056516295154,1.,0.951056516295154,1.,0.951056516295154,1.,0.951056516295154,
1.,0.951056516295154,1.,0.951056516295154,1.,0.951056516295154,1.,0.951056516295154,
1.,0.951056516295154,1.,0.951056516295154,1.,0.951056516295154,1.,0.951056516295154,
1.,0.951056516295154,1.,0.951056516295154,1.,0.951056516295154,1.,0.951056516295154,
1.,0.951056516295154,1.,0.951056516295154,1.,0.951056516295154,1.,0.951056516295154,
1.,0.951056516295154,1.,0.951056516295154,1.,0.951056516295154,1.,0.951056516295154,
1.,0.951056516295154,1.,0.951056516295154,1.,0.951056516295154,1.,0.951056516295154,
1.,0.951056516295154,1.,0.951056516295154,1.,0.951056516295154,1.,0.951056516295154,
1.,0.951056516295154,1.,0.951056516295154,1.,0.951056516295154,1.,0.951056516295154,
1.,0.951056516295154,1.,0.951056516295154,1.,0.951056516295154,1.,0.951056516295154,
1.,0.951056516295154,1.,0.951056516295154,1.,0.951056516295154,1.,0.951056516295154,
1.,0.951056516295154,1.,0.951056516295154,1.,0.951056516295154,1.,0.951056516295154,
1.,0.951056516295154,1.,0.951056516295154,1.,0.951056516295154,1.,0.951056516295154,
1.,0.951056516295154,1.,0.951056516295154,1.,0.951056516295154,1.,0.951056516295154,
1.,0.951056516295154,1.,0.951056516295154,1.,0.951056516295154,1.,0.951056516295154,
1.,0.951056516295154,1.,0.951056516295154,1.,0.951056516295154,1.,0.951056516295154,
1.,0.951056516295154,1.,0.951056516295154,1.,0.951056516295154,1.,0.951056516295154,
1.,0.951056516295154,1.,0.951056516295154,1.,0.951056516295154,1.,0.951056516295154,
1.,0.951056516295154,1.,0.951056516295154,1.,0.951056516295154,1.,0.951056516295154,
1.,0.951056516295154,1.,0.951056516295154,1.,0.951056516295154,1.,0.951056516295154,
1.,0.951056516295154,1.,0.951056516295154,1.,0.951056516295154,1.,0.951056516295154,
1.,0.951056516295154,1.,0.951056516295154,1.,0.951056516295154,1.,0.951056516295154,
1.,0.951056516295154,1.,0.951056516295154,1.,0.951056516295154,1.,0.951056516295154,
1.,0.951056516295154,1.,0.951056516295154,1.,0.951056516295154,1.,0.951056516295154,
1.,0.951056516295154,1.,0.951056516295154,1.,0.951056516295154,1.,0.951056516295154,
1.,0.951056516295154,1.,0.951056516295154,1.,0.951056516295154,1.,0.951056516295154,
1.,0.951056516295154,1.,0.951056516295154,1.,0.951056516295154,1.,0.951056516295154,
1.,0.951056516295154,1.,0.951056516295154,1.,0.951056516295154,1.,0.951056516295154,
1.,0.951056516295154,1.,0.951056516295154,1.,0.951056516295154,1.,0.951056516295154,
1.,0.951056516295154,1.,0.951056516295154,1.,0.951056516295154,1.,0.951056516295154,
1.,0.951056516295154,1.,0.951056516295154,1.,0.951056516295154,1.,0.951056516295154,
1.,0.951056516295154,1.,0.951056516295154,1.,0.951056516295154,1.,0.951056516295154,
1.,0.951056516295154,1.,0.951056516295154,1.,0.951056516295154,1.,0.951056516295154,
1.,0.951056516295154,1.,0.951056516295154,1.,0.951056516295154,1.,0.951056516295154,
1.,0.951056516295154,1.,0.951056516295154,1.,0.951056516295154,1.,0.951056516295154,
1.,0.951056516295154,1.,0.951056516295154,1.,0.978995815093128,0.976019598373506)))
REPRESENTATION_ITEM('')
SURFACE()
);
#6790=B_SPLINE_CURVE_WITH_KNOTS('',3,(#303022,#303023,#303024,#303025,#303026,
#303027,#303028,#303029,#303030,#303031,#303032,#303033,#303034,#303035,
#303036,#303037),.UNSPECIFIED.,.F.,.F.,(4,2,2,2,2,2,2,4),(1.2412134266385,
1.30125065201544,1.44881001361766,1.57542683632653,1.63813614188284,1.76112334826837,
1.8383565168018,1.91232314425083),.UNSPECIFIED.);
#6791=B_SPLINE_CURVE_WITH_KNOTS('',3,(#303042,#303043,#303044,#303045,#303046,
#303047,#303048,#303049,#303050,#303051,#303052,#303053),.UNSPECIFIED.,
 .F.,.F.,(4,2,2,2,2,4),(-0.602485002785239,-0.56859078279277,-0.367777547037733,
-0.175807956195899,-0.0864773397713831,-9.9999999780831E-7),
 .UNSPECIFIED.);
#6792=B_SPLINE_CURVE_WITH_KNOTS('',3,(#303060,#303061,#303062,#303063,#303064,
#303065,#303066,#303067,#303068,#303069,#303070,#303071,#303072,#303073,
#303074,#303075,#303076,#303077,#303078,#303079),.UNSPECIFIED.,.F.,.F.,
(4,2,2,2,2,2,2,2,2,4),(9.9999999701418E-7,0.0982828162925184,0.198026929183757,
0.38987455053706,0.594158820502547,0.77621883872625,0.866427631156547,1.04319620045318,
1.12898218312396,1.2412134266385),.UNSPECIFIED.);
#6793=B_SPLINE_CURVE_WITH_KNOTS('',3,(#303080,#303081,#303082,#303083,#303084,
#303085,#303086,#303087,#303088,#303089,#303090,#303091,#303092,#303093,
#303094,#303095,#303096,#303097,#303098,#303099,#303100,#303101,#303102,
#303103,#303104,#303105,#303106,#303107,#303108,#303109,#303110,#303111,
#303112,#303113,#303114,#303115,#303116,#303117,#303118,#303119),
 .UNSPECIFIED.,.F.,.F.,(4,2,2,2,2,2,2,2,2,2,2,2,2,2,2,2,2,2,2,4),(-3.42352177914162,
-3.36362658540771,-3.17690405027184,-2.99916395534607,-2.81491387816524,
-2.63585257564751,-2.45959577200563,-2.37188103111418,-2.19724000665655,
-2.02164462696103,-1.84975793686824,-1.76568449365736,-1.59640410954265,
-1.51180981583268,-1.34684855225214,-1.26283489210883,-1.10262428644002,
-0.938110474064238,-0.759074924884252,-0.602485002785239),.UNSPECIFIED.);
#6794=B_SPLINE_CURVE_WITH_KNOTS('',3,(#303125,#303126,#303127,#303128,#303129,
#303130,#303131,#303132,#303133,#303134,#303135,#303136,#303137,#303138,
#303139,#303140),.UNSPECIFIED.,.F.,.F.,(4,2,2,2,2,2,2,4),(9.99999999548357E-7,
0.139379921907621,0.277528623112359,0.510933121482433,0.744693179008006,
0.981547966045232,1.21378437584703,1.41773894915106),.UNSPECIFIED.);
#6795=B_SPLINE_CURVE_WITH_KNOTS('',3,(#303143,#303144,#303145,#303146,#303147,
#303148,#303149,#303150,#303151,#303152,#303153,#303154),.UNSPECIFIED.,
 .F.,.F.,(4,2,2,2,2,4),(61.0968842008273,61.0995937956945,61.3385697502591,
61.5709030970278,61.8062941894517,62.0430454361303),.UNSPECIFIED.);
#6796=B_SPLINE_CURVE_WITH_KNOTS('',3,(#303159,#303160,#303161,#303162,#303163,
#303164,#303165,#303166,#303167,#303168,#303169,#303170,#303171,#303172,
#303173,#303174,#303175,#303176,#303177,#303178,#303179,#303180,#303181,
#303182,#303183,#303184,#303185,#303186,#303187,#303188,#303189,#303190,
#303191,#303192,#303193,#303194),.UNSPECIFIED.,.F.,.F.,(4,2,2,2,2,2,2,2,
2,2,2,2,2,2,2,2,2,4),(1.41773894915106,1.45035486160213,1.6851967078116,
1.9178182494756,2.15620987025867,2.38913584240912,2.62348141723324,2.85976986412203,
3.0919410577353,3.32946420051038,3.56378499678541,3.79673459079611,4.03457860182644,
4.26716989015402,4.50224336087877,4.73801127084836,4.97026347926577,5.20262344011782),
 .UNSPECIFIED.);
#6797=B_SPLINE_CURVE_WITH_KNOTS('',3,(#303195,#303196,#303197,#303198,#303199,
#303200,#303201,#303202,#303203,#303204,#303205,#303206,#303207,#303208,
#303209,#303210,#303211,#303212,#303213,#303214,#303215,#303216,#303217,
#303218,#303219,#303220,#303221,#303222,#303223,#303224,#303225,#303226,
#303227,#303228,#303229,#303230),.UNSPECIFIED.,.F.,.F.,(4,2,2,2,2,2,2,2,
2,2,2,2,2,2,2,2,2,4),(57.3134340037929,57.3438788675244,57.5817073246283,
57.8145114738983,58.0488146074359,58.2861002964137,58.5181826423711,58.7544597317251,
58.9886213519691,59.2215184693227,59.4599014470676,59.6923979942522,59.9272282660549,
60.1635828267512,60.3957516150036,60.6326001141031,60.8661989335085,61.0968842008273),
 .UNSPECIFIED.);
#6798=B_SPLINE_CURVE_WITH_KNOTS('',3,(#303235,#303236,#303237,#303238,#303239,
#303240,#303241,#303242,#303243,#303244,#303245,#303246,#303247,#303248,
#303249,#303250,#303251,#303252,#303253,#303254,#303255,#303256,#303257,
#303258,#303259,#303260,#303261,#303262,#303263,#303264,#303265,#303266,
#303267,#303268,#303269,#303270,#303271,#303272),.UNSPECIFIED.,.F.,.F.,
(4,2,2,2,2,2,2,2,2,2,2,2,2,2,2,2,2,2,4),(5.20262344011782,5.20886345742205,
5.44271682375074,5.67612586248115,5.91348234838391,6.14589222000662,6.38180674084541,
6.61711861249481,6.84958963116392,7.08847725119523,7.32180057772338,7.55566394593537,
7.79242943844311,8.02465593652442,8.2613946873114,8.49615433278052,8.7288349619442,
8.96713950524592,8.98804835001342),.UNSPECIFIED.);
#6799=B_SPLINE_CURVE_WITH_KNOTS('',3,(#303273,#303274,#303275,#303276,#303277,
#303278,#303279,#303280,#303281,#303282,#303283,#303284,#303285,#303286,
#303287,#303288,#303289,#303290,#303291,#303292,#303293,#303294,#303295,
#303296,#303297,#303298,#303299,#303300,#303301,#303302,#303303,#303304,
#303305,#303306,#303307,#303308),.UNSPECIFIED.,.F.,.F.,(4,2,2,2,2,2,2,2,
2,2,2,2,2,2,2,2,2,4),(53.5296384471268,53.5876019606723,53.8243393699444,
54.0580154468014,54.2913052178265,54.5301667613154,54.7625089863747,54.9977916571498,
55.2334884215121,55.4658257577282,55.7031570515923,55.9364027204056,56.1702297701125,
56.4085764206654,56.640718837193,56.8764677959731,57.1113380070465,57.3134340037929),
 .UNSPECIFIED.);
#6800=B_SPLINE_CURVE_WITH_KNOTS('',3,(#303313,#303314,#303315,#303316,#303317,
#303318,#303319,#303320,#303321,#303322,#303323,#303324,#303325,#303326,
#303327,#303328,#303329,#303330,#303331,#303332,#303333,#303334,#303335,
#303336,#303337,#303338,#303339,#303340,#303341,#303342,#303343,#303344,
#303345,#303346,#303347,#303348),.UNSPECIFIED.,.F.,.F.,(4,2,2,2,2,2,2,2,
2,2,2,2,2,2,2,2,2,4),(8.98804835001342,9.20000803763523,9.43448334015654,
9.67068900303869,9.90287577614595,10.140591592428,10.3748382650961,10.6078712165112,
10.8456372745515,11.0781976407607,11.3134230786598,11.5491181338964,11.7814110000215,
12.0202212096964,12.2540116065607,12.4875248599571,12.7248157635537,12.7733801753947),
 .UNSPECIFIED.);
#6801=B_SPLINE_CURVE_WITH_KNOTS('',3,(#303349,#303350,#303351,#303352,#303353,
#303354,#303355,#303356,#303357,#303358,#303359,#303360,#303361,#303362,
#303363,#303364,#303365,#303366,#303367,#303368,#303369,#303370,#303371,
#303372,#303373,#303374,#303375,#303376,#303377,#303378,#303379,#303380,
#303381,#303382,#303383,#303384),.UNSPECIFIED.,.F.,.F.,(4,2,2,2,2,2,2,2,
2,2,2,2,2,2,2,2,2,4),(49.746329667915,49.8327292191111,50.0683827642741,
50.30337982278,50.5358649718823,50.7735928734603,51.0064554122485,51.2406622802839,
51.4781147625736,51.7101878221121,51.9463600519697,52.1806257300522,52.4134409835382,
52.6517147664406,52.8842452908403,53.1189716647374,53.3554678492974,53.5296384471268),
 .UNSPECIFIED.);
#6802=B_SPLINE_CURVE_WITH_KNOTS('',3,(#303389,#303390,#303391,#303392,#303393,
#303394,#303395,#303396,#303397,#303398,#303399,#303400,#303401,#303402,
#303403,#303404,#303405,#303406,#303407,#303408,#303409,#303410,#303411,
#303412,#303413,#303414,#303415,#303416,#303417,#303418,#303419,#303420,
#303421,#303422,#303423,#303424),.UNSPECIFIED.,.F.,.F.,(4,2,2,2,2,2,2,2,
2,2,2,2,2,2,2,2,2,4),(12.7733801753947,12.9572214265519,13.1933040723328,
13.4285561614687,13.6610902013302,13.8999129782384,14.1331853642295,14.3671810276077,
14.6038850340275,14.8361313833642,15.073066783886,15.3077721416732,15.5405409570327,
15.778786945767,16.0116287043582,16.2462620388275,16.4824132974095,16.5591900771066),
 .UNSPECIFIED.);
#6803=B_SPLINE_CURVE_WITH_KNOTS('',3,(#303425,#303426,#303427,#303428,#303429,
#303430,#303431,#303432,#303433,#303434,#303435,#303436,#303437,#303438,
#303439,#303440,#303441,#303442,#303443,#303444,#303445,#303446,#303447,
#303448,#303449,#303450,#303451,#303452,#303453,#303454,#303455,#303456,
#303457,#303458,#303459,#303460),.UNSPECIFIED.,.F.,.F.,(4,2,2,2,2,2,2,2,
2,2,2,2,2,2,2,2,2,4),(45.9623756797133,46.0761295473086,46.3107783205002,
46.5474476123326,46.7795766717039,47.0162292218167,47.2500134623971,47.4832269185953,
47.7220001181863,47.9543809031078,48.1895807664551,48.425421304983,48.6577296129388,
48.8949722396374,49.1282975779197,49.3620390544388,49.6005709483308,49.746329667915),
 .UNSPECIFIED.);
#6804=B_SPLINE_CURVE_WITH_KNOTS('',3,(#303465,#303466,#303467,#303468,#303469,
#303470,#303471,#303472,#303473,#303474,#303475,#303476,#303477,#303478,
#303479,#303480,#303481,#303482,#303483,#303484,#303485,#303486,#303487,
#303488,#303489,#303490,#303491,#303492,#303493,#303494,#303495,#303496,
#303497,#303498,#303499,#303500),.UNSPECIFIED.,.F.,.F.,(4,2,2,2,2,2,2,2,
2,2,2,2,2,2,2,2,2,4),(16.5591900771066,16.7146453262928,16.9525810732934,
17.1867819106692,17.4199266177265,17.6576436449791,17.8902036038456,18.1256081763627,
18.3612591412948,18.593621717838,18.8326679852899,19.0664240237015,19.30006893957,
19.5373235019442,19.7697549242191,20.0060316137086,20.24125296691,20.3456492025429),
 .UNSPECIFIED.);
#6805=B_SPLINE_CURVE_WITH_KNOTS('',3,(#303501,#303502,#303503,#303504,#303505,
#303506,#303507,#303508,#303509,#303510,#303511,#303512,#303513,#303514,
#303515,#303516,#303517,#303518,#303519,#303520,#303521,#303522,#303523,
#303524,#303525,#303526,#303527,#303528,#303529,#303530,#303531,#303532,
#303533,#303534,#303535,#303536),.UNSPECIFIED.,.F.,.F.,(4,2,2,2,2,2,2,2,
2,2,2,2,2,2,2,2,2,4),(42.178594420686,42.3197673512826,42.5534505985734,
42.7921972991454,43.0244011651343,43.2599866101189,43.4951403754128,43.7275997075312,
43.9652544313537,44.1982051996161,44.4323426165456,44.669992571529,44.9020862234648,
45.1381803472536,45.3725806597471,45.6053435710459,45.8435349737313,45.9623756797133),
 .UNSPECIFIED.);
#6806=B_SPLINE_CURVE_WITH_KNOTS('',3,(#303541,#303542,#303543,#303544,#303545,
#303546,#303547,#303548,#303549,#303550,#303551,#303552,#303553,#303554,
#303555,#303556,#303557,#303558,#303559,#303560,#303561,#303562,#303563,
#303564,#303565,#303566,#303567,#303568,#303569,#303570,#303571,#303572,
#303573,#303574,#303575,#303576),.UNSPECIFIED.,.F.,.F.,(4,2,2,2,2,2,2,2,
2,2,2,2,2,2,2,2,2,4),(20.3456492025429,20.4738781967648,20.7126658502402,
20.9459188409693,21.1800731686911,21.4167451846275,21.6490409199683,21.886197356947,
22.120877696677,22.3537619853571,22.5919793857185,22.8248255987001,23.0596419467705,
23.2957685294054,23.5280745178391,23.7662528620981,24.0004373054574,24.1324102092935),
 .UNSPECIFIED.);
#6807=B_SPLINE_CURVE_WITH_KNOTS('',3,(#303577,#303578,#303579,#303580,#303581,
#303582,#303583,#303584,#303585,#303586,#303587,#303588,#303589,#303590,
#303591,#303592,#303593,#303594,#303595,#303596,#303597,#303598,#303599,
#303600,#303601,#303602,#303603,#303604,#303605,#303606,#303607,#303608,
#303609,#303610,#303611,#303612),.UNSPECIFIED.,.F.,.F.,(4,2,2,2,2,2,2,2,
2,2,2,2,2,2,2,2,2,4),(38.3941558264512,38.5636470016297,38.7963883805231,
39.0345262052207,39.2672136511948,39.501812999719,39.7386832552294,39.9708371668894,
40.2074331234577,40.441354242262,40.674522022043,40.9132353048738,41.145683924188,
41.3808288230391,41.6168420311341,41.8491511752046,42.0863330635504,42.178594420686),
 .UNSPECIFIED.);
#6808=B_SPLINE_CURVE_WITH_KNOTS('',3,(#303617,#303618,#303619,#303620,#303621,
#303622,#303623,#303624,#303625,#303626,#303627,#303628,#303629,#303630,
#303631,#303632,#303633,#303634,#303635,#303636,#303637,#303638,#303639,
#303640,#303641,#303642,#303643,#303644,#303645,#303646,#303647,#303648,
#303649,#303650,#303651,#303652),.UNSPECIFIED.,.F.,.F.,(4,2,2,2,2,2,2,2,
2,2,2,2,2,2,2,2,2,4),(24.1324102092935,24.2337198206622,24.471417950881,
24.7040079669973,24.9396151150109,25.1752518518046,25.407711692159,25.6469416011285,
25.8805802095303,26.1142355494829,26.3513329821338,26.5836726675167,26.8200187049054,
27.055089591229,27.2876863097957,27.5263175344745,27.7594348383616,27.9188908085219),
 .UNSPECIFIED.);
#6809=B_SPLINE_CURVE_WITH_KNOTS('',3,(#303653,#303654,#303655,#303656,#303657,
#303658,#303659,#303660,#303661,#303662,#303663,#303664,#303665,#303666,
#303667,#303668,#303669,#303670,#303671,#303672,#303673,#303674,#303675,
#303676,#303677,#303678,#303679,#303680,#303681,#303682,#303683,#303684,
#303685,#303686,#303687,#303688),.UNSPECIFIED.,.F.,.F.,(4,2,2,2,2,2,2,2,
2,2,2,2,2,2,2,2,2,4),(34.6093522571136,34.8069208845197,35.0392607700812,
35.2764113533711,35.5099816017935,35.743635416534,35.9826219414602,36.2149002384306,
36.4504465708585,36.6857836018368,36.9182476700206,37.1558583806587,37.388925411623,
37.6230218964636,37.8608958248006,38.0930396222172,38.3290842831678,38.3941558264512),
 .UNSPECIFIED.);
#6810=B_SPLINE_CURVE_WITH_KNOTS('',3,(#303693,#303694,#303695,#303696,#303697,
#303698,#303699,#303700,#303701,#303702,#303703,#303704,#303705,#303706,
#303707,#303708,#303709,#303710,#303711,#303712,#303713,#303714,#303715,
#303716,#303717,#303718,#303719,#303720,#303721,#303722,#303723,#303724,
#303725,#303726,#303727,#303728),.UNSPECIFIED.,.F.,.F.,(4,2,2,2,2,2,2,2,
2,2,2,2,2,2,2,2,2,4),(27.9188908085219,27.9936250793838,28.2301448958016,
28.4623720202115,28.6996226455423,28.9341587490645,29.1670376320634,29.4051056835644,
29.6378398263206,29.8727145737872,30.1086967810473,30.3409577709205,30.5792495072044,
30.8132987490559,31.0465966730789,31.281962442723,31.5178689194523,31.7047302987816),
 .UNSPECIFIED.);
#6811=B_SPLINE_CURVE_WITH_KNOTS('',3,(#303729,#303730,#303731,#303732,#303733,
#303734,#303735,#303736,#303737,#303738,#303739,#303740,#303741,#303742,
#303743,#303744,#303745,#303746,#303747,#303748,#303749,#303750,#303751,
#303752,#303753,#303754,#303755,#303756,#303757,#303758,#303759,#303760,
#303761,#303762,#303763,#303764),.UNSPECIFIED.,.F.,.F.,(4,2,2,2,2,2,2,2,
2,2,2,2,2,2,2,2,2,4),(30.8240674906406,31.0500044124221,31.2822268132115,
31.5182518810668,31.7530013759189,31.9857524436451,32.2238668135051,32.4566740448876,
32.6912533841055,32.9283482461933,33.1605563897487,33.397125421422,33.6312092555386,
33.8643629938688,34.1030462650625,34.3355905929265,34.5707097441297,34.6093522571136),
 .UNSPECIFIED.);
#6812=B_SPLINE_CURVE_WITH_KNOTS('',3,(#303769,#303770,#303771,#303772,#303773,
#303774,#303775,#303776,#303777,#303778,#303779,#303780,#303781,#303782,
#303783,#303784,#303785,#303786,#303787,#303788,#303789,#303790,#303791,
#303792,#303793,#303794,#303795,#303796,#303797,#303798,#303799,#303800,
#303801,#303802,#303803,#303804),.UNSPECIFIED.,.F.,.F.,(4,2,2,2,2,2,2,2,
2,2,2,2,2,2,2,2,2,4),(31.7047302987816,31.7503174680194,31.9877297342918,
32.2211478923376,32.455055736683,32.6936366675314,32.925915263179,33.1617406103227,
33.396810498696,33.6294477866019,33.8673509262892,34.1003153669239,34.3346936583478,
34.5722025916434,34.8044070310837,35.0407555989327,35.2751036862081,35.4902881150602),
 .UNSPECIFIED.);
#6813=B_SPLINE_CURVE_WITH_KNOTS('',3,(#303805,#303806,#303807,#303808,#303809,
#303810,#303811,#303812,#303813,#303814,#303815,#303816,#303817,#303818,
#303819,#303820,#303821,#303822,#303823,#303824,#303825,#303826,#303827,
#303828,#303829,#303830,#303831,#303832,#303833,#303834,#303835,#303836,
#303837,#303838,#303839,#303840,#303841,#303842),.UNSPECIFIED.,.F.,.F.,
(4,2,2,2,2,2,2,2,2,2,2,2,2,2,2,2,2,2,4),(27.0389051345726,27.0577126469844,
27.2919955443905,27.5249424930835,27.7627474109057,27.9953103836241,28.2303964626859,
28.4661265986034,28.6983666265183,28.931906239097,29.1710343343977,29.4034142910445,
29.6389514703502,29.8744945422313,30.106993707325,30.3445906542744,30.5777995450349,
30.8118846482967,30.8240674906406),.UNSPECIFIED.);
#6814=B_SPLINE_CURVE_WITH_KNOTS('',3,(#303847,#303848,#303849,#303850,#303851,
#303852,#303853,#303854,#303855,#303856,#303857,#303858,#303859,#303860,
#303861,#303862,#303863,#303864,#303865,#303866,#303867,#303868,#303869,
#303870,#303871,#303872,#303873,#303874,#303875,#303876,#303877,#303878,
#303879,#303880,#303881,#303882,#303883,#303884),.UNSPECIFIED.,.F.,.F.,
(4,2,2,2,2,2,2,2,2,2,2,2,2,2,2,2,2,2,4),(35.4902881150602,35.5080828782027,
35.7465360959528,35.9791791042568,36.2140806323327,36.4506437626019,36.682920550086,
36.9198374361597,37.1536074034736,37.3870717465179,37.6261155342257,37.8585813647829,
38.0940416659604,38.3298180144348,38.5623085529083,38.7998212119301,39.0331731001541,
39.2671780065184,39.2762581355268),.UNSPECIFIED.);
#6815=B_SPLINE_CURVE_WITH_KNOTS('',3,(#303885,#303886,#303887,#303888,#303889,
#303890,#303891,#303892,#303893,#303894,#303895,#303896,#303897,#303898,
#303899,#303900,#303901,#303902,#303903,#303904,#303905,#303906,#303907,
#303908,#303909,#303910,#303911,#303912,#303913,#303914,#303915,#303916,
#303917,#303918,#303919,#303920),.UNSPECIFIED.,.F.,.F.,(4,2,2,2,2,2,2,2,
2,2,2,2,2,2,2,2,2,4),(23.2541689376758,23.2992951913372,23.5346535319949,
23.7670771733799,24.0060152939412,24.2393803367821,24.4731422028082,24.7099556569758,
24.9421686528967,25.1787552585656,25.4135573935473,25.6461708383038,25.8845213198659,
26.1174130189436,26.3517661968063,26.5880146450337,26.8201680131357,27.0389051345726),
 .UNSPECIFIED.);
#6816=B_SPLINE_CURVE_WITH_KNOTS('',3,(#303925,#303926,#303927,#303928,#303929,
#303930,#303931,#303932,#303933,#303934,#303935,#303936,#303937,#303938,
#303939,#303940,#303941,#303942,#303943,#303944,#303945,#303946,#303947,
#303948,#303949,#303950,#303951,#303952,#303953,#303954,#303955,#303956,
#303957,#303958,#303959,#303960),.UNSPECIFIED.,.F.,.F.,(4,2,2,2,2,2,2,2,
2,2,2,2,2,2,2,2,2,4),(39.2762581355268,39.505587894306,39.7378638237339,
39.9737959988975,40.2087529896849,40.4414587798656,40.6794738873387,40.9123934347045,
41.1468791851678,41.3842358822747,41.6164626815893,41.8529272269335,42.087185358293,
42.3202588625291,42.558832393382,42.7914548517187,43.0264712043312,43.0619965343569),
 .UNSPECIFIED.);
#6817=B_SPLINE_CURVE_WITH_KNOTS('',3,(#303961,#303962,#303963,#303964,#303965,
#303966,#303967,#303968,#303969,#303970,#303971,#303972,#303973,#303974,
#303975,#303976,#303977,#303978,#303979,#303980,#303981,#303982,#303983,
#303984,#303985,#303986,#303987,#303988,#303989,#303990,#303991,#303992,
#303993,#303994,#303995,#303996),.UNSPECIFIED.,.F.,.F.,(4,2,2,2,2,2,2,2,
2,2,2,2,2,2,2,2,2,4),(19.4692315614832,19.5413390779448,19.7776909728097,
20.009851950902,20.2472279055292,20.4816056446896,20.7144924661023,20.9523964880157,
21.1850135373671,21.4199709659037,21.6557950630017,21.8880175434394,22.1264558874441,
22.360357963883,22.5936876630703,22.8310950019613,23.0635099516054,23.2541689376758),
 .UNSPECIFIED.);
#6818=B_SPLINE_CURVE_WITH_KNOTS('',3,(#304001,#304002,#304003,#304004,#304005,
#304006,#304007,#304008,#304009,#304010,#304011,#304012,#304013,#304014,
#304015,#304016,#304017,#304018,#304019,#304020,#304021,#304022,#304023,
#304024,#304025,#304026,#304027,#304028,#304029,#304030,#304031,#304032,
#304033,#304034,#304035,#304036),.UNSPECIFIED.,.F.,.F.,(4,2,2,2,2,2,2,2,
2,2,2,2,2,2,2,2,2,4),(43.0619965343569,43.2629074392662,43.4952316912758,
43.7322705239129,43.9659772908775,44.1995586969195,44.4387280250369,44.6711984122979,
44.9067780999182,45.1424571928423,45.3750181490638,45.6126559706163,45.8459728161458,
46.0800990840976,46.3183727020659,46.5506756306829,46.786738618415,46.8485936589711),
 .UNSPECIFIED.);
#6819=B_SPLINE_CURVE_WITH_KNOTS('',3,(#304037,#304038,#304039,#304040,#304041,
#304042,#304043,#304044,#304045,#304046,#304047,#304048,#304049,#304050,
#304051,#304052,#304053,#304054,#304055,#304056,#304057,#304058,#304059,
#304060,#304061,#304062,#304063,#304064,#304065,#304066,#304067,#304068,
#304069,#304070,#304071,#304072),.UNSPECIFIED.,.F.,.F.,(4,2,2,2,2,2,2,2,
2,2,2,2,2,2,2,2,2,4),(15.6839332892533,15.782821791999,16.0203422716166,
16.2528136896479,16.4884851004376,16.7239507514617,16.9563640658718,17.1954154699755,
17.4288840826316,17.6625668779205,17.8994900438865,18.1317360792813,18.3681791547866,
18.6030837995683,18.8356615401653,19.0741198043588,19.3070917790011,19.4692315614832),
 .UNSPECIFIED.);
#6820=B_SPLINE_CURVE_WITH_KNOTS('',3,(#304077,#304078,#304079,#304080,#304081,
#304082,#304083,#304084,#304085,#304086,#304087,#304088,#304089,#304090,
#304091,#304092,#304093,#304094,#304095,#304096,#304097,#304098,#304099,
#304100,#304101,#304102,#304103,#304104,#304105,#304106,#304107,#304108,
#304109,#304110,#304111,#304112),.UNSPECIFIED.,.F.,.F.,(4,2,2,2,2,2,2,2,
2,2,2,2,2,2,2,2,2,4),(46.8485936589711,47.0216159195647,47.2544177903005,
47.4925687723112,47.725474467191,47.9600911742096,48.1973308216091,48.429608940541,
48.666212658611,48.9004139398187,49.1336081306584,49.3723251234082,49.6049574755668,
49.84011146838,50.0764558850996,50.308855490733,50.5460388328585,50.6352088804023),
 .UNSPECIFIED.);
#6821=B_SPLINE_CURVE_WITH_KNOTS('',3,(#304113,#304114,#304115,#304116,#304117,
#304118,#304119,#304120,#304121,#304122,#304123,#304124,#304125,#304126,
#304127,#304128,#304129,#304130,#304131,#304132,#304133,#304134,#304135,
#304136,#304137,#304138,#304139,#304140,#304141,#304142,#304143,#304144,
#304145,#304146,#304147,#304148),.UNSPECIFIED.,.F.,.F.,(4,2,2,2,2,2,2,2,
2,2,2,2,2,2,2,2,2,4),(11.8986040158769,12.0243613207986,12.2629518588974,
12.4960317159484,12.7302055983916,12.9666854476523,13.1988834932273,13.436124648461,
13.6706219597039,13.9034794829757,14.1415078050586,14.374207473683,14.6090685279858,
14.8450118149834,15.0772466276201,15.315531095212,15.5495427343885,15.6839332892533),
 .UNSPECIFIED.);
#6822=B_SPLINE_CURVE_WITH_KNOTS('',3,(#304153,#304154,#304155,#304156,#304157,
#304158,#304159,#304160,#304161,#304162,#304163,#304164,#304165,#304166,
#304167,#304168,#304169,#304170,#304171,#304172,#304173,#304174,#304175,
#304176,#304177,#304178,#304179,#304180,#304181,#304182,#304183,#304184,
#304185,#304186,#304187,#304188),.UNSPECIFIED.,.F.,.F.,(4,2,2,2,2,2,2,2,
2,2,2,2,2,2,2,2,2,4),(50.6352088804023,50.779714911507,51.0134015677832,
51.2525403684392,51.4848974847376,51.7204727123849,51.9559367579735,52.1884492079589,
52.4260870153873,52.6592513558619,52.8933755513534,53.1313949888071,53.3636070129719,
53.5996759364621,53.8343566499005,54.0671348611935,54.3052954975556,54.4208364023182),
 .UNSPECIFIED.);
#6823=B_SPLINE_CURVE_WITH_KNOTS('',3,(#304189,#304190,#304191,#304192,#304193,
#304194,#304195,#304196,#304197,#304198,#304199,#304200,#304201,#304202,
#304203,#304204,#304205,#304206,#304207,#304208,#304209,#304210,#304211,
#304212,#304213,#304214,#304215,#304216,#304217,#304218,#304219,#304220,
#304221,#304222,#304223,#304224),.UNSPECIFIED.,.F.,.F.,(4,2,2,2,2,2,2,2,
2,2,2,2,2,2,2,2,2,4),(8.11239459364437,8.26523226792941,8.50339890780251,
8.73754315172981,8.97080303206172,9.2084601167785,9.44101557047308,9.67660692827371,
9.91220348953535,10.1446362929211,10.3838249059144,10.6174234764245,10.8510593839814,
11.0881161592483,11.3204238869832,11.5567575241936,11.7917887714086,11.8986040158769),
 .UNSPECIFIED.);
#6824=B_SPLINE_CURVE_WITH_KNOTS('',3,(#304229,#304230,#304231,#304232,#304233,
#304234,#304235,#304236,#304237,#304238,#304239,#304240,#304241,#304242,
#304243,#304244,#304245,#304246,#304247,#304248,#304249,#304250,#304251,
#304252,#304253,#304254,#304255,#304256,#304257,#304258,#304259,#304260,
#304261,#304262,#304263,#304264),.UNSPECIFIED.,.F.,.F.,(4,2,2,2,2,2,2,2,
2,2,2,2,2,2,2,2,2,4),(54.4208364023182,54.5380700593176,54.7726933116663,
55.0096991104518,55.2419101196175,55.4785271334105,55.7125550932901,55.9457489905472,
56.1844822360332,56.4170069289476,56.6521732458631,56.8883096099332,57.1206651900448,
57.3578662747796,57.5913950898769,57.825097912479,58.0639871623955,58.2062941786064),
 .UNSPECIFIED.);
#6825=B_SPLINE_CURVE_WITH_KNOTS('',3,(#304265,#304266,#304267,#304268,#304269,
#304270,#304271,#304272,#304273,#304274,#304275,#304276,#304277,#304278,
#304279,#304280,#304281,#304282,#304283,#304284,#304285,#304286,#304287,
#304288,#304289,#304290,#304291,#304292,#304293,#304294,#304295,#304296,
#304297,#304298,#304299,#304300),.UNSPECIFIED.,.F.,.F.,(4,2,2,2,2,2,2,2,
2,2,2,2,2,2,2,2,2,4),(4.32614092106817,4.5074264780588,4.74368643906955,
4.97886575266752,5.21146326404075,5.45020780664062,5.6834205406393,5.9175544876609,
6.15418409958964,6.38644747818929,6.62359002635956,6.85822908616689,7.09108833089345,
7.32926347972645,7.56207220923553,7.79687076043539,8.03295588228145,8.11239459364437),
 .UNSPECIFIED.);
#6826=B_SPLINE_CURVE_WITH_KNOTS('',3,(#304309,#304310,#304311,#304312),
 .UNSPECIFIED.,.F.,.F.,(4,4),(61.9907935238473,62.0594966999548),
 .UNSPECIFIED.);
#6827=B_SPLINE_CURVE_WITH_KNOTS('',3,(#304315,#304316,#304317,#304318,#304319,
#304320,#304321,#304322,#304323,#304324),.UNSPECIFIED.,.F.,.F.,(4,2,2,2,
4),(9.99999995233633E-7,0.139869391385364,0.278811600184122,0.517011378301891,
0.54061986447261),.UNSPECIFIED.);
#6828=B_SPLINE_CURVE_WITH_KNOTS('',3,(#305074,#305075,#305076,#305077,#305078,
#305079,#305080,#305081,#305082,#305083,#305084,#305085,#305086,#305087),
 .UNSPECIFIED.,.F.,.F.,(4,2,2,2,2,2,4),(-0.78047807977081,-0.695301881662505,
-0.593639893486405,-0.425675928226966,-0.218826818693263,-0.10960289024564,
-9.99999999806711E-7),.UNSPECIFIED.);
#6829=B_SPLINE_CURVE_WITH_KNOTS('',3,(#305089,#305090,#305091,#305092,#305093,
#305094,#305095,#305096,#305097,#305098,#305099,#305100,#305101,#305102,
#305103,#305104,#305105,#305106,#305107,#305108,#305109,#305110,#305111,
#305112,#305113,#305114),.UNSPECIFIED.,.F.,.F.,(4,2,2,2,2,2,2,2,2,2,2,2,
4),(-4.05239234980258,-3.93862550091755,-3.82743496185452,-3.59617522122579,
-3.30037507154232,-3.02929753430978,-2.90428875735206,-2.65825727750779,
-2.41593958732872,-2.17055900710192,-1.91716465057545,-1.61902945081212,
-1.46516536274864),.UNSPECIFIED.);
#6830=B_SPLINE_CURVE_WITH_KNOTS('',3,(#305116,#305117,#305118,#305119,#305120,
#305121,#305122,#305123,#305124,#305125,#305126,#305127,#305128,#305129,
#305130,#305131,#305132,#305133),.UNSPECIFIED.,.F.,.F.,(4,2,2,2,2,2,2,2,
4),(-1.46516536274864,-1.34971750991573,-1.10796030676733,-0.986694312735197,
-0.753300167825488,-0.517085622070828,-0.401640164419751,-0.188272205565867,
-9.99999999695689E-7),.UNSPECIFIED.);
#6831=B_SPLINE_CURVE_WITH_KNOTS('',3,(#305864,#305865,#305866,#305867,#305868,
#305869,#305870,#305871,#305872,#305873,#305874,#305875,#305876,#305877,
#305878,#305879,#305880,#305881,#305882,#305883,#305884,#305885,#305886,
#305887,#305888,#305889,#305890,#305891,#305892,#305893,#305894,#305895,
#305896,#305897,#305898,#305899),.UNSPECIFIED.,.F.,.F.,(4,2,2,2,2,2,2,2,
2,2,2,2,2,2,2,2,2,4),(0.54061986447261,0.74981201493592,0.98442493645702,
1.22053124981613,1.45273047421174,1.69065225033218,1.92480945062251,2.15792871651212,
2.39560117799006,2.62812310862901,2.8635094758593,3.09911678414555,3.3314492881675,
3.57048314820672,3.80419695742923,4.03781856148348,4.27503010720451,4.32614092106817),
 .UNSPECIFIED.);
#6832=B_SPLINE_CURVE_WITH_KNOTS('',3,(#306633,#306634,#306635,#306636,#306637,
#306638,#306639,#306640,#306641,#306642,#306643,#306644,#306645,#306646,
#306647,#306648,#306649,#306650,#306651,#306652,#306653,#306654,#306655,
#306656,#306657,#306658,#306659,#306660,#306661,#306662,#306663,#306664,
#306665,#306666,#306667,#306668),.UNSPECIFIED.,.F.,.F.,(4,2,2,2,2,2,2,2,
2,2,2,2,2,2,2,2,2,4),(58.2062941786064,58.2962573272515,58.531858244201,
58.7671282443229,58.9996221986813,59.2372904797072,59.4703266701106,59.7044785679362,
59.9422635556724,60.1744124212493,60.4105174589839,60.6450243103711,60.8778099818224,
61.1160107455192,61.3486800137014,61.5833395502273,61.8201331537292,61.9907935238473),
 .UNSPECIFIED.);
#6833=B_SPLINE_CURVE_WITH_KNOTS('',3,(#306669,#306670,#306671,#306672,#306673,
#306674,#306675,#306676,#306677,#306678,#306679,#306680,#306681,#306682),
 .UNSPECIFIED.,.F.,.F.,(4,2,2,2,2,2,4),(-4.24206895984873,-4.08128650184182,
-3.92521410894753,-3.82989233455649,-3.64245446409652,-3.5499952935536,
-3.42352177914162),.UNSPECIFIED.);
#6834=B_SPLINE_CURVE_WITH_KNOTS('',3,(#306687,#306688,#306689,#306690,#306691,
#306692,#306693,#306694,#306695,#306696,#306697,#306698,#306699,#306700,
#306701,#306702,#306703,#306704,#306705),.UNSPECIFIED.,.F.,.F.,(4,1,1,1,
1,1,1,1,1,1,1,1,1,1,1,1,4),(0.,0.0577170366867072,0.113994474768008,0.16893758423175,
0.224179487123504,0.279968804571931,0.337633163696686,0.397092193126611,
0.459041827583877,0.522525900750905,0.586121573329079,0.650102352916103,
0.71540731027663,0.782762550840158,0.852275272320573,0.924507298607219,
1.),.UNSPECIFIED.);
#6835=B_SPLINE_CURVE_WITH_KNOTS('',3,(#306707,#306708,#306709,#306710,#306711,
#306712,#306713,#306714,#306715,#306716,#306717,#306718,#306719,#306720,
#306721,#306722,#306723,#306724,#306725),.UNSPECIFIED.,.F.,.F.,(4,1,1,1,
1,1,1,1,1,1,1,1,1,1,1,1,4),(0.,0.0768723536038944,0.150603343572851,0.220876273582275,
0.288315870518755,0.35395225660761,0.418604106617997,0.481972048717606,
0.545247561534372,0.606993813632933,0.665860906234417,0.723420981486814,
0.778433488719744,0.833552283298071,0.88813757158342,0.943362448943921,
1.),.UNSPECIFIED.);
#6836=B_SPLINE_CURVE_WITH_KNOTS('',3,(#306727,#306728,#306729,#306730,#306731,
#306732,#306733,#306734,#306735,#306736,#306737,#306738,#306739,#306740,
#306741,#306742,#306743,#306744,#306745),.UNSPECIFIED.,.F.,.F.,(4,1,1,1,
1,1,1,1,1,1,1,1,1,1,1,1,4),(0.,0.0580692684342556,0.114001303445375,0.169772099070702,
0.224674954494909,0.280054150165824,0.336957215314267,0.395112576113712,
0.456649482459617,0.519182398591372,0.582165728137028,0.645753825355143,
0.710908012329458,0.778341319290106,0.848949505917864,0.922850140892551,
1.),.UNSPECIFIED.);
#6837=B_SPLINE_CURVE_WITH_KNOTS('',3,(#306746,#306747,#306748,#306749,#306750,
#306751,#306752,#306753,#306754,#306755,#306756,#306757,#306758,#306759,
#306760,#306761,#306762,#306763,#306764),.UNSPECIFIED.,.F.,.F.,(4,1,1,1,
1,1,1,1,1,1,1,1,1,1,1,1,4),(0.,0.0766164418639844,0.150101977842741,0.220268821680907,
0.287483908975341,0.35290178839726,0.417338409308383,0.480866360224848,
0.543808187325834,0.605854592868513,0.665047756996982,0.722013651121557,
0.777789178028364,0.832724479504672,0.887128050755955,0.942855781853261,
1.),.UNSPECIFIED.);
#6838=B_SPLINE_CURVE_WITH_KNOTS('',3,(#306768,#306769,#306770,#306771,#306772,
#306773,#306774,#306775,#306776,#306777,#306778),.UNSPECIFIED.,.F.,.F.,
(4,1,1,1,1,1,1,1,4),(0.,0.113035127206385,0.22352787461649,0.337812984577189,
0.462304974001557,0.590889524052717,0.720496476039469,0.855414628911259,
1.),.UNSPECIFIED.);
#6839=B_SPLINE_CURVE_WITH_KNOTS('',3,(#306780,#306781,#306782,#306783,#306784,
#306785,#306786,#306787,#306788,#306789,#306790),.UNSPECIFIED.,.F.,.F.,
(4,1,1,1,1,1,1,1,4),(0.,0.153975786043391,0.294620990206987,0.425952943236339,
0.551063084753368,0.669883873511439,0.780296648018842,0.888858324162197,
1.),.UNSPECIFIED.);
#6840=B_SPLINE_CURVE_WITH_KNOTS('',3,(#306792,#306793,#306794,#306795,#306796,
#306797,#306798,#306799,#306800,#306801,#306802),.UNSPECIFIED.,.F.,.F.,
(4,1,1,1,1,1,1,1,4),(0.,0.113008663357688,0.223447121007772,0.335763095333029,
0.457240997711765,0.584219963833153,0.714811315114105,0.851997802140335,
1.),.UNSPECIFIED.);
#6841=B_SPLINE_CURVE_WITH_KNOTS('',3,(#306803,#306804,#306805,#306806,#306807,
#306808,#306809,#306810,#306811,#306812,#306813),.UNSPECIFIED.,.F.,.F.,
(4,1,1,1,1,1,1,1,4),(0.,0.149379665294656,0.288273014687601,0.418942648167458,
0.547753389590675,0.670496533301504,0.782663672045753,0.890203158268387,
1.),.UNSPECIFIED.);
#6842=B_SPLINE_CURVE_WITH_KNOTS('',3,(#306817,#306818,#306819,#306820,#306821,
#306822,#306823,#306824,#306825,#306826,#306827,#306828,#306829,#306830,
#306831,#306832,#306833,#306834,#306835),.UNSPECIFIED.,.F.,.F.,(4,1,1,1,
1,1,1,1,1,1,1,1,1,1,1,1,4),(0.,0.0577170366867072,0.113994474768008,0.16893758423175,
0.224179487123505,0.279968804571931,0.337633163696686,0.397092193126611,
0.459041827583877,0.522525900750905,0.586121573329079,0.650102352916103,
0.71540731027663,0.782762550840158,0.852275272320572,0.924507298607219,
1.),.UNSPECIFIED.);
#6843=B_SPLINE_CURVE_WITH_KNOTS('',3,(#306837,#306838,#306839,#306840,#306841,
#306842,#306843,#306844,#306845,#306846,#306847,#306848,#306849,#306850,
#306851,#306852,#306853,#306854,#306855),.UNSPECIFIED.,.F.,.F.,(4,1,1,1,
1,1,1,1,1,1,1,1,1,1,1,1,4),(0.,0.0768723536038944,0.150603343572851,0.220876273582275,
0.288315870518755,0.35395225660761,0.418604106617997,0.481972048717605,
0.545247561534372,0.606993813632933,0.665860906234417,0.723420981486814,
0.778433488719744,0.833552283298071,0.88813757158342,0.943362448943921,
1.),.UNSPECIFIED.);
#6844=B_SPLINE_CURVE_WITH_KNOTS('',3,(#306857,#306858,#306859,#306860,#306861,
#306862,#306863,#306864,#306865,#306866,#306867,#306868,#306869,#306870,
#306871,#306872,#306873,#306874,#306875),.UNSPECIFIED.,.F.,.F.,(4,1,1,1,
1,1,1,1,1,1,1,1,1,1,1,1,4),(0.,0.0580692684342556,0.114001303445375,0.169772099070702,
0.224674954494909,0.280054150165824,0.336957215314267,0.395112576113712,
0.456649482459617,0.519182398591372,0.582165728137028,0.645753825355143,
0.710908012329458,0.778341319290106,0.848949505917864,0.922850140892551,
1.),.UNSPECIFIED.);
#6845=B_SPLINE_CURVE_WITH_KNOTS('',3,(#306876,#306877,#306878,#306879,#306880,
#306881,#306882,#306883,#306884,#306885,#306886,#306887,#306888,#306889,
#306890,#306891,#306892,#306893,#306894),.UNSPECIFIED.,.F.,.F.,(4,1,1,1,
1,1,1,1,1,1,1,1,1,1,1,1,4),(0.,0.0766164418639844,0.150101977842741,0.220268821680907,
0.287483908975341,0.35290178839726,0.417338409308383,0.480866360224848,
0.543808187325834,0.605854592868513,0.665047756996982,0.722013651121557,
0.777789178028364,0.832724479504672,0.887128050755955,0.942855781853261,
1.),.UNSPECIFIED.);
#6846=B_SPLINE_CURVE_WITH_KNOTS('',3,(#306898,#306899,#306900,#306901,#306902,
#306903,#306904,#306905,#306906,#306907,#306908),.UNSPECIFIED.,.F.,.F.,
(4,1,1,1,1,1,1,1,4),(0.,0.113035127206385,0.22352787461649,0.337812984577189,
0.462304974001557,0.590889524052717,0.720496476039469,0.855414628911259,
1.),.UNSPECIFIED.);
#6847=B_SPLINE_CURVE_WITH_KNOTS('',3,(#306910,#306911,#306912,#306913,#306914,
#306915,#306916,#306917,#306918,#306919,#306920),.UNSPECIFIED.,.F.,.F.,
(4,1,1,1,1,1,1,1,4),(0.,0.153975786043391,0.294620990206987,0.42595294323634,
0.551063084753368,0.669883873511439,0.780296648018842,0.888858324162197,
1.),.UNSPECIFIED.);
#6848=B_SPLINE_CURVE_WITH_KNOTS('',3,(#306922,#306923,#306924,#306925,#306926,
#306927,#306928,#306929,#306930,#306931,#306932),.UNSPECIFIED.,.F.,.F.,
(4,1,1,1,1,1,1,1,4),(0.,0.113008663357688,0.223447121007772,0.335763095333029,
0.457240997711765,0.584219963833153,0.714811315114105,0.851997802140335,
1.),.UNSPECIFIED.);
#6849=B_SPLINE_CURVE_WITH_KNOTS('',3,(#306933,#306934,#306935,#306936,#306937,
#306938,#306939,#306940,#306941,#306942,#306943),.UNSPECIFIED.,.F.,.F.,
(4,1,1,1,1,1,1,1,4),(0.,0.149379665294656,0.288273014687601,0.418942648167458,
0.547753389590675,0.670496533301504,0.782663672045753,0.890203158268387,
1.),.UNSPECIFIED.);
#6850=B_SPLINE_CURVE_WITH_KNOTS('',3,(#306985,#306986,#306987,#306988,#306989,
#306990,#306991,#306992,#306993,#306994,#306995,#306996,#306997,#306998,
#306999,#307000,#307001,#307002,#307003),.UNSPECIFIED.,.F.,.F.,(4,1,1,1,
1,1,1,1,1,1,1,1,1,1,1,1,4),(0.,0.0771498591074487,0.151050494082136,0.221658680709894,
0.289091987670543,0.354246174644858,0.417834271862972,0.480817601408628,
0.543350517540383,0.604887423886288,0.663042784685733,0.719945849834176,
0.775325045505091,0.830227900929299,0.885998696554625,0.941930731565744,
1.),.UNSPECIFIED.);
#6851=B_SPLINE_CURVE_WITH_KNOTS('',3,(#307044,#307045,#307046,#307047,#307048,
#307049,#307050,#307051,#307052,#307053,#307054,#307055,#307056,#307057,
#307058,#307059,#307060,#307061,#307062),.UNSPECIFIED.,.F.,.F.,(4,1,1,1,
1,1,1,1,1,1,1,1,1,1,1,1,4),(-1.,-0.942855781853261,-0.887128050755955,-0.832724479504672,
-0.777789178028364,-0.722013651121557,-0.665047756996982,-0.605854592868513,
-0.543808187325834,-0.480866360224848,-0.417338409308383,-0.35290178839726,
-0.287483908975341,-0.220268821680907,-0.150101977842741,-0.0766164418639844,
0.),.UNSPECIFIED.);
#6852=B_SPLINE_CURVE_WITH_KNOTS('',3,(#307103,#307104,#307105,#307106,#307107,
#307108,#307109,#307110,#307111,#307112,#307113,#307114,#307115,#307116,
#307117,#307118,#307119,#307120,#307121),.UNSPECIFIED.,.F.,.F.,(4,1,1,1,
1,1,1,1,1,1,1,1,1,1,1,1,4),(0.,0.075492701392781,0.147724727679427,0.217237449159842,
0.284592689723369,0.349897647083897,0.413878426670921,0.477474099249095,
0.540958172416123,0.602907806873388,0.662366836303314,0.72003119542807,
0.775820512876496,0.83106241576825,0.886005525231993,0.942282963313293,
1.),.UNSPECIFIED.);
#6853=B_SPLINE_CURVE_WITH_KNOTS('',3,(#307161,#307162,#307163,#307164,#307165,
#307166,#307167,#307168,#307169,#307170,#307171,#307172,#307173,#307174,
#307175,#307176,#307177,#307178,#307179),.UNSPECIFIED.,.F.,.F.,(4,1,1,1,
1,1,1,1,1,1,1,1,1,1,1,1,4),(0.,0.0566375510560788,0.11186242841658,0.166447716701929,
0.221566511280256,0.276579018513186,0.334139093765582,0.393006186367067,
0.454752438465628,0.518027951282394,0.581395893382003,0.646047743392391,
0.711684129481244,0.779123726417726,0.849396656427148,0.923127646396106,
1.),.UNSPECIFIED.);
#6854=B_SPLINE_CURVE_WITH_KNOTS('',3,(#307205,#307206,#307207,#307208,#307209,
#307210,#307211,#307212,#307213,#307214,#307215),.UNSPECIFIED.,.F.,.F.,
(4,1,1,1,1,1,1,1,4),(0.,0.148002197859665,0.285188684885895,0.415780036166847,
0.542759002288235,0.664236904666971,0.776552878992228,0.886991336642312,
1.),.UNSPECIFIED.);
#6855=B_SPLINE_CURVE_WITH_KNOTS('',3,(#307240,#307241,#307242,#307243,#307244,
#307245,#307246,#307247,#307248,#307249,#307250),.UNSPECIFIED.,.F.,.F.,
(4,1,1,1,1,1,1,1,4),(0.,0.109796841731613,0.217336327954247,0.329503466698497,
0.452246610409325,0.581057351832542,0.711726985312399,0.850620334705344,
1.),.UNSPECIFIED.);
#6856=B_SPLINE_CURVE_WITH_KNOTS('',3,(#307275,#307276,#307277,#307278,#307279,
#307280,#307281,#307282,#307283,#307284,#307285),.UNSPECIFIED.,.F.,.F.,
(4,1,1,1,1,1,1,1,4),(0.,0.144585371088741,0.279503523960531,0.409110475947283,
0.537695025998443,0.662187015422811,0.77647212538351,0.886964872793615,
1.),.UNSPECIFIED.);
#6857=B_SPLINE_CURVE_WITH_KNOTS('',3,(#307309,#307310,#307311,#307312,#307313,
#307314,#307315,#307316,#307317,#307318,#307319),.UNSPECIFIED.,.F.,.F.,
(4,1,1,1,1,1,1,1,4),(0.,0.111141675837803,0.219703351981158,0.330116126488561,
0.448936915246632,0.57404705676366,0.705379009793014,0.846024213956609,
1.),.UNSPECIFIED.);
#6858=B_SPLINE_CURVE_WITH_KNOTS('',3,(#307361,#307362,#307363,#307364,#307365,
#307366,#307367,#307368,#307369,#307370,#307371,#307372,#307373,#307374,
#307375,#307376,#307377,#307378,#307379),.UNSPECIFIED.,.F.,.F.,(4,1,1,1,
1,1,1,1,1,1,1,1,1,1,1,1,4),(0.,0.0771498591074487,0.151050494082136,0.221658680709894,
0.289091987670542,0.354246174644858,0.417834271862972,0.480817601408628,
0.543350517540383,0.604887423886288,0.663042784685733,0.719945849834176,
0.775325045505091,0.830227900929299,0.885998696554625,0.941930731565744,
1.),.UNSPECIFIED.);
#6859=B_SPLINE_CURVE_WITH_KNOTS('',3,(#307420,#307421,#307422,#307423,#307424,
#307425,#307426,#307427,#307428,#307429,#307430,#307431,#307432,#307433,
#307434,#307435,#307436,#307437,#307438),.UNSPECIFIED.,.F.,.F.,(4,1,1,1,
1,1,1,1,1,1,1,1,1,1,1,1,4),(-1.,-0.942855781853261,-0.887128050755955,-0.832724479504672,
-0.777789178028364,-0.722013651121557,-0.665047756996982,-0.605854592868513,
-0.543808187325834,-0.480866360224848,-0.417338409308383,-0.35290178839726,
-0.287483908975341,-0.220268821680907,-0.150101977842741,-0.0766164418639844,
0.),.UNSPECIFIED.);
#6860=B_SPLINE_CURVE_WITH_KNOTS('',3,(#307479,#307480,#307481,#307482,#307483,
#307484,#307485,#307486,#307487,#307488,#307489,#307490,#307491,#307492,
#307493,#307494,#307495,#307496,#307497),.UNSPECIFIED.,.F.,.F.,(4,1,1,1,
1,1,1,1,1,1,1,1,1,1,1,1,4),(0.,0.075492701392781,0.147724727679427,0.217237449159842,
0.284592689723369,0.349897647083897,0.413878426670921,0.477474099249095,
0.540958172416123,0.602907806873388,0.662366836303314,0.72003119542807,
0.775820512876496,0.83106241576825,0.886005525231992,0.942282963313293,
1.),.UNSPECIFIED.);
#6861=B_SPLINE_CURVE_WITH_KNOTS('',3,(#307537,#307538,#307539,#307540,#307541,
#307542,#307543,#307544,#307545,#307546,#307547,#307548,#307549,#307550,
#307551,#307552,#307553,#307554,#307555),.UNSPECIFIED.,.F.,.F.,(4,1,1,1,
1,1,1,1,1,1,1,1,1,1,1,1,4),(0.,0.0566375510560786,0.11186242841658,0.16644771670193,
0.221566511280256,0.276579018513186,0.334139093765582,0.393006186367067,
0.454752438465629,0.518027951282395,0.581395893382003,0.646047743392391,
0.711684129481244,0.779123726417726,0.849396656427148,0.923127646396106,
1.),.UNSPECIFIED.);
#6862=B_SPLINE_CURVE_WITH_KNOTS('',3,(#307581,#307582,#307583,#307584,#307585,
#307586,#307587,#307588,#307589,#307590,#307591),.UNSPECIFIED.,.F.,.F.,
(4,1,1,1,1,1,1,1,4),(0.,0.148002197859665,0.285188684885895,0.415780036166847,
0.542759002288235,0.664236904666971,0.776552878992228,0.886991336642312,
1.),.UNSPECIFIED.);
#6863=B_SPLINE_CURVE_WITH_KNOTS('',3,(#307616,#307617,#307618,#307619,#307620,
#307621,#307622,#307623,#307624,#307625,#307626),.UNSPECIFIED.,.F.,.F.,
(4,1,1,1,1,1,1,1,4),(0.,0.109796841731613,0.217336327954247,0.329503466698497,
0.452246610409325,0.581057351832542,0.711726985312399,0.850620334705344,
1.),.UNSPECIFIED.);
#6864=B_SPLINE_CURVE_WITH_KNOTS('',3,(#307651,#307652,#307653,#307654,#307655,
#307656,#307657,#307658,#307659,#307660,#307661),.UNSPECIFIED.,.F.,.F.,
(4,1,1,1,1,1,1,1,4),(0.,0.144585371088741,0.279503523960531,0.409110475947283,
0.537695025998443,0.662187015422811,0.77647212538351,0.886964872793615,
1.),.UNSPECIFIED.);
#6865=B_SPLINE_CURVE_WITH_KNOTS('',3,(#307685,#307686,#307687,#307688,#307689,
#307690,#307691,#307692,#307693,#307694,#307695),.UNSPECIFIED.,.F.,.F.,
(4,1,1,1,1,1,1,1,4),(0.,0.111141675837803,0.219703351981158,0.330116126488562,
0.448936915246632,0.57404705676366,0.705379009793014,0.846024213956609,
1.),.UNSPECIFIED.);
#6866=B_SPLINE_CURVE_WITH_KNOTS('',3,(#307699,#307700,#307701,#307702,#307703,
#307704,#307705,#307706,#307707,#307708,#307709),.UNSPECIFIED.,.F.,.F.,
(4,1,1,1,1,1,1,1,4),(0.,0.14381860843526,0.276720184060535,0.40139659054717,
0.520594774062884,0.637293245567233,0.75409807560852,0.873962190826757,
1.),.UNSPECIFIED.);
#6867=B_SPLINE_CURVE_WITH_KNOTS('',3,(#307711,#307712,#307713,#307714,#307715,
#307716,#307717,#307718,#307719,#307720,#307721,#307722,#307723,#307724,
#307725,#307726,#307727,#307728,#307729),.UNSPECIFIED.,.F.,.F.,(4,1,1,1,
1,1,1,1,1,1,1,1,1,1,1,1,4),(-1.,-0.940276800846585,-0.882061797546221,-0.824126149789293,
-0.767064167323289,-0.71022527848224,-0.653190706601446,-0.595069793647295,
-0.535395707628871,-0.475131662182092,-0.41333034849776,-0.350394511043543,
-0.285894163869826,-0.218686839383758,-0.148475385165302,-0.0756779287595513,
0.),.UNSPECIFIED.);
#6868=B_SPLINE_CURVE_WITH_KNOTS('',3,(#307731,#307732,#307733,#307734,#307735,
#307736,#307737,#307738,#307739,#307740,#307741,#307742,#307743,#307744,
#307745,#307746,#307747,#307748,#307749),.UNSPECIFIED.,.F.,.F.,(4,1,1,1,
1,1,1,1,1,1,1,1,1,1,1,1,4),(0.,0.0735593902167768,0.144406880522386,0.212035000612302,
0.277455182895964,0.341240831122113,0.403615225713777,0.465772853725949,
0.527839405900435,0.589271108646648,0.648485061002809,0.706313491571885,
0.763897708792844,0.820995580197687,0.879024456534409,0.938439191447014,
1.),.UNSPECIFIED.);
#6869=B_SPLINE_CURVE_WITH_KNOTS('',3,(#307751,#307752,#307753,#307754,#307755,
#307756,#307757,#307758,#307759,#307760,#307761,#307762,#307763,#307764,
#307765,#307766,#307767,#307768,#307769),.UNSPECIFIED.,.F.,.F.,(4,1,1,1,
1,1,1,1,1,1,1,1,1,1,1,1,4),(0.,0.0612675560073353,0.120821287104165,0.178985698366598,
0.236645059586719,0.294395620729497,0.352792725296381,0.412241000299045,
0.474276810949433,0.536953714018934,0.599593467559458,0.66197417732883,
0.725552076032239,0.790752056360384,0.857809975221741,0.927515627061441,
1.),.UNSPECIFIED.);
#6870=B_SPLINE_CURVE_WITH_KNOTS('',3,(#307771,#307772,#307773,#307774,#307775,
#307776,#307777,#307778,#307779,#307780,#307781,#307782,#307783,#307784,
#307785,#307786,#307787,#307788,#307789),.UNSPECIFIED.,.F.,.F.,(4,1,1,1,
1,1,1,1,1,1,1,1,1,1,1,1,4),(0.,0.0737198727326366,0.143946935064662,0.212133747062962,
0.277912671008997,0.34156704167165,0.403626619899118,0.464825448444965,
0.524706702690351,0.583602784640957,0.642223378321782,0.700523711411864,
0.758512105377773,0.816969451940464,0.876419241746809,0.937592570779656,
1.),.UNSPECIFIED.);
#6871=B_SPLINE_CURVE_WITH_KNOTS('',3,(#307791,#307792,#307793,#307794,#307795,
#307796,#307797,#307798,#307799,#307800,#307801),.UNSPECIFIED.,.F.,.F.,
(4,1,1,1,1,1,1,1,4),(0.,0.129460777681808,0.251364758465844,0.369750478112862,
0.48633159458772,0.605179466580234,0.728807707522854,0.859213949280771,
1.),.UNSPECIFIED.);
#6872=B_SPLINE_CURVE_WITH_KNOTS('',3,(#307803,#307804,#307805,#307806,#307807,
#307808,#307809,#307810,#307811,#307812,#307813,#307814,#307815,#307816,
#307817,#307818,#307819,#307820,#307821),.UNSPECIFIED.,.F.,.F.,(4,1,1,1,
1,1,1,1,1,1,1,1,1,1,1,1,4),(0.,0.0724915710472832,0.142248636949713,0.209709388595723,
0.274857515432795,0.338249555361619,0.400730922620109,0.462891931966943,
0.525566461597643,0.587484469713601,0.64667511935087,0.705219765007066,
0.762798326707908,0.820199705010802,0.878348632650845,0.938420716788534,
1.),.UNSPECIFIED.);
#6873=B_SPLINE_CURVE_WITH_KNOTS('',3,(#307822,#307823,#307824,#307825,#307826,
#307827,#307828,#307829,#307830,#307831,#307832,#307833,#307834,#307835,
#307836,#307837,#307838,#307839,#307840),.UNSPECIFIED.,.F.,.F.,(4,1,1,1,
1,1,1,1,1,1,1,1,1,1,1,1,4),(0.,0.0618009710281554,0.122005337166018,0.18035060128547,
0.237956680350668,0.295993496555078,0.354224180223643,0.413796608373368,
0.475344905905867,0.537628047311842,0.600103014912843,0.662388390250829,
0.725572014773438,0.790351843146754,0.857597742298064,0.927154440774627,
1.),.UNSPECIFIED.);
#6874=B_SPLINE_CURVE_WITH_KNOTS('',3,(#307844,#307845,#307846,#307847,#307848,
#307849,#307850,#307851,#307852,#307853,#307854),.UNSPECIFIED.,.F.,.F.,
(4,1,1,1,1,1,1,1,4),(0.,0.14381860843526,0.276720184060535,0.40139659054717,
0.520594774062884,0.637293245567233,0.75409807560852,0.873962190826756,
1.),.UNSPECIFIED.);
#6875=B_SPLINE_CURVE_WITH_KNOTS('',3,(#307856,#307857,#307858,#307859,#307860,
#307861,#307862,#307863,#307864,#307865,#307866,#307867,#307868,#307869,
#307870,#307871,#307872,#307873,#307874),.UNSPECIFIED.,.F.,.F.,(4,1,1,1,
1,1,1,1,1,1,1,1,1,1,1,1,4),(-1.,-0.940276800846584,-0.882061797546221,-0.824126149789293,
-0.767064167323289,-0.71022527848224,-0.653190706601445,-0.595069793647295,
-0.535395707628871,-0.475131662182092,-0.41333034849776,-0.350394511043543,
-0.285894163869826,-0.218686839383758,-0.148475385165302,-0.0756779287595513,
0.),.UNSPECIFIED.);
#6876=B_SPLINE_CURVE_WITH_KNOTS('',3,(#307876,#307877,#307878,#307879,#307880,
#307881,#307882,#307883,#307884,#307885,#307886,#307887,#307888,#307889,
#307890,#307891,#307892,#307893,#307894),.UNSPECIFIED.,.F.,.F.,(4,1,1,1,
1,1,1,1,1,1,1,1,1,1,1,1,4),(0.,0.0735593902167768,0.144406880522386,0.212035000612302,
0.277455182895964,0.341240831122113,0.403615225713777,0.465772853725949,
0.527839405900435,0.589271108646648,0.648485061002809,0.706313491571885,
0.763897708792844,0.820995580197687,0.879024456534409,0.938439191447014,
1.),.UNSPECIFIED.);
#6877=B_SPLINE_CURVE_WITH_KNOTS('',3,(#307896,#307897,#307898,#307899,#307900,
#307901,#307902,#307903,#307904,#307905,#307906,#307907,#307908,#307909,
#307910,#307911,#307912,#307913,#307914),.UNSPECIFIED.,.F.,.F.,(4,1,1,1,
1,1,1,1,1,1,1,1,1,1,1,1,4),(0.,0.0612675560073353,0.120821287104165,0.178985698366598,
0.236645059586719,0.294395620729497,0.352792725296381,0.412241000299045,
0.474276810949433,0.536953714018934,0.599593467559457,0.66197417732883,
0.725552076032239,0.790752056360384,0.857809975221741,0.927515627061441,
1.),.UNSPECIFIED.);
#6878=B_SPLINE_CURVE_WITH_KNOTS('',3,(#307916,#307917,#307918,#307919,#307920,
#307921,#307922,#307923,#307924,#307925,#307926,#307927,#307928,#307929,
#307930,#307931,#307932,#307933,#307934),.UNSPECIFIED.,.F.,.F.,(4,1,1,1,
1,1,1,1,1,1,1,1,1,1,1,1,4),(0.,0.0737198727326366,0.143946935064662,0.212133747062962,
0.277912671008997,0.34156704167165,0.403626619899117,0.464825448444965,
0.524706702690351,0.583602784640957,0.642223378321781,0.700523711411864,
0.758512105377773,0.816969451940464,0.876419241746809,0.937592570779656,
1.),.UNSPECIFIED.);
#6879=B_SPLINE_CURVE_WITH_KNOTS('',3,(#307936,#307937,#307938,#307939,#307940,
#307941,#307942,#307943,#307944,#307945,#307946),.UNSPECIFIED.,.F.,.F.,
(4,1,1,1,1,1,1,1,4),(0.,0.129460777681808,0.251364758465844,0.369750478112862,
0.48633159458772,0.605179466580234,0.728807707522854,0.859213949280771,
1.),.UNSPECIFIED.);
#6880=B_SPLINE_CURVE_WITH_KNOTS('',3,(#307948,#307949,#307950,#307951,#307952,
#307953,#307954,#307955,#307956,#307957,#307958,#307959,#307960,#307961,
#307962,#307963,#307964,#307965,#307966),.UNSPECIFIED.,.F.,.F.,(4,1,1,1,
1,1,1,1,1,1,1,1,1,1,1,1,4),(0.,0.0724915710472832,0.142248636949713,0.209709388595723,
0.274857515432795,0.33824955536162,0.400730922620109,0.462891931966943,
0.525566461597643,0.587484469713601,0.64667511935087,0.705219765007066,
0.762798326707908,0.820199705010802,0.878348632650845,0.938420716788534,
1.),.UNSPECIFIED.);
#6881=B_SPLINE_CURVE_WITH_KNOTS('',3,(#307967,#307968,#307969,#307970,#307971,
#307972,#307973,#307974,#307975,#307976,#307977,#307978,#307979,#307980,
#307981,#307982,#307983,#307984,#307985),.UNSPECIFIED.,.F.,.F.,(4,1,1,1,
1,1,1,1,1,1,1,1,1,1,1,1,4),(0.,0.0618009710281554,0.122005337166018,0.18035060128547,
0.237956680350668,0.295993496555078,0.354224180223643,0.413796608373368,
0.475344905905867,0.537628047311842,0.600103014912843,0.662388390250829,
0.725572014773438,0.790351843146754,0.857597742298064,0.927154440774627,
1.),.UNSPECIFIED.);
#6882=B_SPLINE_CURVE_WITH_KNOTS('',3,(#308037,#308038,#308039,#308040,#308041,
#308042,#308043,#308044,#308045,#308046,#308047,#308048,#308049,#308050,
#308051,#308052,#308053,#308054,#308055),.UNSPECIFIED.,.F.,.F.,(4,1,1,1,
1,1,1,1,1,1,1,1,1,1,1,1,4),(0.,0.0624074292203441,0.123580758253191,0.183030548059535,
0.241487894622227,0.299476288588136,0.357776621678218,0.416397215359044,
0.475293297309649,0.535174551555035,0.596373380100883,0.65843295832835,
0.722087328991003,0.787866252937039,0.856053064935337,0.926280127267363,
1.),.UNSPECIFIED.);
#6883=B_SPLINE_CURVE_WITH_KNOTS('',3,(#308080,#308081,#308082,#308083,#308084,
#308085,#308086,#308087,#308088,#308089,#308090),.UNSPECIFIED.,.F.,.F.,
(4,1,1,1,1,1,1,1,4),(0.,0.140786050719229,0.271192292477146,0.394820533419766,
0.51366840541228,0.630249521887138,0.748635241534156,0.870539222318192,
1.),.UNSPECIFIED.);
#6884=B_SPLINE_CURVE_WITH_KNOTS('',3,(#308131,#308132,#308133,#308134,#308135,
#308136,#308137,#308138,#308139,#308140,#308141,#308142,#308143,#308144,
#308145,#308146,#308147,#308148,#308149),.UNSPECIFIED.,.F.,.F.,(4,1,1,1,
1,1,1,1,1,1,1,1,1,1,1,1,4),(0.,0.061579283211466,0.121651367349155,0.179800294989198,
0.237201673292092,0.294780234992934,0.353324880649131,0.412515530286399,
0.474433538402357,0.537108068033057,0.599269077379891,0.66175044463838,
0.725142484567205,0.790290611404277,0.857751363050287,0.927508428952717,
1.),.UNSPECIFIED.);
#6885=B_SPLINE_CURVE_WITH_KNOTS('',3,(#308190,#308191,#308192,#308193,#308194,
#308195,#308196,#308197,#308198,#308199,#308200,#308201,#308202,#308203,
#308204,#308205,#308206,#308207,#308208),.UNSPECIFIED.,.F.,.F.,(4,1,1,1,
1,1,1,1,1,1,1,1,1,1,1,1,4),(0.,0.0728455592253727,0.142402257701936,0.209648156853246,
0.274427985226561,0.337611609749171,0.399896985087157,0.462371952688158,
0.524655094094133,0.586203391626632,0.645775819776357,0.704006503444922,
0.762043319649332,0.81964939871453,0.877994662833982,0.938199028971844,
1.),.UNSPECIFIED.);
#6886=B_SPLINE_CURVE_WITH_KNOTS('',3,(#308233,#308234,#308235,#308236,#308237,
#308238,#308239,#308240,#308241,#308242,#308243),.UNSPECIFIED.,.F.,.F.,
(4,1,1,1,1,1,1,1,4),(0.,0.126037809173243,0.24590192439148,0.362706754432767,
0.479405225937116,0.59860340945283,0.723279815939465,0.85618139156474,1.),
 .UNSPECIFIED.);
#6887=B_SPLINE_CURVE_WITH_KNOTS('',3,(#308284,#308285,#308286,#308287,#308288,
#308289,#308290,#308291,#308292,#308293,#308294,#308295,#308296,#308297,
#308298,#308299,#308300,#308301,#308302),.UNSPECIFIED.,.F.,.F.,(4,1,1,1,
1,1,1,1,1,1,1,1,1,1,1,1,4),(0.,0.0756779287595513,0.148475385165302,0.218686839383758,
0.285894163869826,0.350394511043543,0.41333034849776,0.475131662182092,
0.535395707628871,0.595069793647295,0.653190706601446,0.71022527848224,
0.767064167323289,0.824126149789293,0.882061797546221,0.940276800846585,
1.),.UNSPECIFIED.);
#6888=B_SPLINE_CURVE_WITH_KNOTS('',3,(#308343,#308344,#308345,#308346,#308347,
#308348,#308349,#308350,#308351,#308352,#308353,#308354,#308355,#308356,
#308357,#308358,#308359,#308360,#308361),.UNSPECIFIED.,.F.,.F.,(4,1,1,1,
1,1,1,1,1,1,1,1,1,1,1,1,4),(0.,0.061560808552986,0.120975543465591,0.179004419802313,
0.236102291207156,0.293686508428115,0.351514938997191,0.410728891353352,
0.472160594099565,0.534227146274051,0.596384774286223,0.658759168877887,
0.722544817104037,0.787964999387698,0.855593119477614,0.926440609783223,
1.),.UNSPECIFIED.);
#6889=B_SPLINE_CURVE_WITH_KNOTS('',3,(#308400,#308401,#308402,#308403,#308404,
#308405,#308406,#308407,#308408,#308409,#308410,#308411,#308412,#308413,
#308414,#308415,#308416,#308417,#308418),.UNSPECIFIED.,.F.,.F.,(4,1,1,1,
1,1,1,1,1,1,1,1,1,1,1,1,4),(0.,0.0724843729385586,0.142190024778259,0.209247943639616,
0.274447923967761,0.33802582267117,0.400406532440542,0.463046285981066,
0.525723189050567,0.587758999700955,0.647207274703619,0.705604379270503,
0.76335494041328,0.821014301633402,0.879178712895835,0.938732443992665,
1.),.UNSPECIFIED.);
#6890=B_SPLINE_CURVE_WITH_KNOTS('',3,(#308461,#308462,#308463,#308464,#308465,
#308466,#308467,#308468,#308469,#308470,#308471,#308472,#308473,#308474,
#308475,#308476,#308477,#308478,#308479),.UNSPECIFIED.,.F.,.F.,(4,1,1,1,
1,1,1,1,1,1,1,1,1,1,1,1,4),(0.,0.0624074292203441,0.123580758253191,0.183030548059535,
0.241487894622227,0.299476288588135,0.357776621678218,0.416397215359044,
0.475293297309649,0.535174551555035,0.596373380100883,0.65843295832835,
0.722087328991003,0.787866252937039,0.856053064935338,0.926280127267363,
1.),.UNSPECIFIED.);
#6891=B_SPLINE_CURVE_WITH_KNOTS('',3,(#308504,#308505,#308506,#308507,#308508,
#308509,#308510,#308511,#308512,#308513,#308514),.UNSPECIFIED.,.F.,.F.,
(4,1,1,1,1,1,1,1,4),(0.,0.140786050719229,0.271192292477146,0.394820533419766,
0.51366840541228,0.630249521887138,0.748635241534156,0.870539222318192,
1.),.UNSPECIFIED.);
#6892=B_SPLINE_CURVE_WITH_KNOTS('',3,(#308555,#308556,#308557,#308558,#308559,
#308560,#308561,#308562,#308563,#308564,#308565,#308566,#308567,#308568,
#308569,#308570,#308571,#308572,#308573),.UNSPECIFIED.,.F.,.F.,(4,1,1,1,
1,1,1,1,1,1,1,1,1,1,1,1,4),(0.,0.061579283211466,0.121651367349155,0.179800294989198,
0.237201673292092,0.294780234992934,0.353324880649131,0.412515530286399,
0.474433538402357,0.537108068033057,0.599269077379891,0.66175044463838,
0.725142484567205,0.790290611404277,0.857751363050287,0.927508428952717,
1.),.UNSPECIFIED.);
#6893=B_SPLINE_CURVE_WITH_KNOTS('',3,(#308614,#308615,#308616,#308617,#308618,
#308619,#308620,#308621,#308622,#308623,#308624,#308625,#308626,#308627,
#308628,#308629,#308630,#308631,#308632),.UNSPECIFIED.,.F.,.F.,(4,1,1,1,
1,1,1,1,1,1,1,1,1,1,1,1,4),(0.,0.0728455592253727,0.142402257701936,0.209648156853246,
0.274427985226561,0.337611609749171,0.399896985087157,0.462371952688158,
0.524655094094133,0.586203391626633,0.645775819776357,0.704006503444922,
0.762043319649332,0.81964939871453,0.877994662833982,0.938199028971844,
1.),.UNSPECIFIED.);
#6894=B_SPLINE_CURVE_WITH_KNOTS('',3,(#308657,#308658,#308659,#308660,#308661,
#308662,#308663,#308664,#308665,#308666,#308667),.UNSPECIFIED.,.F.,.F.,
(4,1,1,1,1,1,1,1,4),(0.,0.126037809173244,0.24590192439148,0.362706754432767,
0.479405225937116,0.59860340945283,0.723279815939465,0.85618139156474,1.),
 .UNSPECIFIED.);
#6895=B_SPLINE_CURVE_WITH_KNOTS('',3,(#308708,#308709,#308710,#308711,#308712,
#308713,#308714,#308715,#308716,#308717,#308718,#308719,#308720,#308721,
#308722,#308723,#308724,#308725,#308726),.UNSPECIFIED.,.F.,.F.,(4,1,1,1,
1,1,1,1,1,1,1,1,1,1,1,1,4),(0.,0.0756779287595513,0.148475385165302,0.218686839383758,
0.285894163869826,0.350394511043543,0.41333034849776,0.475131662182092,
0.535395707628871,0.595069793647295,0.653190706601445,0.71022527848224,
0.767064167323289,0.824126149789293,0.882061797546221,0.940276800846584,
1.),.UNSPECIFIED.);
#6896=B_SPLINE_CURVE_WITH_KNOTS('',3,(#308767,#308768,#308769,#308770,#308771,
#308772,#308773,#308774,#308775,#308776,#308777,#308778,#308779,#308780,
#308781,#308782,#308783,#308784,#308785),.UNSPECIFIED.,.F.,.F.,(4,1,1,1,
1,1,1,1,1,1,1,1,1,1,1,1,4),(0.,0.061560808552986,0.120975543465591,0.179004419802313,
0.236102291207156,0.293686508428115,0.351514938997191,0.410728891353352,
0.472160594099565,0.534227146274051,0.596384774286223,0.658759168877887,
0.722544817104037,0.787964999387698,0.855593119477614,0.926440609783223,
1.),.UNSPECIFIED.);
#6897=B_SPLINE_CURVE_WITH_KNOTS('',3,(#308824,#308825,#308826,#308827,#308828,
#308829,#308830,#308831,#308832,#308833,#308834,#308835,#308836,#308837,
#308838,#308839,#308840,#308841,#308842),.UNSPECIFIED.,.F.,.F.,(4,1,1,1,
1,1,1,1,1,1,1,1,1,1,1,1,4),(0.,0.0724843729385586,0.142190024778259,0.209247943639616,
0.274447923967761,0.33802582267117,0.400406532440542,0.463046285981066,
0.525723189050567,0.587758999700955,0.647207274703619,0.705604379270503,
0.76335494041328,0.821014301633402,0.879178712895835,0.938732443992665,
1.),.UNSPECIFIED.);
#7197=CONICAL_SURFACE('',#104638,6.,0.539306738866249);
#7198=CONICAL_SURFACE('',#104641,6.,0.539306738866249);
#7199=CONICAL_SURFACE('',#104684,4.6875,0.785398163397456);
#7200=CONICAL_SURFACE('',#104705,9.5,1.0471975511966);
#7201=CONICAL_SURFACE('',#104706,9.5,1.0471975511966);
#7202=CONICAL_SURFACE('',#104707,9.5,1.0471975511966);
#7203=CONICAL_SURFACE('',#104708,9.5,1.0471975511966);
#7204=CONICAL_SURFACE('',#104709,9.5,1.0471975511966);
#7205=CONICAL_SURFACE('',#104710,9.5,1.0471975511966);
#7206=CONICAL_SURFACE('',#104719,6.,0.539306738866249);
#7237=SHAPE_REPRESENTATION_RELATIONSHIP('SRR','None',#310912,#7254);
#7254=ADVANCED_BREP_SHAPE_REPRESENTATION('',(#7389),#310621);
#7322=STYLED_ITEM('',(#311008),#7389);
#7389=MANIFOLD_SOLID_BREP('Body1',#93773);
#7696=FACE_BOUND('',#20391,.T.);
#7697=FACE_BOUND('',#20392,.T.);
#7698=FACE_BOUND('',#20394,.T.);
#7699=FACE_BOUND('',#20395,.T.);
#7700=FACE_BOUND('',#20418,.T.);
#7701=FACE_BOUND('',#20419,.T.);
#7702=FACE_BOUND('',#20420,.T.);
#7703=FACE_BOUND('',#20434,.T.);
#8660=PLANE('',#104682);
#8661=PLANE('',#104687);
#8662=PLANE('',#104688);
#8663=PLANE('',#104689);
#8664=PLANE('',#104690);
#8665=PLANE('',#104691);
#8666=PLANE('',#104692);
#8667=PLANE('',#104693);
#8668=PLANE('',#104694);
#8669=PLANE('',#104695);
#8670=PLANE('',#104696);
#8671=PLANE('',#104697);
#8672=PLANE('',#104698);
#8673=PLANE('',#104711);
#8674=PLANE('',#104712);
#8675=PLANE('',#104713);
#8676=PLANE('',#104714);
#8677=PLANE('',#104715);
#8678=PLANE('',#104716);
#8679=PLANE('',#104717);
#14285=FACE_OUTER_BOUND('',#20329,.T.);
#14286=FACE_OUTER_BOUND('',#20330,.T.);
#14287=FACE_OUTER_BOUND('',#20331,.T.);
#14288=FACE_OUTER_BOUND('',#20332,.T.);
#14289=FACE_OUTER_BOUND('',#20333,.T.);
#14290=FACE_OUTER_BOUND('',#20334,.T.);
#14291=FACE_OUTER_BOUND('',#20335,.T.);
#14292=FACE_OUTER_BOUND('',#20336,.T.);
#14293=FACE_OUTER_BOUND('',#20337,.T.);
#14294=FACE_OUTER_BOUND('',#20338,.T.);
#14295=FACE_OUTER_BOUND('',#20339,.T.);
#14296=FACE_OUTER_BOUND('',#20340,.T.);
#14297=FACE_OUTER_BOUND('',#20341,.T.);
#14298=FACE_OUTER_BOUND('',#20342,.T.);
#14299=FACE_OUTER_BOUND('',#20343,.T.);
#14300=FACE_OUTER_BOUND('',#20344,.T.);
#14301=FACE_OUTER_BOUND('',#20345,.T.);
#14302=FACE_OUTER_BOUND('',#20346,.T.);
#14303=FACE_OUTER_BOUND('',#20347,.T.);
#14304=FACE_OUTER_BOUND('',#20348,.T.);
#14305=FACE_OUTER_BOUND('',#20349,.T.);
#14306=FACE_OUTER_BOUND('',#20350,.T.);
#14307=FACE_OUTER_BOUND('',#20351,.T.);
#14308=FACE_OUTER_BOUND('',#20352,.T.);
#14309=FACE_OUTER_BOUND('',#20353,.T.);
#14310=FACE_OUTER_BOUND('',#20354,.T.);
#14311=FACE_OUTER_BOUND('',#20355,.T.);
#14312=FACE_OUTER_BOUND('',#20356,.T.);
#14313=FACE_OUTER_BOUND('',#20357,.T.);
#14314=FACE_OUTER_BOUND('',#20358,.T.);
#14315=FACE_OUTER_BOUND('',#20359,.T.);
#14316=FACE_OUTER_BOUND('',#20360,.T.);
#14317=FACE_OUTER_BOUND('',#20361,.T.);
#14318=FACE_OUTER_BOUND('',#20362,.T.);
#14319=FACE_OUTER_BOUND('',#20363,.T.);
#14320=FACE_OUTER_BOUND('',#20364,.T.);
#14321=FACE_OUTER_BOUND('',#20365,.T.);
#14322=FACE_OUTER_BOUND('',#20366,.T.);
#14323=FACE_OUTER_BOUND('',#20367,.T.);
#14324=FACE_OUTER_BOUND('',#20368,.T.);
#14325=FACE_OUTER_BOUND('',#20369,.T.);
#14326=FACE_OUTER_BOUND('',#20370,.T.);
#14327=FACE_OUTER_BOUND('',#20371,.T.);
#14328=FACE_OUTER_BOUND('',#20372,.T.);
#14329=FACE_OUTER_BOUND('',#20373,.T.);
#14330=FACE_OUTER_BOUND('',#20374,.T.);
#14331=FACE_OUTER_BOUND('',#20375,.T.);
#14332=FACE_OUTER_BOUND('',#20376,.T.);
#14333=FACE_OUTER_BOUND('',#20377,.T.);
#14334=FACE_OUTER_BOUND('',#20378,.T.);
#14335=FACE_OUTER_BOUND('',#20379,.T.);
#14336=FACE_OUTER_BOUND('',#20380,.T.);
#14337=FACE_OUTER_BOUND('',#20381,.T.);
#14338=FACE_OUTER_BOUND('',#20382,.T.);
#14339=FACE_OUTER_BOUND('',#20383,.T.);
#14340=FACE_OUTER_BOUND('',#20384,.T.);
#14341=FACE_OUTER_BOUND('',#20385,.T.);
#14342=FACE_OUTER_BOUND('',#20386,.T.);
#14343=FACE_OUTER_BOUND('',#20387,.T.);
#14344=FACE_OUTER_BOUND('',#20388,.T.);
#14345=FACE_OUTER_BOUND('',#20389,.T.);
#14346=FACE_OUTER_BOUND('',#20390,.T.);
#14347=FACE_OUTER_BOUND('',#20393,.T.);
#14348=FACE_OUTER_BOUND('',#20396,.T.);
#14349=FACE_OUTER_BOUND('',#20397,.T.);
#14350=FACE_OUTER_BOUND('',#20398,.T.);
#14351=FACE_OUTER_BOUND('',#20399,.T.);
#14352=FACE_OUTER_BOUND('',#20400,.T.);
#14353=FACE_OUTER_BOUND('',#20401,.T.);
#14354=FACE_OUTER_BOUND('',#20402,.T.);
#14355=FACE_OUTER_BOUND('',#20403,.T.);
#14356=FACE_OUTER_BOUND('',#20404,.T.);
#14357=FACE_OUTER_BOUND('',#20405,.T.);
#14358=FACE_OUTER_BOUND('',#20406,.T.);
#14359=FACE_OUTER_BOUND('',#20407,.T.);
#14360=FACE_OUTER_BOUND('',#20408,.T.);
#14361=FACE_OUTER_BOUND('',#20409,.T.);
#14362=FACE_OUTER_BOUND('',#20410,.T.);
#14363=FACE_OUTER_BOUND('',#20411,.T.);
#14364=FACE_OUTER_BOUND('',#20412,.T.);
#14365=FACE_OUTER_BOUND('',#20413,.T.);
#14366=FACE_OUTER_BOUND('',#20414,.T.);
#14367=FACE_OUTER_BOUND('',#20415,.T.);
#14368=FACE_OUTER_BOUND('',#20416,.T.);
#14369=FACE_OUTER_BOUND('',#20417,.T.);
#14370=FACE_OUTER_BOUND('',#20421,.T.);
#14371=FACE_OUTER_BOUND('',#20422,.T.);
#14372=FACE_OUTER_BOUND('',#20423,.T.);
#14373=FACE_OUTER_BOUND('',#20424,.T.);
#14374=FACE_OUTER_BOUND('',#20425,.T.);
#14375=FACE_OUTER_BOUND('',#20426,.T.);
#14376=FACE_OUTER_BOUND('',#20427,.T.);
#14377=FACE_OUTER_BOUND('',#20428,.T.);
#14378=FACE_OUTER_BOUND('',#20429,.T.);
#14379=FACE_OUTER_BOUND('',#20430,.T.);
#14380=FACE_OUTER_BOUND('',#20431,.T.);
#14381=FACE_OUTER_BOUND('',#20432,.T.);
#14382=FACE_OUTER_BOUND('',#20433,.T.);
#14383=FACE_OUTER_BOUND('',#20435,.T.);
#14384=FACE_OUTER_BOUND('',#20436,.T.);
#20329=EDGE_LOOP('',(#85011,#85012,#85013,#85014,#85015));
#20330=EDGE_LOOP('',(#85016,#85017,#85018,#85019,#85020));
#20331=EDGE_LOOP('',(#85021,#85022,#85023,#85024));
#20332=EDGE_LOOP('',(#85025,#85026,#85027,#85028));
#20333=EDGE_LOOP('',(#85029,#85030,#85031,#85032));
#20334=EDGE_LOOP('',(#85033,#85034,#85035,#85036));
#20335=EDGE_LOOP('',(#85037,#85038,#85039,#85040));
#20336=EDGE_LOOP('',(#85041,#85042,#85043,#85044));
#20337=EDGE_LOOP('',(#85045,#85046,#85047,#85048));
#20338=EDGE_LOOP('',(#85049,#85050,#85051,#85052));
#20339=EDGE_LOOP('',(#85053,#85054,#85055,#85056));
#20340=EDGE_LOOP('',(#85057,#85058,#85059,#85060));
#20341=EDGE_LOOP('',(#85061,#85062,#85063,#85064));
#20342=EDGE_LOOP('',(#85065,#85066,#85067,#85068));
#20343=EDGE_LOOP('',(#85069,#85070,#85071,#85072));
#20344=EDGE_LOOP('',(#85073,#85074,#85075,#85076));
#20345=EDGE_LOOP('',(#85077,#85078,#85079,#85080));
#20346=EDGE_LOOP('',(#85081,#85082,#85083,#85084));
#20347=EDGE_LOOP('',(#85085,#85086,#85087,#85088,#85089,#85090,#85091,#85092,
#85093));
#20348=EDGE_LOOP('',(#85094,#85095,#85096));
#20349=EDGE_LOOP('',(#85097,#85098,#85099,#85100,#85101));
#20350=EDGE_LOOP('',(#85102,#85103,#85104,#85105));
#20351=EDGE_LOOP('',(#85106,#85107,#85108,#85109));
#20352=EDGE_LOOP('',(#85110,#85111,#85112,#85113));
#20353=EDGE_LOOP('',(#85114,#85115,#85116,#85117));
#20354=EDGE_LOOP('',(#85118,#85119,#85120,#85121));
#20355=EDGE_LOOP('',(#85122,#85123,#85124,#85125));
#20356=EDGE_LOOP('',(#85126,#85127,#85128,#85129));
#20357=EDGE_LOOP('',(#85130,#85131,#85132,#85133));
#20358=EDGE_LOOP('',(#85134,#85135,#85136,#85137));
#20359=EDGE_LOOP('',(#85138,#85139,#85140,#85141));
#20360=EDGE_LOOP('',(#85142,#85143,#85144,#85145));
#20361=EDGE_LOOP('',(#85146,#85147,#85148,#85149));
#20362=EDGE_LOOP('',(#85150,#85151,#85152,#85153));
#20363=EDGE_LOOP('',(#85154,#85155,#85156,#85157));
#20364=EDGE_LOOP('',(#85158,#85159,#85160,#85161,#85162));
#20365=EDGE_LOOP('',(#85163));
#20366=EDGE_LOOP('',(#85164,#85165,#85166,#85167,#85168,#85169,#85170,#85171,
#85172));
#20367=EDGE_LOOP('',(#85173,#85174,#85175,#85176,#85177,#85178,#85179,#85180,
#85181,#85182,#85183,#85184,#85185,#85186,#85187,#85188,#85189,#85190,#85191,
#85192,#85193,#85194,#85195,#85196,#85197,#85198,#85199,#85200,#85201,#85202,
#85203,#85204,#85205,#85206,#85207,#85208,#85209,#85210));
#20368=EDGE_LOOP('',(#85211,#85212,#85213,#85214,#85215,#85216,#85217,#85218,
#85219,#85220,#85221,#85222,#85223,#85224,#85225,#85226,#85227,#85228,#85229,
#85230,#85231,#85232,#85233,#85234,#85235,#85236,#85237,#85238,#85239,#85240,
#85241,#85242,#85243,#85244,#85245,#85246,#85247,#85248,#85249,#85250));
#20369=EDGE_LOOP('',(#85251,#85252,#85253));
#20370=EDGE_LOOP('',(#85254,#85255,#85256,#85257));
#20371=EDGE_LOOP('',(#85258,#85259,#85260,#85261));
#20372=EDGE_LOOP('',(#85262,#85263,#85264,#85265));
#20373=EDGE_LOOP('',(#85266,#85267,#85268,#85269));
#20374=EDGE_LOOP('',(#85270,#85271,#85272,#85273));
#20375=EDGE_LOOP('',(#85274,#85275,#85276,#85277));
#20376=EDGE_LOOP('',(#85278,#85279,#85280,#85281));
#20377=EDGE_LOOP('',(#85282,#85283,#85284,#85285));
#20378=EDGE_LOOP('',(#85286,#85287,#85288,#85289));
#20379=EDGE_LOOP('',(#85290,#85291,#85292,#85293));
#20380=EDGE_LOOP('',(#85294,#85295,#85296,#85297));
#20381=EDGE_LOOP('',(#85298,#85299,#85300,#85301));
#20382=EDGE_LOOP('',(#85302,#85303,#85304,#85305));
#20383=EDGE_LOOP('',(#85306,#85307,#85308,#85309));
#20384=EDGE_LOOP('',(#85310,#85311,#85312,#85313));
#20385=EDGE_LOOP('',(#85314,#85315,#85316,#85317));
#20386=EDGE_LOOP('',(#85318,#85319,#85320,#85321));
#20387=EDGE_LOOP('',(#85322,#85323,#85324,#85325));
#20388=EDGE_LOOP('',(#85326,#85327,#85328,#85329));
#20389=EDGE_LOOP('',(#85330,#85331,#85332,#85333));
#20390=EDGE_LOOP('',(#85334,#85335,#85336,#85337,#85338,#85339,#85340,#85341));
#20391=EDGE_LOOP('',(#85342,#85343,#85344,#85345));
#20392=EDGE_LOOP('',(#85346,#85347,#85348,#85349));
#20393=EDGE_LOOP('',(#85350,#85351,#85352,#85353,#85354,#85355,#85356,#85357));
#20394=EDGE_LOOP('',(#85358,#85359,#85360,#85361));
#20395=EDGE_LOOP('',(#85362,#85363,#85364,#85365));
#20396=EDGE_LOOP('',(#85366,#85367,#85368,#85369));
#20397=EDGE_LOOP('',(#85370,#85371,#85372,#85373));
#20398=EDGE_LOOP('',(#85374,#85375,#85376,#85377));
#20399=EDGE_LOOP('',(#85378,#85379,#85380,#85381));
#20400=EDGE_LOOP('',(#85382,#85383,#85384,#85385));
#20401=EDGE_LOOP('',(#85386,#85387,#85388,#85389));
#20402=EDGE_LOOP('',(#85390,#85391,#85392,#85393));
#20403=EDGE_LOOP('',(#85394,#85395,#85396,#85397));
#20404=EDGE_LOOP('',(#85398,#85399,#85400,#85401));
#20405=EDGE_LOOP('',(#85402,#85403,#85404,#85405));
#20406=EDGE_LOOP('',(#85406,#85407,#85408,#85409));
#20407=EDGE_LOOP('',(#85410,#85411,#85412,#85413));
#20408=EDGE_LOOP('',(#85414,#85415,#85416,#85417));
#20409=EDGE_LOOP('',(#85418,#85419,#85420,#85421));
#20410=EDGE_LOOP('',(#85422,#85423,#85424,#85425));
#20411=EDGE_LOOP('',(#85426,#85427,#85428,#85429));
#20412=EDGE_LOOP('',(#85430,#85431,#85432,#85433));
#20413=EDGE_LOOP('',(#85434,#85435,#85436,#85437));
#20414=EDGE_LOOP('',(#85438,#85439,#85440,#85441));
#20415=EDGE_LOOP('',(#85442,#85443,#85444,#85445));
#20416=EDGE_LOOP('',(#85446,#85447,#85448,#85449));
#20417=EDGE_LOOP('',(#85450,#85451,#85452,#85453,#85454,#85455));
#20418=EDGE_LOOP('',(#85456,#85457,#85458,#85459,#85460,#85461,#85462,#85463));
#20419=EDGE_LOOP('',(#85464,#85465,#85466,#85467,#85468,#85469,#85470,#85471));
#20420=EDGE_LOOP('',(#85472,#85473,#85474,#85475));
#20421=EDGE_LOOP('',(#85476,#85477,#85478));
#20422=EDGE_LOOP('',(#85479,#85480,#85481));
#20423=EDGE_LOOP('',(#85482,#85483,#85484));
#20424=EDGE_LOOP('',(#85485,#85486,#85487));
#20425=EDGE_LOOP('',(#85488,#85489,#85490));
#20426=EDGE_LOOP('',(#85491,#85492,#85493));
#20427=EDGE_LOOP('',(#85494,#85495,#85496,#85497,#85498));
#20428=EDGE_LOOP('',(#85499,#85500,#85501,#85502,#85503));
#20429=EDGE_LOOP('',(#85504,#85505,#85506,#85507,#85508));
#20430=EDGE_LOOP('',(#85509,#85510,#85511,#85512,#85513));
#20431=EDGE_LOOP('',(#85514,#85515,#85516,#85517,#85518));
#20432=EDGE_LOOP('',(#85519,#85520,#85521,#85522,#85523));
#20433=EDGE_LOOP('',(#85524,#85525,#85526,#85527,#85528,#85529));
#20434=EDGE_LOOP('',(#85530));
#20435=EDGE_LOOP('',(#85531,#85532,#85533,#85534));
#20436=EDGE_LOOP('',(#85535,#85536,#85537,#85538));
#24710=LINE('',#303020,#29057);
#24711=LINE('',#303057,#29058);
#24712=LINE('',#303123,#29059);
#24713=LINE('',#303158,#29060);
#24714=LINE('',#303234,#29061);
#24715=LINE('',#303312,#29062);
#24716=LINE('',#303388,#29063);
#24717=LINE('',#303464,#29064);
#24718=LINE('',#303540,#29065);
#24719=LINE('',#303616,#29066);
#24720=LINE('',#303692,#29067);
#24721=LINE('',#303768,#29068);
#24722=LINE('',#303846,#29069);
#24723=LINE('',#303924,#29070);
#24724=LINE('',#304000,#29071);
#24725=LINE('',#304076,#29072);
#24726=LINE('',#304152,#29073);
#24727=LINE('',#304228,#29074);
#24728=LINE('',#304305,#29075);
#24729=LINE('',#304314,#29076);
#24730=LINE('',#304328,#29077);
#24731=LINE('',#304335,#29078);
#24732=LINE('',#304381,#29079);
#24733=LINE('',#304427,#29080);
#24734=LINE('',#304473,#29081);
#24735=LINE('',#304519,#29082);
#24736=LINE('',#304565,#29083);
#24737=LINE('',#304611,#29084);
#24738=LINE('',#304657,#29085);
#24739=LINE('',#304703,#29086);
#24740=LINE('',#304749,#29087);
#24741=LINE('',#304795,#29088);
#24742=LINE('',#304841,#29089);
#24743=LINE('',#304887,#29090);
#24744=LINE('',#304933,#29091);
#24745=LINE('',#304979,#29092);
#24746=LINE('',#305025,#29093);
#24747=LINE('',#305115,#29094);
#24748=LINE('',#306983,#29095);
#24749=LINE('',#307004,#29096);
#24750=LINE('',#307063,#29097);
#24751=LINE('',#307122,#29098);
#24752=LINE('',#307203,#29099);
#24753=LINE('',#307216,#29100);
#24754=LINE('',#307251,#29101);
#24755=LINE('',#307286,#29102);
#24756=LINE('',#307359,#29103);
#24757=LINE('',#307380,#29104);
#24758=LINE('',#307439,#29105);
#24759=LINE('',#307498,#29106);
#24760=LINE('',#307579,#29107);
#24761=LINE('',#307592,#29108);
#24762=LINE('',#307627,#29109);
#24763=LINE('',#307662,#29110);
#24764=LINE('',#307989,#29111);
#24765=LINE('',#307991,#29112);
#24766=LINE('',#307993,#29113);
#24767=LINE('',#307994,#29114);
#24768=LINE('',#308034,#29115);
#24769=LINE('',#308036,#29116);
#24770=LINE('',#308079,#29117);
#24771=LINE('',#308130,#29118);
#24772=LINE('',#308189,#29119);
#24773=LINE('',#308232,#29120);
#24774=LINE('',#308283,#29121);
#24775=LINE('',#308342,#29122);
#24776=LINE('',#308458,#29123);
#24777=LINE('',#308460,#29124);
#24778=LINE('',#308503,#29125);
#24779=LINE('',#308554,#29126);
#24780=LINE('',#308613,#29127);
#24781=LINE('',#308656,#29128);
#24782=LINE('',#308707,#29129);
#24783=LINE('',#308766,#29130);
#24784=LINE('',#308845,#29131);
#24785=LINE('',#308847,#29132);
#24786=LINE('',#308848,#29133);
#24787=LINE('',#308851,#29134);
#24788=LINE('',#308852,#29135);
#24789=LINE('',#308855,#29136);
#24790=LINE('',#308856,#29137);
#24791=LINE('',#308858,#29138);
#24792=LINE('',#308922,#29139);
#24793=LINE('',#308924,#29140);
#24794=LINE('',#308925,#29141);
#24795=LINE('',#308928,#29142);
#24796=LINE('',#308929,#29143);
#24797=LINE('',#308932,#29144);
#24798=LINE('',#308933,#29145);
#24799=LINE('',#308936,#29146);
#24800=LINE('',#308937,#29147);
#24801=LINE('',#308940,#29148);
#24802=LINE('',#308941,#29149);
#24803=LINE('',#308943,#29150);
#29057=VECTOR('',#130445,6.);
#29058=VECTOR('',#130452,6.);
#29059=VECTOR('',#130457,6.);
#29060=VECTOR('',#130462,6.);
#29061=VECTOR('',#130465,6.);
#29062=VECTOR('',#130468,6.);
#29063=VECTOR('',#130471,6.);
#29064=VECTOR('',#130474,6.);
#29065=VECTOR('',#130477,6.);
#29066=VECTOR('',#130480,6.);
#29067=VECTOR('',#130483,6.);
#29068=VECTOR('',#130486,6.);
#29069=VECTOR('',#130489,6.);
#29070=VECTOR('',#130492,6.);
#29071=VECTOR('',#130495,6.);
#29072=VECTOR('',#130498,6.);
#29073=VECTOR('',#130501,6.);
#29074=VECTOR('',#130504,6.);
#29075=VECTOR('',#130509,6.);
#29076=VECTOR('',#130512,6.);
#29077=VECTOR('',#130517,4.86334165753294);
#29078=VECTOR('',#130520,4.86334165753294);
#29079=VECTOR('',#130523,4.86334165753294);
#29080=VECTOR('',#130526,4.86334165753294);
#29081=VECTOR('',#130529,4.86334165753294);
#29082=VECTOR('',#130532,4.86334165753294);
#29083=VECTOR('',#130535,4.86334165753294);
#29084=VECTOR('',#130538,4.86334165753294);
#29085=VECTOR('',#130541,4.86334165753294);
#29086=VECTOR('',#130544,4.86334165753294);
#29087=VECTOR('',#130547,4.86334165753294);
#29088=VECTOR('',#130550,4.86334165753294);
#29089=VECTOR('',#130553,4.86334165753294);
#29090=VECTOR('',#130556,4.86334165753294);
#29091=VECTOR('',#130559,4.86334165753294);
#29092=VECTOR('',#130562,4.86334165753294);
#29093=VECTOR('',#130565,4.86334165753294);
#29094=VECTOR('',#130576,4.6875);
#29095=VECTOR('',#130587,1000.);
#29096=VECTOR('',#130588,1000.);
#29097=VECTOR('',#130589,1000.);
#29098=VECTOR('',#130590,1000.);
#29099=VECTOR('',#130591,1000.);
#29100=VECTOR('',#130592,1000.);
#29101=VECTOR('',#130593,1000.);
#29102=VECTOR('',#130594,1000.);
#29103=VECTOR('',#130595,1000.);
#29104=VECTOR('',#130596,1000.);
#29105=VECTOR('',#130597,1000.);
#29106=VECTOR('',#130598,1000.);
#29107=VECTOR('',#130599,1000.);
#29108=VECTOR('',#130600,1000.);
#29109=VECTOR('',#130601,1000.);
#29110=VECTOR('',#130602,1000.);
#29111=VECTOR('',#130609,1000.);
#29112=VECTOR('',#130610,1000.);
#29113=VECTOR('',#130611,1000.);
#29114=VECTOR('',#130612,1000.);
#29115=VECTOR('',#130613,1000.);
#29116=VECTOR('',#130614,1000.);
#29117=VECTOR('',#130615,1000.);
#29118=VECTOR('',#130616,1000.);
#29119=VECTOR('',#130617,1000.);
#29120=VECTOR('',#130618,1000.);
#29121=VECTOR('',#130619,1000.);
#29122=VECTOR('',#130620,1000.);
#29123=VECTOR('',#130621,1000.);
#29124=VECTOR('',#130622,1000.);
#29125=VECTOR('',#130623,1000.);
#29126=VECTOR('',#130624,1000.);
#29127=VECTOR('',#130625,1000.);
#29128=VECTOR('',#130626,1000.);
#29129=VECTOR('',#130627,1000.);
#29130=VECTOR('',#130628,1000.);
#29131=VECTOR('',#130631,1000.);
#29132=VECTOR('',#130632,1000.);
#29133=VECTOR('',#130633,1000.);
#29134=VECTOR('',#130636,1000.);
#29135=VECTOR('',#130637,1000.);
#29136=VECTOR('',#130640,1000.);
#29137=VECTOR('',#130641,1000.);
#29138=VECTOR('',#130644,1000.);
#29139=VECTOR('',#130673,1000.);
#29140=VECTOR('',#130674,1000.);
#29141=VECTOR('',#130675,1000.);
#29142=VECTOR('',#130678,1000.);
#29143=VECTOR('',#130679,1000.);
#29144=VECTOR('',#130682,1000.);
#29145=VECTOR('',#130683,1000.);
#29146=VECTOR('',#130686,1000.);
#29147=VECTOR('',#130687,1000.);
#29148=VECTOR('',#130690,1000.);
#29149=VECTOR('',#130691,1000.);
#29150=VECTOR('',#130694,1000.);
#35069=CIRCLE('',#104639,4.86334165753398);
#35070=CIRCLE('',#104640,4.86334165753398);
#35071=CIRCLE('',#104642,6.);
#35072=CIRCLE('',#104644,6.);
#35073=CIRCLE('',#104661,6.);
#35074=CIRCLE('',#104662,6.);
#35075=CIRCLE('',#104663,6.);
#35076=CIRCLE('',#104681,4.86334165753294);
#35077=CIRCLE('',#104683,4.6875);
#35078=CIRCLE('',#104685,4.86334165753294);
#35079=CIRCLE('',#104699,9.5);
#35080=CIRCLE('',#104700,9.5);
#35081=CIRCLE('',#104701,9.5);
#35082=CIRCLE('',#104702,9.5);
#35083=CIRCLE('',#104703,9.5);
#35084=CIRCLE('',#104704,9.5);
#43366=VERTEX_POINT('',#303018);
#43367=VERTEX_POINT('',#303019);
#43368=VERTEX_POINT('',#303021);
#43369=VERTEX_POINT('',#303038);
#43370=VERTEX_POINT('',#303040);
#43371=VERTEX_POINT('',#303055);
#43372=VERTEX_POINT('',#303056);
#43373=VERTEX_POINT('',#303058);
#43374=VERTEX_POINT('',#303121);
#43375=VERTEX_POINT('',#303122);
#43376=VERTEX_POINT('',#303124);
#43377=VERTEX_POINT('',#303141);
#43378=VERTEX_POINT('',#303156);
#43379=VERTEX_POINT('',#303157);
#43380=VERTEX_POINT('',#303232);
#43381=VERTEX_POINT('',#303233);
#43382=VERTEX_POINT('',#303310);
#43383=VERTEX_POINT('',#303311);
#43384=VERTEX_POINT('',#303386);
#43385=VERTEX_POINT('',#303387);
#43386=VERTEX_POINT('',#303462);
#43387=VERTEX_POINT('',#303463);
#43388=VERTEX_POINT('',#303538);
#43389=VERTEX_POINT('',#303539);
#43390=VERTEX_POINT('',#303614);
#43391=VERTEX_POINT('',#303615);
#43392=VERTEX_POINT('',#303690);
#43393=VERTEX_POINT('',#303691);
#43394=VERTEX_POINT('',#303766);
#43395=VERTEX_POINT('',#303767);
#43396=VERTEX_POINT('',#303844);
#43397=VERTEX_POINT('',#303845);
#43398=VERTEX_POINT('',#303922);
#43399=VERTEX_POINT('',#303923);
#43400=VERTEX_POINT('',#303998);
#43401=VERTEX_POINT('',#303999);
#43402=VERTEX_POINT('',#304074);
#43403=VERTEX_POINT('',#304075);
#43404=VERTEX_POINT('',#304150);
#43405=VERTEX_POINT('',#304151);
#43406=VERTEX_POINT('',#304226);
#43407=VERTEX_POINT('',#304227);
#43408=VERTEX_POINT('',#304302);
#43409=VERTEX_POINT('',#304304);
#43410=VERTEX_POINT('',#304306);
#43411=VERTEX_POINT('',#304308);
#43412=VERTEX_POINT('',#304313);
#43413=VERTEX_POINT('',#304327);
#43414=VERTEX_POINT('',#304333);
#43415=VERTEX_POINT('',#304334);
#43416=VERTEX_POINT('',#304379);
#43417=VERTEX_POINT('',#304380);
#43418=VERTEX_POINT('',#304425);
#43419=VERTEX_POINT('',#304426);
#43420=VERTEX_POINT('',#304471);
#43421=VERTEX_POINT('',#304472);
#43422=VERTEX_POINT('',#304517);
#43423=VERTEX_POINT('',#304518);
#43424=VERTEX_POINT('',#304563);
#43425=VERTEX_POINT('',#304564);
#43426=VERTEX_POINT('',#304609);
#43427=VERTEX_POINT('',#304610);
#43428=VERTEX_POINT('',#304655);
#43429=VERTEX_POINT('',#304656);
#43430=VERTEX_POINT('',#304701);
#43431=VERTEX_POINT('',#304702);
#43432=VERTEX_POINT('',#304747);
#43433=VERTEX_POINT('',#304748);
#43434=VERTEX_POINT('',#304793);
#43435=VERTEX_POINT('',#304794);
#43436=VERTEX_POINT('',#304839);
#43437=VERTEX_POINT('',#304840);
#43438=VERTEX_POINT('',#304885);
#43439=VERTEX_POINT('',#304886);
#43440=VERTEX_POINT('',#304931);
#43441=VERTEX_POINT('',#304932);
#43442=VERTEX_POINT('',#304977);
#43443=VERTEX_POINT('',#304978);
#43444=VERTEX_POINT('',#305023);
#43445=VERTEX_POINT('',#305024);
#43446=VERTEX_POINT('',#305026);
#43447=VERTEX_POINT('',#305069);
#43448=VERTEX_POINT('',#305072);
#43449=VERTEX_POINT('',#305088);
#43450=VERTEX_POINT('',#306685);
#43451=VERTEX_POINT('',#306686);
#43452=VERTEX_POINT('',#306706);
#43453=VERTEX_POINT('',#306726);
#43454=VERTEX_POINT('',#306766);
#43455=VERTEX_POINT('',#306767);
#43456=VERTEX_POINT('',#306779);
#43457=VERTEX_POINT('',#306791);
#43458=VERTEX_POINT('',#306815);
#43459=VERTEX_POINT('',#306816);
#43460=VERTEX_POINT('',#306836);
#43461=VERTEX_POINT('',#306856);
#43462=VERTEX_POINT('',#306896);
#43463=VERTEX_POINT('',#306897);
#43464=VERTEX_POINT('',#306909);
#43465=VERTEX_POINT('',#306921);
#43466=VERTEX_POINT('',#306982);
#43467=VERTEX_POINT('',#306984);
#43468=VERTEX_POINT('',#307043);
#43469=VERTEX_POINT('',#307102);
#43470=VERTEX_POINT('',#307202);
#43471=VERTEX_POINT('',#307204);
#43472=VERTEX_POINT('',#307239);
#43473=VERTEX_POINT('',#307274);
#43474=VERTEX_POINT('',#307358);
#43475=VERTEX_POINT('',#307360);
#43476=VERTEX_POINT('',#307419);
#43477=VERTEX_POINT('',#307478);
#43478=VERTEX_POINT('',#307578);
#43479=VERTEX_POINT('',#307580);
#43480=VERTEX_POINT('',#307615);
#43481=VERTEX_POINT('',#307650);
#43482=VERTEX_POINT('',#307697);
#43483=VERTEX_POINT('',#307698);
#43484=VERTEX_POINT('',#307710);
#43485=VERTEX_POINT('',#307730);
#43486=VERTEX_POINT('',#307750);
#43487=VERTEX_POINT('',#307770);
#43488=VERTEX_POINT('',#307790);
#43489=VERTEX_POINT('',#307802);
#43490=VERTEX_POINT('',#307842);
#43491=VERTEX_POINT('',#307843);
#43492=VERTEX_POINT('',#307855);
#43493=VERTEX_POINT('',#307875);
#43494=VERTEX_POINT('',#307895);
#43495=VERTEX_POINT('',#307915);
#43496=VERTEX_POINT('',#307935);
#43497=VERTEX_POINT('',#307947);
#43498=VERTEX_POINT('',#307987);
#43499=VERTEX_POINT('',#307988);
#43500=VERTEX_POINT('',#307990);
#43501=VERTEX_POINT('',#307992);
#43502=VERTEX_POINT('',#308033);
#43503=VERTEX_POINT('',#308035);
#43504=VERTEX_POINT('',#308078);
#43505=VERTEX_POINT('',#308129);
#43506=VERTEX_POINT('',#308188);
#43507=VERTEX_POINT('',#308231);
#43508=VERTEX_POINT('',#308282);
#43509=VERTEX_POINT('',#308341);
#43510=VERTEX_POINT('',#308457);
#43511=VERTEX_POINT('',#308459);
#43512=VERTEX_POINT('',#308502);
#43513=VERTEX_POINT('',#308553);
#43514=VERTEX_POINT('',#308612);
#43515=VERTEX_POINT('',#308655);
#43516=VERTEX_POINT('',#308706);
#43517=VERTEX_POINT('',#308765);
#43518=VERTEX_POINT('',#308844);
#43519=VERTEX_POINT('',#308846);
#43520=VERTEX_POINT('',#308850);
#43521=VERTEX_POINT('',#308854);
#43522=VERTEX_POINT('',#308860);
#43523=VERTEX_POINT('',#308861);
#43524=VERTEX_POINT('',#308863);
#43525=VERTEX_POINT('',#308865);
#43526=VERTEX_POINT('',#308867);
#43527=VERTEX_POINT('',#308869);
#43528=VERTEX_POINT('',#308873);
#43529=VERTEX_POINT('',#308881);
#43530=VERTEX_POINT('',#308889);
#43531=VERTEX_POINT('',#308897);
#43532=VERTEX_POINT('',#308905);
#43533=VERTEX_POINT('',#308913);
#43534=VERTEX_POINT('',#308921);
#43535=VERTEX_POINT('',#308923);
#43536=VERTEX_POINT('',#308927);
#43537=VERTEX_POINT('',#308931);
#43538=VERTEX_POINT('',#308935);
#43539=VERTEX_POINT('',#308939);
#57285=EDGE_CURVE('',#43366,#43367,#24710,.T.);
#57286=EDGE_CURVE('',#43366,#43368,#6790,.T.);
#57287=EDGE_CURVE('',#43368,#43369,#35069,.T.);
#57288=EDGE_CURVE('',#43369,#43370,#35070,.T.);
#57289=EDGE_CURVE('',#43370,#43367,#6791,.F.);
#57290=EDGE_CURVE('',#43371,#43372,#24711,.T.);
#57291=EDGE_CURVE('',#43371,#43373,#35071,.T.);
#57292=EDGE_CURVE('',#43373,#43366,#6792,.T.);
#57293=EDGE_CURVE('',#43367,#43372,#6793,.F.);
#57294=EDGE_CURVE('',#43374,#43375,#24712,.T.);
#57295=EDGE_CURVE('',#43374,#43376,#6794,.F.);
#57296=EDGE_CURVE('',#43376,#43377,#35072,.T.);
#57297=EDGE_CURVE('',#43377,#43375,#6795,.F.);
#57298=EDGE_CURVE('',#43378,#43379,#24713,.T.);
#57299=EDGE_CURVE('',#43378,#43374,#6796,.F.);
#57300=EDGE_CURVE('',#43375,#43379,#6797,.F.);
#57301=EDGE_CURVE('',#43380,#43381,#24714,.T.);
#57302=EDGE_CURVE('',#43380,#43378,#6798,.F.);
#57303=EDGE_CURVE('',#43379,#43381,#6799,.F.);
#57304=EDGE_CURVE('',#43382,#43383,#24715,.T.);
#57305=EDGE_CURVE('',#43382,#43380,#6800,.F.);
#57306=EDGE_CURVE('',#43381,#43383,#6801,.F.);
#57307=EDGE_CURVE('',#43384,#43385,#24716,.T.);
#57308=EDGE_CURVE('',#43384,#43382,#6802,.F.);
#57309=EDGE_CURVE('',#43383,#43385,#6803,.F.);
#57310=EDGE_CURVE('',#43386,#43387,#24717,.T.);
#57311=EDGE_CURVE('',#43386,#43384,#6804,.F.);
#57312=EDGE_CURVE('',#43385,#43387,#6805,.F.);
#57313=EDGE_CURVE('',#43388,#43389,#24718,.T.);
#57314=EDGE_CURVE('',#43388,#43386,#6806,.F.);
#57315=EDGE_CURVE('',#43387,#43389,#6807,.F.);
#57316=EDGE_CURVE('',#43390,#43391,#24719,.T.);
#57317=EDGE_CURVE('',#43390,#43388,#6808,.F.);
#57318=EDGE_CURVE('',#43389,#43391,#6809,.F.);
#57319=EDGE_CURVE('',#43392,#43393,#24720,.T.);
#57320=EDGE_CURVE('',#43392,#43390,#6810,.F.);
#57321=EDGE_CURVE('',#43391,#43393,#6811,.F.);
#57322=EDGE_CURVE('',#43394,#43395,#24721,.T.);
#57323=EDGE_CURVE('',#43394,#43392,#6812,.F.);
#57324=EDGE_CURVE('',#43393,#43395,#6813,.F.);
#57325=EDGE_CURVE('',#43396,#43397,#24722,.T.);
#57326=EDGE_CURVE('',#43396,#43394,#6814,.F.);
#57327=EDGE_CURVE('',#43395,#43397,#6815,.F.);
#57328=EDGE_CURVE('',#43398,#43399,#24723,.T.);
#57329=EDGE_CURVE('',#43398,#43396,#6816,.F.);
#57330=EDGE_CURVE('',#43397,#43399,#6817,.F.);
#57331=EDGE_CURVE('',#43400,#43401,#24724,.T.);
#57332=EDGE_CURVE('',#43400,#43398,#6818,.F.);
#57333=EDGE_CURVE('',#43399,#43401,#6819,.F.);
#57334=EDGE_CURVE('',#43402,#43403,#24725,.T.);
#57335=EDGE_CURVE('',#43402,#43400,#6820,.F.);
#57336=EDGE_CURVE('',#43401,#43403,#6821,.F.);
#57337=EDGE_CURVE('',#43404,#43405,#24726,.T.);
#57338=EDGE_CURVE('',#43404,#43402,#6822,.F.);
#57339=EDGE_CURVE('',#43403,#43405,#6823,.F.);
#57340=EDGE_CURVE('',#43406,#43407,#24727,.T.);
#57341=EDGE_CURVE('',#43406,#43404,#6824,.F.);
#57342=EDGE_CURVE('',#43405,#43407,#6825,.F.);
#57343=EDGE_CURVE('',#43408,#43408,#35073,.T.);
#57344=EDGE_CURVE('',#43408,#43409,#24728,.T.);
#57345=EDGE_CURVE('',#43410,#43409,#35074,.T.);
#57346=EDGE_CURVE('',#43410,#43411,#6826,.F.);
#57347=EDGE_CURVE('',#43411,#43412,#24729,.T.);
#57348=EDGE_CURVE('',#43412,#43373,#6827,.F.);
#57349=EDGE_CURVE('',#43409,#43371,#35075,.T.);
#57350=EDGE_CURVE('',#43413,#43369,#24730,.T.);
#57351=EDGE_CURVE('',#43413,#43370,#1692,.T.);
#57352=EDGE_CURVE('',#43414,#43415,#24731,.T.);
#57353=EDGE_CURVE('',#43414,#43413,#1693,.T.);
#57354=EDGE_CURVE('',#43415,#43368,#1694,.T.);
#57355=EDGE_CURVE('',#43416,#43417,#24732,.T.);
#57356=EDGE_CURVE('',#43416,#43414,#1695,.T.);
#57357=EDGE_CURVE('',#43417,#43415,#1696,.T.);
#57358=EDGE_CURVE('',#43418,#43419,#24733,.T.);
#57359=EDGE_CURVE('',#43418,#43416,#1697,.T.);
#57360=EDGE_CURVE('',#43419,#43417,#1698,.T.);
#57361=EDGE_CURVE('',#43420,#43421,#24734,.T.);
#57362=EDGE_CURVE('',#43420,#43418,#1699,.T.);
#57363=EDGE_CURVE('',#43421,#43419,#1700,.T.);
#57364=EDGE_CURVE('',#43422,#43423,#24735,.T.);
#57365=EDGE_CURVE('',#43422,#43420,#1701,.T.);
#57366=EDGE_CURVE('',#43423,#43421,#1702,.T.);
#57367=EDGE_CURVE('',#43424,#43425,#24736,.T.);
#57368=EDGE_CURVE('',#43424,#43422,#1703,.T.);
#57369=EDGE_CURVE('',#43425,#43423,#1704,.T.);
#57370=EDGE_CURVE('',#43426,#43427,#24737,.T.);
#57371=EDGE_CURVE('',#43426,#43424,#1705,.T.);
#57372=EDGE_CURVE('',#43427,#43425,#1706,.T.);
#57373=EDGE_CURVE('',#43428,#43429,#24738,.T.);
#57374=EDGE_CURVE('',#43428,#43426,#1707,.T.);
#57375=EDGE_CURVE('',#43429,#43427,#1708,.T.);
#57376=EDGE_CURVE('',#43430,#43431,#24739,.T.);
#57377=EDGE_CURVE('',#43430,#43428,#1709,.T.);
#57378=EDGE_CURVE('',#43431,#43429,#1710,.T.);
#57379=EDGE_CURVE('',#43432,#43433,#24740,.T.);
#57380=EDGE_CURVE('',#43432,#43430,#1711,.T.);
#57381=EDGE_CURVE('',#43433,#43431,#1712,.T.);
#57382=EDGE_CURVE('',#43434,#43435,#24741,.T.);
#57383=EDGE_CURVE('',#43434,#43432,#1713,.T.);
#57384=EDGE_CURVE('',#43435,#43433,#1714,.T.);
#57385=EDGE_CURVE('',#43436,#43437,#24742,.T.);
#57386=EDGE_CURVE('',#43436,#43434,#1715,.T.);
#57387=EDGE_CURVE('',#43437,#43435,#1716,.T.);
#57388=EDGE_CURVE('',#43438,#43439,#24743,.T.);
#57389=EDGE_CURVE('',#43438,#43436,#1717,.T.);
#57390=EDGE_CURVE('',#43439,#43437,#1718,.T.);
#57391=EDGE_CURVE('',#43440,#43441,#24744,.T.);
#57392=EDGE_CURVE('',#43440,#43438,#1719,.T.);
#57393=EDGE_CURVE('',#43441,#43439,#1720,.T.);
#57394=EDGE_CURVE('',#43442,#43443,#24745,.T.);
#57395=EDGE_CURVE('',#43442,#43440,#1721,.T.);
#57396=EDGE_CURVE('',#43443,#43441,#1722,.T.);
#57397=EDGE_CURVE('',#43444,#43445,#24746,.T.);
#57398=EDGE_CURVE('',#43444,#43446,#35076,.T.);
#57399=EDGE_CURVE('',#43446,#43442,#1723,.T.);
#57400=EDGE_CURVE('',#43445,#43443,#1724,.T.);
#57401=EDGE_CURVE('',#43447,#43447,#35077,.T.);
#57402=EDGE_CURVE('',#43448,#43444,#35078,.T.);
#57403=EDGE_CURVE('',#43377,#43448,#6828,.F.);
#57404=EDGE_CURVE('',#43449,#43376,#6829,.F.);
#57405=EDGE_CURVE('',#43449,#43447,#24747,.T.);
#57406=EDGE_CURVE('',#43446,#43449,#6830,.F.);
#57407=EDGE_CURVE('',#43407,#43412,#6831,.F.);
#57408=EDGE_CURVE('',#43448,#43445,#1725,.T.);
#57409=EDGE_CURVE('',#43411,#43406,#6832,.F.);
#57410=EDGE_CURVE('',#43372,#43410,#6833,.F.);
#57411=EDGE_CURVE('',#43450,#43451,#6834,.T.);
#57412=EDGE_CURVE('',#43451,#43452,#6835,.T.);
#57413=EDGE_CURVE('',#43452,#43453,#6836,.T.);
#57414=EDGE_CURVE('',#43453,#43450,#6837,.T.);
#57415=EDGE_CURVE('',#43454,#43455,#6838,.T.);
#57416=EDGE_CURVE('',#43455,#43456,#6839,.T.);
#57417=EDGE_CURVE('',#43456,#43457,#6840,.T.);
#57418=EDGE_CURVE('',#43457,#43454,#6841,.T.);
#57419=EDGE_CURVE('',#43458,#43459,#6842,.T.);
#57420=EDGE_CURVE('',#43459,#43460,#6843,.T.);
#57421=EDGE_CURVE('',#43460,#43461,#6844,.T.);
#57422=EDGE_CURVE('',#43461,#43458,#6845,.T.);
#57423=EDGE_CURVE('',#43462,#43463,#6846,.T.);
#57424=EDGE_CURVE('',#43463,#43464,#6847,.T.);
#57425=EDGE_CURVE('',#43464,#43465,#6848,.T.);
#57426=EDGE_CURVE('',#43465,#43462,#6849,.T.);
#57427=EDGE_CURVE('',#43466,#43452,#24748,.T.);
#57428=EDGE_CURVE('',#43467,#43466,#6850,.T.);
#57429=EDGE_CURVE('',#43467,#43453,#24749,.T.);
#57430=EDGE_CURVE('',#43468,#43467,#6851,.T.);
#57431=EDGE_CURVE('',#43468,#43450,#24750,.T.);
#57432=EDGE_CURVE('',#43469,#43468,#6852,.T.);
#57433=EDGE_CURVE('',#43469,#43451,#24751,.T.);
#57434=EDGE_CURVE('',#43466,#43469,#6853,.T.);
#57435=EDGE_CURVE('',#43470,#43456,#24752,.T.);
#57436=EDGE_CURVE('',#43471,#43470,#6854,.T.);
#57437=EDGE_CURVE('',#43471,#43457,#24753,.T.);
#57438=EDGE_CURVE('',#43472,#43471,#6855,.T.);
#57439=EDGE_CURVE('',#43472,#43454,#24754,.T.);
#57440=EDGE_CURVE('',#43473,#43472,#6856,.T.);
#57441=EDGE_CURVE('',#43473,#43455,#24755,.T.);
#57442=EDGE_CURVE('',#43470,#43473,#6857,.T.);
#57443=EDGE_CURVE('',#43474,#43460,#24756,.T.);
#57444=EDGE_CURVE('',#43475,#43474,#6858,.T.);
#57445=EDGE_CURVE('',#43475,#43461,#24757,.T.);
#57446=EDGE_CURVE('',#43476,#43475,#6859,.T.);
#57447=EDGE_CURVE('',#43476,#43458,#24758,.T.);
#57448=EDGE_CURVE('',#43477,#43476,#6860,.T.);
#57449=EDGE_CURVE('',#43477,#43459,#24759,.T.);
#57450=EDGE_CURVE('',#43474,#43477,#6861,.T.);
#57451=EDGE_CURVE('',#43478,#43464,#24760,.T.);
#57452=EDGE_CURVE('',#43479,#43478,#6862,.T.);
#57453=EDGE_CURVE('',#43479,#43465,#24761,.T.);
#57454=EDGE_CURVE('',#43480,#43479,#6863,.T.);
#57455=EDGE_CURVE('',#43480,#43462,#24762,.T.);
#57456=EDGE_CURVE('',#43481,#43480,#6864,.T.);
#57457=EDGE_CURVE('',#43481,#43463,#24763,.T.);
#57458=EDGE_CURVE('',#43478,#43481,#6865,.T.);
#57459=EDGE_CURVE('',#43482,#43483,#6866,.T.);
#57460=EDGE_CURVE('',#43483,#43484,#6867,.T.);
#57461=EDGE_CURVE('',#43484,#43485,#6868,.T.);
#57462=EDGE_CURVE('',#43485,#43486,#6869,.T.);
#57463=EDGE_CURVE('',#43486,#43487,#6870,.T.);
#57464=EDGE_CURVE('',#43487,#43488,#6871,.T.);
#57465=EDGE_CURVE('',#43488,#43489,#6872,.T.);
#57466=EDGE_CURVE('',#43489,#43482,#6873,.T.);
#57467=EDGE_CURVE('',#43490,#43491,#6874,.T.);
#57468=EDGE_CURVE('',#43491,#43492,#6875,.T.);
#57469=EDGE_CURVE('',#43492,#43493,#6876,.T.);
#57470=EDGE_CURVE('',#43493,#43494,#6877,.T.);
#57471=EDGE_CURVE('',#43494,#43495,#6878,.T.);
#57472=EDGE_CURVE('',#43495,#43496,#6879,.T.);
#57473=EDGE_CURVE('',#43496,#43497,#6880,.T.);
#57474=EDGE_CURVE('',#43497,#43490,#6881,.T.);
#57475=EDGE_CURVE('',#43498,#43499,#24764,.T.);
#57476=EDGE_CURVE('',#43499,#43500,#24765,.T.);
#57477=EDGE_CURVE('',#43500,#43501,#24766,.T.);
#57478=EDGE_CURVE('',#43501,#43498,#24767,.T.);
#57479=EDGE_CURVE('',#43487,#43502,#24768,.T.);
#57480=EDGE_CURVE('',#43486,#43503,#24769,.T.);
#57481=EDGE_CURVE('',#43502,#43503,#6882,.T.);
#57482=EDGE_CURVE('',#43488,#43504,#24770,.T.);
#57483=EDGE_CURVE('',#43504,#43502,#6883,.T.);
#57484=EDGE_CURVE('',#43489,#43505,#24771,.T.);
#57485=EDGE_CURVE('',#43505,#43504,#6884,.T.);
#57486=EDGE_CURVE('',#43482,#43506,#24772,.T.);
#57487=EDGE_CURVE('',#43506,#43505,#6885,.T.);
#57488=EDGE_CURVE('',#43483,#43507,#24773,.T.);
#57489=EDGE_CURVE('',#43507,#43506,#6886,.T.);
#57490=EDGE_CURVE('',#43484,#43508,#24774,.T.);
#57491=EDGE_CURVE('',#43508,#43507,#6887,.T.);
#57492=EDGE_CURVE('',#43485,#43509,#24775,.T.);
#57493=EDGE_CURVE('',#43509,#43508,#6888,.T.);
#57494=EDGE_CURVE('',#43503,#43509,#6889,.T.);
#57495=EDGE_CURVE('',#43495,#43510,#24776,.T.);
#57496=EDGE_CURVE('',#43494,#43511,#24777,.T.);
#57497=EDGE_CURVE('',#43510,#43511,#6890,.T.);
#57498=EDGE_CURVE('',#43496,#43512,#24778,.T.);
#57499=EDGE_CURVE('',#43512,#43510,#6891,.T.);
#57500=EDGE_CURVE('',#43497,#43513,#24779,.T.);
#57501=EDGE_CURVE('',#43513,#43512,#6892,.T.);
#57502=EDGE_CURVE('',#43490,#43514,#24780,.T.);
#57503=EDGE_CURVE('',#43514,#43513,#6893,.T.);
#57504=EDGE_CURVE('',#43491,#43515,#24781,.T.);
#57505=EDGE_CURVE('',#43515,#43514,#6894,.T.);
#57506=EDGE_CURVE('',#43492,#43516,#24782,.T.);
#57507=EDGE_CURVE('',#43516,#43515,#6895,.T.);
#57508=EDGE_CURVE('',#43493,#43517,#24783,.T.);
#57509=EDGE_CURVE('',#43517,#43516,#6896,.T.);
#57510=EDGE_CURVE('',#43511,#43517,#6897,.T.);
#57511=EDGE_CURVE('',#43499,#43518,#24784,.T.);
#57512=EDGE_CURVE('',#43498,#43519,#24785,.T.);
#57513=EDGE_CURVE('',#43518,#43519,#24786,.T.);
#57514=EDGE_CURVE('',#43500,#43520,#24787,.T.);
#57515=EDGE_CURVE('',#43520,#43518,#24788,.T.);
#57516=EDGE_CURVE('',#43501,#43521,#24789,.T.);
#57517=EDGE_CURVE('',#43521,#43520,#24790,.T.);
#57518=EDGE_CURVE('',#43519,#43521,#24791,.T.);
#57519=EDGE_CURVE('',#43522,#43523,#35079,.T.);
#57520=EDGE_CURVE('',#43523,#43524,#35080,.T.);
#57521=EDGE_CURVE('',#43524,#43525,#35081,.T.);
#57522=EDGE_CURVE('',#43525,#43526,#35082,.T.);
#57523=EDGE_CURVE('',#43526,#43527,#35083,.T.);
#57524=EDGE_CURVE('',#43527,#43522,#35084,.T.);
#57525=EDGE_CURVE('',#43527,#43528,#1726,.T.);
#57526=EDGE_CURVE('',#43528,#43522,#1727,.T.);
#57527=EDGE_CURVE('',#43522,#43529,#1728,.T.);
#57528=EDGE_CURVE('',#43529,#43523,#1729,.T.);
#57529=EDGE_CURVE('',#43523,#43530,#1730,.T.);
#57530=EDGE_CURVE('',#43530,#43524,#1731,.T.);
#57531=EDGE_CURVE('',#43524,#43531,#1732,.T.);
#57532=EDGE_CURVE('',#43531,#43525,#1733,.T.);
#57533=EDGE_CURVE('',#43526,#43532,#1734,.T.);
#57534=EDGE_CURVE('',#43532,#43527,#1735,.T.);
#57535=EDGE_CURVE('',#43533,#43526,#1736,.T.);
#57536=EDGE_CURVE('',#43525,#43533,#1737,.T.);
#57537=EDGE_CURVE('',#43532,#43534,#24792,.T.);
#57538=EDGE_CURVE('',#43534,#43535,#24793,.T.);
#57539=EDGE_CURVE('',#43528,#43535,#24794,.T.);
#57540=EDGE_CURVE('',#43535,#43536,#24795,.T.);
#57541=EDGE_CURVE('',#43529,#43536,#24796,.T.);
#57542=EDGE_CURVE('',#43536,#43537,#24797,.T.);
#57543=EDGE_CURVE('',#43530,#43537,#24798,.T.);
#57544=EDGE_CURVE('',#43537,#43538,#24799,.T.);
#57545=EDGE_CURVE('',#43531,#43538,#24800,.T.);
#57546=EDGE_CURVE('',#43538,#43539,#24801,.T.);
#57547=EDGE_CURVE('',#43533,#43539,#24802,.T.);
#57548=EDGE_CURVE('',#43539,#43534,#24803,.T.);
#85011=ORIENTED_EDGE('',*,*,#57285,.F.);
#85012=ORIENTED_EDGE('',*,*,#57286,.T.);
#85013=ORIENTED_EDGE('',*,*,#57287,.T.);
#85014=ORIENTED_EDGE('',*,*,#57288,.T.);
#85015=ORIENTED_EDGE('',*,*,#57289,.T.);
#85016=ORIENTED_EDGE('',*,*,#57290,.F.);
#85017=ORIENTED_EDGE('',*,*,#57291,.T.);
#85018=ORIENTED_EDGE('',*,*,#57292,.T.);
#85019=ORIENTED_EDGE('',*,*,#57285,.T.);
#85020=ORIENTED_EDGE('',*,*,#57293,.T.);
#85021=ORIENTED_EDGE('',*,*,#57294,.F.);
#85022=ORIENTED_EDGE('',*,*,#57295,.T.);
#85023=ORIENTED_EDGE('',*,*,#57296,.T.);
#85024=ORIENTED_EDGE('',*,*,#57297,.T.);
#85025=ORIENTED_EDGE('',*,*,#57298,.F.);
#85026=ORIENTED_EDGE('',*,*,#57299,.T.);
#85027=ORIENTED_EDGE('',*,*,#57294,.T.);
#85028=ORIENTED_EDGE('',*,*,#57300,.T.);
#85029=ORIENTED_EDGE('',*,*,#57301,.F.);
#85030=ORIENTED_EDGE('',*,*,#57302,.T.);
#85031=ORIENTED_EDGE('',*,*,#57298,.T.);
#85032=ORIENTED_EDGE('',*,*,#57303,.T.);
#85033=ORIENTED_EDGE('',*,*,#57304,.F.);
#85034=ORIENTED_EDGE('',*,*,#57305,.T.);
#85035=ORIENTED_EDGE('',*,*,#57301,.T.);
#85036=ORIENTED_EDGE('',*,*,#57306,.T.);
#85037=ORIENTED_EDGE('',*,*,#57307,.F.);
#85038=ORIENTED_EDGE('',*,*,#57308,.T.);
#85039=ORIENTED_EDGE('',*,*,#57304,.T.);
#85040=ORIENTED_EDGE('',*,*,#57309,.T.);
#85041=ORIENTED_EDGE('',*,*,#57310,.F.);
#85042=ORIENTED_EDGE('',*,*,#57311,.T.);
#85043=ORIENTED_EDGE('',*,*,#57307,.T.);
#85044=ORIENTED_EDGE('',*,*,#57312,.T.);
#85045=ORIENTED_EDGE('',*,*,#57313,.F.);
#85046=ORIENTED_EDGE('',*,*,#57314,.T.);
#85047=ORIENTED_EDGE('',*,*,#57310,.T.);
#85048=ORIENTED_EDGE('',*,*,#57315,.T.);
#85049=ORIENTED_EDGE('',*,*,#57316,.F.);
#85050=ORIENTED_EDGE('',*,*,#57317,.T.);
#85051=ORIENTED_EDGE('',*,*,#57313,.T.);
#85052=ORIENTED_EDGE('',*,*,#57318,.T.);
#85053=ORIENTED_EDGE('',*,*,#57319,.F.);
#85054=ORIENTED_EDGE('',*,*,#57320,.T.);
#85055=ORIENTED_EDGE('',*,*,#57316,.T.);
#85056=ORIENTED_EDGE('',*,*,#57321,.T.);
#85057=ORIENTED_EDGE('',*,*,#57322,.F.);
#85058=ORIENTED_EDGE('',*,*,#57323,.T.);
#85059=ORIENTED_EDGE('',*,*,#57319,.T.);
#85060=ORIENTED_EDGE('',*,*,#57324,.T.);
#85061=ORIENTED_EDGE('',*,*,#57325,.F.);
#85062=ORIENTED_EDGE('',*,*,#57326,.T.);
#85063=ORIENTED_EDGE('',*,*,#57322,.T.);
#85064=ORIENTED_EDGE('',*,*,#57327,.T.);
#85065=ORIENTED_EDGE('',*,*,#57328,.F.);
#85066=ORIENTED_EDGE('',*,*,#57329,.T.);
#85067=ORIENTED_EDGE('',*,*,#57325,.T.);
#85068=ORIENTED_EDGE('',*,*,#57330,.T.);
#85069=ORIENTED_EDGE('',*,*,#57331,.F.);
#85070=ORIENTED_EDGE('',*,*,#57332,.T.);
#85071=ORIENTED_EDGE('',*,*,#57328,.T.);
#85072=ORIENTED_EDGE('',*,*,#57333,.T.);
#85073=ORIENTED_EDGE('',*,*,#57334,.F.);
#85074=ORIENTED_EDGE('',*,*,#57335,.T.);
#85075=ORIENTED_EDGE('',*,*,#57331,.T.);
#85076=ORIENTED_EDGE('',*,*,#57336,.T.);
#85077=ORIENTED_EDGE('',*,*,#57337,.F.);
#85078=ORIENTED_EDGE('',*,*,#57338,.T.);
#85079=ORIENTED_EDGE('',*,*,#57334,.T.);
#85080=ORIENTED_EDGE('',*,*,#57339,.T.);
#85081=ORIENTED_EDGE('',*,*,#57340,.F.);
#85082=ORIENTED_EDGE('',*,*,#57341,.T.);
#85083=ORIENTED_EDGE('',*,*,#57337,.T.);
#85084=ORIENTED_EDGE('',*,*,#57342,.T.);
#85085=ORIENTED_EDGE('',*,*,#57343,.F.);
#85086=ORIENTED_EDGE('',*,*,#57344,.T.);
#85087=ORIENTED_EDGE('',*,*,#57345,.F.);
#85088=ORIENTED_EDGE('',*,*,#57346,.T.);
#85089=ORIENTED_EDGE('',*,*,#57347,.T.);
#85090=ORIENTED_EDGE('',*,*,#57348,.T.);
#85091=ORIENTED_EDGE('',*,*,#57291,.F.);
#85092=ORIENTED_EDGE('',*,*,#57349,.F.);
#85093=ORIENTED_EDGE('',*,*,#57344,.F.);
#85094=ORIENTED_EDGE('',*,*,#57350,.F.);
#85095=ORIENTED_EDGE('',*,*,#57351,.T.);
#85096=ORIENTED_EDGE('',*,*,#57288,.F.);
#85097=ORIENTED_EDGE('',*,*,#57352,.F.);
#85098=ORIENTED_EDGE('',*,*,#57353,.T.);
#85099=ORIENTED_EDGE('',*,*,#57350,.T.);
#85100=ORIENTED_EDGE('',*,*,#57287,.F.);
#85101=ORIENTED_EDGE('',*,*,#57354,.F.);
#85102=ORIENTED_EDGE('',*,*,#57355,.F.);
#85103=ORIENTED_EDGE('',*,*,#57356,.T.);
#85104=ORIENTED_EDGE('',*,*,#57352,.T.);
#85105=ORIENTED_EDGE('',*,*,#57357,.F.);
#85106=ORIENTED_EDGE('',*,*,#57358,.F.);
#85107=ORIENTED_EDGE('',*,*,#57359,.T.);
#85108=ORIENTED_EDGE('',*,*,#57355,.T.);
#85109=ORIENTED_EDGE('',*,*,#57360,.F.);
#85110=ORIENTED_EDGE('',*,*,#57361,.F.);
#85111=ORIENTED_EDGE('',*,*,#57362,.T.);
#85112=ORIENTED_EDGE('',*,*,#57358,.T.);
#85113=ORIENTED_EDGE('',*,*,#57363,.F.);
#85114=ORIENTED_EDGE('',*,*,#57364,.F.);
#85115=ORIENTED_EDGE('',*,*,#57365,.T.);
#85116=ORIENTED_EDGE('',*,*,#57361,.T.);
#85117=ORIENTED_EDGE('',*,*,#57366,.F.);
#85118=ORIENTED_EDGE('',*,*,#57367,.F.);
#85119=ORIENTED_EDGE('',*,*,#57368,.T.);
#85120=ORIENTED_EDGE('',*,*,#57364,.T.);
#85121=ORIENTED_EDGE('',*,*,#57369,.F.);
#85122=ORIENTED_EDGE('',*,*,#57370,.F.);
#85123=ORIENTED_EDGE('',*,*,#57371,.T.);
#85124=ORIENTED_EDGE('',*,*,#57367,.T.);
#85125=ORIENTED_EDGE('',*,*,#57372,.F.);
#85126=ORIENTED_EDGE('',*,*,#57373,.F.);
#85127=ORIENTED_EDGE('',*,*,#57374,.T.);
#85128=ORIENTED_EDGE('',*,*,#57370,.T.);
#85129=ORIENTED_EDGE('',*,*,#57375,.F.);
#85130=ORIENTED_EDGE('',*,*,#57376,.F.);
#85131=ORIENTED_EDGE('',*,*,#57377,.T.);
#85132=ORIENTED_EDGE('',*,*,#57373,.T.);
#85133=ORIENTED_EDGE('',*,*,#57378,.F.);
#85134=ORIENTED_EDGE('',*,*,#57379,.F.);
#85135=ORIENTED_EDGE('',*,*,#57380,.T.);
#85136=ORIENTED_EDGE('',*,*,#57376,.T.);
#85137=ORIENTED_EDGE('',*,*,#57381,.F.);
#85138=ORIENTED_EDGE('',*,*,#57382,.F.);
#85139=ORIENTED_EDGE('',*,*,#57383,.T.);
#85140=ORIENTED_EDGE('',*,*,#57379,.T.);
#85141=ORIENTED_EDGE('',*,*,#57384,.F.);
#85142=ORIENTED_EDGE('',*,*,#57385,.F.);
#85143=ORIENTED_EDGE('',*,*,#57386,.T.);
#85144=ORIENTED_EDGE('',*,*,#57382,.T.);
#85145=ORIENTED_EDGE('',*,*,#57387,.F.);
#85146=ORIENTED_EDGE('',*,*,#57388,.F.);
#85147=ORIENTED_EDGE('',*,*,#57389,.T.);
#85148=ORIENTED_EDGE('',*,*,#57385,.T.);
#85149=ORIENTED_EDGE('',*,*,#57390,.F.);
#85150=ORIENTED_EDGE('',*,*,#57391,.F.);
#85151=ORIENTED_EDGE('',*,*,#57392,.T.);
#85152=ORIENTED_EDGE('',*,*,#57388,.T.);
#85153=ORIENTED_EDGE('',*,*,#57393,.F.);
#85154=ORIENTED_EDGE('',*,*,#57394,.F.);
#85155=ORIENTED_EDGE('',*,*,#57395,.T.);
#85156=ORIENTED_EDGE('',*,*,#57391,.T.);
#85157=ORIENTED_EDGE('',*,*,#57396,.F.);
#85158=ORIENTED_EDGE('',*,*,#57397,.F.);
#85159=ORIENTED_EDGE('',*,*,#57398,.T.);
#85160=ORIENTED_EDGE('',*,*,#57399,.T.);
#85161=ORIENTED_EDGE('',*,*,#57394,.T.);
#85162=ORIENTED_EDGE('',*,*,#57400,.F.);
#85163=ORIENTED_EDGE('',*,*,#57401,.F.);
#85164=ORIENTED_EDGE('',*,*,#57402,.F.);
#85165=ORIENTED_EDGE('',*,*,#57403,.F.);
#85166=ORIENTED_EDGE('',*,*,#57296,.F.);
#85167=ORIENTED_EDGE('',*,*,#57404,.F.);
#85168=ORIENTED_EDGE('',*,*,#57405,.T.);
#85169=ORIENTED_EDGE('',*,*,#57401,.T.);
#85170=ORIENTED_EDGE('',*,*,#57405,.F.);
#85171=ORIENTED_EDGE('',*,*,#57406,.F.);
#85172=ORIENTED_EDGE('',*,*,#57398,.F.);
#85173=ORIENTED_EDGE('',*,*,#57292,.F.);
#85174=ORIENTED_EDGE('',*,*,#57348,.F.);
#85175=ORIENTED_EDGE('',*,*,#57407,.F.);
#85176=ORIENTED_EDGE('',*,*,#57342,.F.);
#85177=ORIENTED_EDGE('',*,*,#57339,.F.);
#85178=ORIENTED_EDGE('',*,*,#57336,.F.);
#85179=ORIENTED_EDGE('',*,*,#57333,.F.);
#85180=ORIENTED_EDGE('',*,*,#57330,.F.);
#85181=ORIENTED_EDGE('',*,*,#57327,.F.);
#85182=ORIENTED_EDGE('',*,*,#57324,.F.);
#85183=ORIENTED_EDGE('',*,*,#57321,.F.);
#85184=ORIENTED_EDGE('',*,*,#57318,.F.);
#85185=ORIENTED_EDGE('',*,*,#57315,.F.);
#85186=ORIENTED_EDGE('',*,*,#57312,.F.);
#85187=ORIENTED_EDGE('',*,*,#57309,.F.);
#85188=ORIENTED_EDGE('',*,*,#57306,.F.);
#85189=ORIENTED_EDGE('',*,*,#57303,.F.);
#85190=ORIENTED_EDGE('',*,*,#57300,.F.);
#85191=ORIENTED_EDGE('',*,*,#57297,.F.);
#85192=ORIENTED_EDGE('',*,*,#57403,.T.);
#85193=ORIENTED_EDGE('',*,*,#57408,.T.);
#85194=ORIENTED_EDGE('',*,*,#57400,.T.);
#85195=ORIENTED_EDGE('',*,*,#57396,.T.);
#85196=ORIENTED_EDGE('',*,*,#57393,.T.);
#85197=ORIENTED_EDGE('',*,*,#57390,.T.);
#85198=ORIENTED_EDGE('',*,*,#57387,.T.);
#85199=ORIENTED_EDGE('',*,*,#57384,.T.);
#85200=ORIENTED_EDGE('',*,*,#57381,.T.);
#85201=ORIENTED_EDGE('',*,*,#57378,.T.);
#85202=ORIENTED_EDGE('',*,*,#57375,.T.);
#85203=ORIENTED_EDGE('',*,*,#57372,.T.);
#85204=ORIENTED_EDGE('',*,*,#57369,.T.);
#85205=ORIENTED_EDGE('',*,*,#57366,.T.);
#85206=ORIENTED_EDGE('',*,*,#57363,.T.);
#85207=ORIENTED_EDGE('',*,*,#57360,.T.);
#85208=ORIENTED_EDGE('',*,*,#57357,.T.);
#85209=ORIENTED_EDGE('',*,*,#57354,.T.);
#85210=ORIENTED_EDGE('',*,*,#57286,.F.);
#85211=ORIENTED_EDGE('',*,*,#57289,.F.);
#85212=ORIENTED_EDGE('',*,*,#57351,.F.);
#85213=ORIENTED_EDGE('',*,*,#57353,.F.);
#85214=ORIENTED_EDGE('',*,*,#57356,.F.);
#85215=ORIENTED_EDGE('',*,*,#57359,.F.);
#85216=ORIENTED_EDGE('',*,*,#57362,.F.);
#85217=ORIENTED_EDGE('',*,*,#57365,.F.);
#85218=ORIENTED_EDGE('',*,*,#57368,.F.);
#85219=ORIENTED_EDGE('',*,*,#57371,.F.);
#85220=ORIENTED_EDGE('',*,*,#57374,.F.);
#85221=ORIENTED_EDGE('',*,*,#57377,.F.);
#85222=ORIENTED_EDGE('',*,*,#57380,.F.);
#85223=ORIENTED_EDGE('',*,*,#57383,.F.);
#85224=ORIENTED_EDGE('',*,*,#57386,.F.);
#85225=ORIENTED_EDGE('',*,*,#57389,.F.);
#85226=ORIENTED_EDGE('',*,*,#57392,.F.);
#85227=ORIENTED_EDGE('',*,*,#57395,.F.);
#85228=ORIENTED_EDGE('',*,*,#57399,.F.);
#85229=ORIENTED_EDGE('',*,*,#57406,.T.);
#85230=ORIENTED_EDGE('',*,*,#57404,.T.);
#85231=ORIENTED_EDGE('',*,*,#57295,.F.);
#85232=ORIENTED_EDGE('',*,*,#57299,.F.);
#85233=ORIENTED_EDGE('',*,*,#57302,.F.);
#85234=ORIENTED_EDGE('',*,*,#57305,.F.);
#85235=ORIENTED_EDGE('',*,*,#57308,.F.);
#85236=ORIENTED_EDGE('',*,*,#57311,.F.);
#85237=ORIENTED_EDGE('',*,*,#57314,.F.);
#85238=ORIENTED_EDGE('',*,*,#57317,.F.);
#85239=ORIENTED_EDGE('',*,*,#57320,.F.);
#85240=ORIENTED_EDGE('',*,*,#57323,.F.);
#85241=ORIENTED_EDGE('',*,*,#57326,.F.);
#85242=ORIENTED_EDGE('',*,*,#57329,.F.);
#85243=ORIENTED_EDGE('',*,*,#57332,.F.);
#85244=ORIENTED_EDGE('',*,*,#57335,.F.);
#85245=ORIENTED_EDGE('',*,*,#57338,.F.);
#85246=ORIENTED_EDGE('',*,*,#57341,.F.);
#85247=ORIENTED_EDGE('',*,*,#57409,.F.);
#85248=ORIENTED_EDGE('',*,*,#57346,.F.);
#85249=ORIENTED_EDGE('',*,*,#57410,.F.);
#85250=ORIENTED_EDGE('',*,*,#57293,.F.);
#85251=ORIENTED_EDGE('',*,*,#57397,.T.);
#85252=ORIENTED_EDGE('',*,*,#57408,.F.);
#85253=ORIENTED_EDGE('',*,*,#57402,.T.);
#85254=ORIENTED_EDGE('',*,*,#57411,.T.);
#85255=ORIENTED_EDGE('',*,*,#57412,.T.);
#85256=ORIENTED_EDGE('',*,*,#57413,.T.);
#85257=ORIENTED_EDGE('',*,*,#57414,.T.);
#85258=ORIENTED_EDGE('',*,*,#57415,.T.);
#85259=ORIENTED_EDGE('',*,*,#57416,.T.);
#85260=ORIENTED_EDGE('',*,*,#57417,.T.);
#85261=ORIENTED_EDGE('',*,*,#57418,.T.);
#85262=ORIENTED_EDGE('',*,*,#57419,.T.);
#85263=ORIENTED_EDGE('',*,*,#57420,.T.);
#85264=ORIENTED_EDGE('',*,*,#57421,.T.);
#85265=ORIENTED_EDGE('',*,*,#57422,.T.);
#85266=ORIENTED_EDGE('',*,*,#57423,.T.);
#85267=ORIENTED_EDGE('',*,*,#57424,.T.);
#85268=ORIENTED_EDGE('',*,*,#57425,.T.);
#85269=ORIENTED_EDGE('',*,*,#57426,.T.);
#85270=ORIENTED_EDGE('',*,*,#57427,.F.);
#85271=ORIENTED_EDGE('',*,*,#57428,.F.);
#85272=ORIENTED_EDGE('',*,*,#57429,.T.);
#85273=ORIENTED_EDGE('',*,*,#57413,.F.);
#85274=ORIENTED_EDGE('',*,*,#57429,.F.);
#85275=ORIENTED_EDGE('',*,*,#57430,.F.);
#85276=ORIENTED_EDGE('',*,*,#57431,.T.);
#85277=ORIENTED_EDGE('',*,*,#57414,.F.);
#85278=ORIENTED_EDGE('',*,*,#57431,.F.);
#85279=ORIENTED_EDGE('',*,*,#57432,.F.);
#85280=ORIENTED_EDGE('',*,*,#57433,.T.);
#85281=ORIENTED_EDGE('',*,*,#57411,.F.);
#85282=ORIENTED_EDGE('',*,*,#57433,.F.);
#85283=ORIENTED_EDGE('',*,*,#57434,.F.);
#85284=ORIENTED_EDGE('',*,*,#57427,.T.);
#85285=ORIENTED_EDGE('',*,*,#57412,.F.);
#85286=ORIENTED_EDGE('',*,*,#57435,.F.);
#85287=ORIENTED_EDGE('',*,*,#57436,.F.);
#85288=ORIENTED_EDGE('',*,*,#57437,.T.);
#85289=ORIENTED_EDGE('',*,*,#57417,.F.);
#85290=ORIENTED_EDGE('',*,*,#57437,.F.);
#85291=ORIENTED_EDGE('',*,*,#57438,.F.);
#85292=ORIENTED_EDGE('',*,*,#57439,.T.);
#85293=ORIENTED_EDGE('',*,*,#57418,.F.);
#85294=ORIENTED_EDGE('',*,*,#57439,.F.);
#85295=ORIENTED_EDGE('',*,*,#57440,.F.);
#85296=ORIENTED_EDGE('',*,*,#57441,.T.);
#85297=ORIENTED_EDGE('',*,*,#57415,.F.);
#85298=ORIENTED_EDGE('',*,*,#57441,.F.);
#85299=ORIENTED_EDGE('',*,*,#57442,.F.);
#85300=ORIENTED_EDGE('',*,*,#57435,.T.);
#85301=ORIENTED_EDGE('',*,*,#57416,.F.);
#85302=ORIENTED_EDGE('',*,*,#57443,.F.);
#85303=ORIENTED_EDGE('',*,*,#57444,.F.);
#85304=ORIENTED_EDGE('',*,*,#57445,.T.);
#85305=ORIENTED_EDGE('',*,*,#57421,.F.);
#85306=ORIENTED_EDGE('',*,*,#57445,.F.);
#85307=ORIENTED_EDGE('',*,*,#57446,.F.);
#85308=ORIENTED_EDGE('',*,*,#57447,.T.);
#85309=ORIENTED_EDGE('',*,*,#57422,.F.);
#85310=ORIENTED_EDGE('',*,*,#57447,.F.);
#85311=ORIENTED_EDGE('',*,*,#57448,.F.);
#85312=ORIENTED_EDGE('',*,*,#57449,.T.);
#85313=ORIENTED_EDGE('',*,*,#57419,.F.);
#85314=ORIENTED_EDGE('',*,*,#57449,.F.);
#85315=ORIENTED_EDGE('',*,*,#57450,.F.);
#85316=ORIENTED_EDGE('',*,*,#57443,.T.);
#85317=ORIENTED_EDGE('',*,*,#57420,.F.);
#85318=ORIENTED_EDGE('',*,*,#57451,.F.);
#85319=ORIENTED_EDGE('',*,*,#57452,.F.);
#85320=ORIENTED_EDGE('',*,*,#57453,.T.);
#85321=ORIENTED_EDGE('',*,*,#57425,.F.);
#85322=ORIENTED_EDGE('',*,*,#57453,.F.);
#85323=ORIENTED_EDGE('',*,*,#57454,.F.);
#85324=ORIENTED_EDGE('',*,*,#57455,.T.);
#85325=ORIENTED_EDGE('',*,*,#57426,.F.);
#85326=ORIENTED_EDGE('',*,*,#57455,.F.);
#85327=ORIENTED_EDGE('',*,*,#57456,.F.);
#85328=ORIENTED_EDGE('',*,*,#57457,.T.);
#85329=ORIENTED_EDGE('',*,*,#57423,.F.);
#85330=ORIENTED_EDGE('',*,*,#57457,.F.);
#85331=ORIENTED_EDGE('',*,*,#57458,.F.);
#85332=ORIENTED_EDGE('',*,*,#57451,.T.);
#85333=ORIENTED_EDGE('',*,*,#57424,.F.);
#85334=ORIENTED_EDGE('',*,*,#57459,.T.);
#85335=ORIENTED_EDGE('',*,*,#57460,.T.);
#85336=ORIENTED_EDGE('',*,*,#57461,.T.);
#85337=ORIENTED_EDGE('',*,*,#57462,.T.);
#85338=ORIENTED_EDGE('',*,*,#57463,.T.);
#85339=ORIENTED_EDGE('',*,*,#57464,.T.);
#85340=ORIENTED_EDGE('',*,*,#57465,.T.);
#85341=ORIENTED_EDGE('',*,*,#57466,.T.);
#85342=ORIENTED_EDGE('',*,*,#57434,.T.);
#85343=ORIENTED_EDGE('',*,*,#57432,.T.);
#85344=ORIENTED_EDGE('',*,*,#57430,.T.);
#85345=ORIENTED_EDGE('',*,*,#57428,.T.);
#85346=ORIENTED_EDGE('',*,*,#57442,.T.);
#85347=ORIENTED_EDGE('',*,*,#57440,.T.);
#85348=ORIENTED_EDGE('',*,*,#57438,.T.);
#85349=ORIENTED_EDGE('',*,*,#57436,.T.);
#85350=ORIENTED_EDGE('',*,*,#57467,.T.);
#85351=ORIENTED_EDGE('',*,*,#57468,.T.);
#85352=ORIENTED_EDGE('',*,*,#57469,.T.);
#85353=ORIENTED_EDGE('',*,*,#57470,.T.);
#85354=ORIENTED_EDGE('',*,*,#57471,.T.);
#85355=ORIENTED_EDGE('',*,*,#57472,.T.);
#85356=ORIENTED_EDGE('',*,*,#57473,.T.);
#85357=ORIENTED_EDGE('',*,*,#57474,.T.);
#85358=ORIENTED_EDGE('',*,*,#57450,.T.);
#85359=ORIENTED_EDGE('',*,*,#57448,.T.);
#85360=ORIENTED_EDGE('',*,*,#57446,.T.);
#85361=ORIENTED_EDGE('',*,*,#57444,.T.);
#85362=ORIENTED_EDGE('',*,*,#57458,.T.);
#85363=ORIENTED_EDGE('',*,*,#57456,.T.);
#85364=ORIENTED_EDGE('',*,*,#57454,.T.);
#85365=ORIENTED_EDGE('',*,*,#57452,.T.);
#85366=ORIENTED_EDGE('',*,*,#57475,.T.);
#85367=ORIENTED_EDGE('',*,*,#57476,.T.);
#85368=ORIENTED_EDGE('',*,*,#57477,.T.);
#85369=ORIENTED_EDGE('',*,*,#57478,.T.);
#85370=ORIENTED_EDGE('',*,*,#57479,.F.);
#85371=ORIENTED_EDGE('',*,*,#57463,.F.);
#85372=ORIENTED_EDGE('',*,*,#57480,.T.);
#85373=ORIENTED_EDGE('',*,*,#57481,.F.);
#85374=ORIENTED_EDGE('',*,*,#57482,.F.);
#85375=ORIENTED_EDGE('',*,*,#57464,.F.);
#85376=ORIENTED_EDGE('',*,*,#57479,.T.);
#85377=ORIENTED_EDGE('',*,*,#57483,.F.);
#85378=ORIENTED_EDGE('',*,*,#57484,.F.);
#85379=ORIENTED_EDGE('',*,*,#57465,.F.);
#85380=ORIENTED_EDGE('',*,*,#57482,.T.);
#85381=ORIENTED_EDGE('',*,*,#57485,.F.);
#85382=ORIENTED_EDGE('',*,*,#57486,.F.);
#85383=ORIENTED_EDGE('',*,*,#57466,.F.);
#85384=ORIENTED_EDGE('',*,*,#57484,.T.);
#85385=ORIENTED_EDGE('',*,*,#57487,.F.);
#85386=ORIENTED_EDGE('',*,*,#57488,.F.);
#85387=ORIENTED_EDGE('',*,*,#57459,.F.);
#85388=ORIENTED_EDGE('',*,*,#57486,.T.);
#85389=ORIENTED_EDGE('',*,*,#57489,.F.);
#85390=ORIENTED_EDGE('',*,*,#57490,.F.);
#85391=ORIENTED_EDGE('',*,*,#57460,.F.);
#85392=ORIENTED_EDGE('',*,*,#57488,.T.);
#85393=ORIENTED_EDGE('',*,*,#57491,.F.);
#85394=ORIENTED_EDGE('',*,*,#57492,.F.);
#85395=ORIENTED_EDGE('',*,*,#57461,.F.);
#85396=ORIENTED_EDGE('',*,*,#57490,.T.);
#85397=ORIENTED_EDGE('',*,*,#57493,.F.);
#85398=ORIENTED_EDGE('',*,*,#57480,.F.);
#85399=ORIENTED_EDGE('',*,*,#57462,.F.);
#85400=ORIENTED_EDGE('',*,*,#57492,.T.);
#85401=ORIENTED_EDGE('',*,*,#57494,.F.);
#85402=ORIENTED_EDGE('',*,*,#57495,.F.);
#85403=ORIENTED_EDGE('',*,*,#57471,.F.);
#85404=ORIENTED_EDGE('',*,*,#57496,.T.);
#85405=ORIENTED_EDGE('',*,*,#57497,.F.);
#85406=ORIENTED_EDGE('',*,*,#57498,.F.);
#85407=ORIENTED_EDGE('',*,*,#57472,.F.);
#85408=ORIENTED_EDGE('',*,*,#57495,.T.);
#85409=ORIENTED_EDGE('',*,*,#57499,.F.);
#85410=ORIENTED_EDGE('',*,*,#57500,.F.);
#85411=ORIENTED_EDGE('',*,*,#57473,.F.);
#85412=ORIENTED_EDGE('',*,*,#57498,.T.);
#85413=ORIENTED_EDGE('',*,*,#57501,.F.);
#85414=ORIENTED_EDGE('',*,*,#57502,.F.);
#85415=ORIENTED_EDGE('',*,*,#57474,.F.);
#85416=ORIENTED_EDGE('',*,*,#57500,.T.);
#85417=ORIENTED_EDGE('',*,*,#57503,.F.);
#85418=ORIENTED_EDGE('',*,*,#57504,.F.);
#85419=ORIENTED_EDGE('',*,*,#57467,.F.);
#85420=ORIENTED_EDGE('',*,*,#57502,.T.);
#85421=ORIENTED_EDGE('',*,*,#57505,.F.);
#85422=ORIENTED_EDGE('',*,*,#57506,.F.);
#85423=ORIENTED_EDGE('',*,*,#57468,.F.);
#85424=ORIENTED_EDGE('',*,*,#57504,.T.);
#85425=ORIENTED_EDGE('',*,*,#57507,.F.);
#85426=ORIENTED_EDGE('',*,*,#57508,.F.);
#85427=ORIENTED_EDGE('',*,*,#57469,.F.);
#85428=ORIENTED_EDGE('',*,*,#57506,.T.);
#85429=ORIENTED_EDGE('',*,*,#57509,.F.);
#85430=ORIENTED_EDGE('',*,*,#57496,.F.);
#85431=ORIENTED_EDGE('',*,*,#57470,.F.);
#85432=ORIENTED_EDGE('',*,*,#57508,.T.);
#85433=ORIENTED_EDGE('',*,*,#57510,.F.);
#85434=ORIENTED_EDGE('',*,*,#57511,.F.);
#85435=ORIENTED_EDGE('',*,*,#57475,.F.);
#85436=ORIENTED_EDGE('',*,*,#57512,.T.);
#85437=ORIENTED_EDGE('',*,*,#57513,.F.);
#85438=ORIENTED_EDGE('',*,*,#57514,.F.);
#85439=ORIENTED_EDGE('',*,*,#57476,.F.);
#85440=ORIENTED_EDGE('',*,*,#57511,.T.);
#85441=ORIENTED_EDGE('',*,*,#57515,.F.);
#85442=ORIENTED_EDGE('',*,*,#57516,.F.);
#85443=ORIENTED_EDGE('',*,*,#57477,.F.);
#85444=ORIENTED_EDGE('',*,*,#57514,.T.);
#85445=ORIENTED_EDGE('',*,*,#57517,.F.);
#85446=ORIENTED_EDGE('',*,*,#57512,.F.);
#85447=ORIENTED_EDGE('',*,*,#57478,.F.);
#85448=ORIENTED_EDGE('',*,*,#57516,.T.);
#85449=ORIENTED_EDGE('',*,*,#57518,.F.);
#85450=ORIENTED_EDGE('',*,*,#57519,.T.);
#85451=ORIENTED_EDGE('',*,*,#57520,.T.);
#85452=ORIENTED_EDGE('',*,*,#57521,.T.);
#85453=ORIENTED_EDGE('',*,*,#57522,.T.);
#85454=ORIENTED_EDGE('',*,*,#57523,.T.);
#85455=ORIENTED_EDGE('',*,*,#57524,.T.);
#85456=ORIENTED_EDGE('',*,*,#57494,.T.);
#85457=ORIENTED_EDGE('',*,*,#57493,.T.);
#85458=ORIENTED_EDGE('',*,*,#57491,.T.);
#85459=ORIENTED_EDGE('',*,*,#57489,.T.);
#85460=ORIENTED_EDGE('',*,*,#57487,.T.);
#85461=ORIENTED_EDGE('',*,*,#57485,.T.);
#85462=ORIENTED_EDGE('',*,*,#57483,.T.);
#85463=ORIENTED_EDGE('',*,*,#57481,.T.);
#85464=ORIENTED_EDGE('',*,*,#57510,.T.);
#85465=ORIENTED_EDGE('',*,*,#57509,.T.);
#85466=ORIENTED_EDGE('',*,*,#57507,.T.);
#85467=ORIENTED_EDGE('',*,*,#57505,.T.);
#85468=ORIENTED_EDGE('',*,*,#57503,.T.);
#85469=ORIENTED_EDGE('',*,*,#57501,.T.);
#85470=ORIENTED_EDGE('',*,*,#57499,.T.);
#85471=ORIENTED_EDGE('',*,*,#57497,.T.);
#85472=ORIENTED_EDGE('',*,*,#57518,.T.);
#85473=ORIENTED_EDGE('',*,*,#57517,.T.);
#85474=ORIENTED_EDGE('',*,*,#57515,.T.);
#85475=ORIENTED_EDGE('',*,*,#57513,.T.);
#85476=ORIENTED_EDGE('',*,*,#57525,.T.);
#85477=ORIENTED_EDGE('',*,*,#57526,.T.);
#85478=ORIENTED_EDGE('',*,*,#57524,.F.);
#85479=ORIENTED_EDGE('',*,*,#57527,.T.);
#85480=ORIENTED_EDGE('',*,*,#57528,.T.);
#85481=ORIENTED_EDGE('',*,*,#57519,.F.);
#85482=ORIENTED_EDGE('',*,*,#57529,.T.);
#85483=ORIENTED_EDGE('',*,*,#57530,.T.);
#85484=ORIENTED_EDGE('',*,*,#57520,.F.);
#85485=ORIENTED_EDGE('',*,*,#57531,.T.);
#85486=ORIENTED_EDGE('',*,*,#57532,.T.);
#85487=ORIENTED_EDGE('',*,*,#57521,.F.);
#85488=ORIENTED_EDGE('',*,*,#57533,.T.);
#85489=ORIENTED_EDGE('',*,*,#57534,.T.);
#85490=ORIENTED_EDGE('',*,*,#57523,.F.);
#85491=ORIENTED_EDGE('',*,*,#57535,.T.);
#85492=ORIENTED_EDGE('',*,*,#57522,.F.);
#85493=ORIENTED_EDGE('',*,*,#57536,.T.);
#85494=ORIENTED_EDGE('',*,*,#57534,.F.);
#85495=ORIENTED_EDGE('',*,*,#57537,.T.);
#85496=ORIENTED_EDGE('',*,*,#57538,.T.);
#85497=ORIENTED_EDGE('',*,*,#57539,.F.);
#85498=ORIENTED_EDGE('',*,*,#57525,.F.);
#85499=ORIENTED_EDGE('',*,*,#57526,.F.);
#85500=ORIENTED_EDGE('',*,*,#57539,.T.);
#85501=ORIENTED_EDGE('',*,*,#57540,.T.);
#85502=ORIENTED_EDGE('',*,*,#57541,.F.);
#85503=ORIENTED_EDGE('',*,*,#57527,.F.);
#85504=ORIENTED_EDGE('',*,*,#57528,.F.);
#85505=ORIENTED_EDGE('',*,*,#57541,.T.);
#85506=ORIENTED_EDGE('',*,*,#57542,.T.);
#85507=ORIENTED_EDGE('',*,*,#57543,.F.);
#85508=ORIENTED_EDGE('',*,*,#57529,.F.);
#85509=ORIENTED_EDGE('',*,*,#57530,.F.);
#85510=ORIENTED_EDGE('',*,*,#57543,.T.);
#85511=ORIENTED_EDGE('',*,*,#57544,.T.);
#85512=ORIENTED_EDGE('',*,*,#57545,.F.);
#85513=ORIENTED_EDGE('',*,*,#57531,.F.);
#85514=ORIENTED_EDGE('',*,*,#57532,.F.);
#85515=ORIENTED_EDGE('',*,*,#57545,.T.);
#85516=ORIENTED_EDGE('',*,*,#57546,.T.);
#85517=ORIENTED_EDGE('',*,*,#57547,.F.);
#85518=ORIENTED_EDGE('',*,*,#57536,.F.);
#85519=ORIENTED_EDGE('',*,*,#57535,.F.);
#85520=ORIENTED_EDGE('',*,*,#57547,.T.);
#85521=ORIENTED_EDGE('',*,*,#57548,.T.);
#85522=ORIENTED_EDGE('',*,*,#57537,.F.);
#85523=ORIENTED_EDGE('',*,*,#57533,.F.);
#85524=ORIENTED_EDGE('',*,*,#57548,.F.);
#85525=ORIENTED_EDGE('',*,*,#57546,.F.);
#85526=ORIENTED_EDGE('',*,*,#57544,.F.);
#85527=ORIENTED_EDGE('',*,*,#57542,.F.);
#85528=ORIENTED_EDGE('',*,*,#57540,.F.);
#85529=ORIENTED_EDGE('',*,*,#57538,.F.);
#85530=ORIENTED_EDGE('',*,*,#57343,.T.);
#85531=ORIENTED_EDGE('',*,*,#57347,.F.);
#85532=ORIENTED_EDGE('',*,*,#57409,.T.);
#85533=ORIENTED_EDGE('',*,*,#57340,.T.);
#85534=ORIENTED_EDGE('',*,*,#57407,.T.);
#85535=ORIENTED_EDGE('',*,*,#57290,.T.);
#85536=ORIENTED_EDGE('',*,*,#57410,.T.);
#85537=ORIENTED_EDGE('',*,*,#57345,.T.);
#85538=ORIENTED_EDGE('',*,*,#57349,.T.);
#87914=CYLINDRICAL_SURFACE('',#104643,6.);
#87915=CYLINDRICAL_SURFACE('',#104645,6.);
#87916=CYLINDRICAL_SURFACE('',#104646,6.);
#87917=CYLINDRICAL_SURFACE('',#104647,6.);
#87918=CYLINDRICAL_SURFACE('',#104648,6.);
#87919=CYLINDRICAL_SURFACE('',#104649,6.);
#87920=CYLINDRICAL_SURFACE('',#104650,6.);
#87921=CYLINDRICAL_SURFACE('',#104651,6.);
#87922=CYLINDRICAL_SURFACE('',#104652,6.);
#87923=CYLINDRICAL_SURFACE('',#104653,6.);
#87924=CYLINDRICAL_SURFACE('',#104654,6.);
#87925=CYLINDRICAL_SURFACE('',#104655,6.);
#87926=CYLINDRICAL_SURFACE('',#104656,6.);
#87927=CYLINDRICAL_SURFACE('',#104657,6.);
#87928=CYLINDRICAL_SURFACE('',#104658,6.);
#87929=CYLINDRICAL_SURFACE('',#104659,6.);
#87930=CYLINDRICAL_SURFACE('',#104660,6.);
#87931=CYLINDRICAL_SURFACE('',#104664,4.86334165753294);
#87932=CYLINDRICAL_SURFACE('',#104665,4.86334165753294);
#87933=CYLINDRICAL_SURFACE('',#104666,4.86334165753294);
#87934=CYLINDRICAL_SURFACE('',#104667,4.86334165753294);
#87935=CYLINDRICAL_SURFACE('',#104668,4.86334165753294);
#87936=CYLINDRICAL_SURFACE('',#104669,4.86334165753294);
#87937=CYLINDRICAL_SURFACE('',#104670,4.86334165753294);
#87938=CYLINDRICAL_SURFACE('',#104671,4.86334165753294);
#87939=CYLINDRICAL_SURFACE('',#104672,4.86334165753294);
#87940=CYLINDRICAL_SURFACE('',#104673,4.86334165753294);
#87941=CYLINDRICAL_SURFACE('',#104674,4.86334165753294);
#87942=CYLINDRICAL_SURFACE('',#104675,4.86334165753294);
#87943=CYLINDRICAL_SURFACE('',#104676,4.86334165753294);
#87944=CYLINDRICAL_SURFACE('',#104677,4.86334165753294);
#87945=CYLINDRICAL_SURFACE('',#104678,4.86334165753294);
#87946=CYLINDRICAL_SURFACE('',#104679,4.86334165753294);
#87947=CYLINDRICAL_SURFACE('',#104680,4.86334165753294);
#87948=CYLINDRICAL_SURFACE('',#104686,4.86334165753294);
#87949=CYLINDRICAL_SURFACE('',#104718,6.);
#93564=ADVANCED_FACE('',(#14285),#7197,.T.);
#93565=ADVANCED_FACE('',(#14286),#7198,.T.);
#93566=ADVANCED_FACE('',(#14287),#87914,.T.);
#93567=ADVANCED_FACE('',(#14288),#87915,.T.);
#93568=ADVANCED_FACE('',(#14289),#87916,.T.);
#93569=ADVANCED_FACE('',(#14290),#87917,.T.);
#93570=ADVANCED_FACE('',(#14291),#87918,.T.);
#93571=ADVANCED_FACE('',(#14292),#87919,.T.);
#93572=ADVANCED_FACE('',(#14293),#87920,.T.);
#93573=ADVANCED_FACE('',(#14294),#87921,.T.);
#93574=ADVANCED_FACE('',(#14295),#87922,.T.);
#93575=ADVANCED_FACE('',(#14296),#87923,.T.);
#93576=ADVANCED_FACE('',(#14297),#87924,.T.);
#93577=ADVANCED_FACE('',(#14298),#87925,.T.);
#93578=ADVANCED_FACE('',(#14299),#87926,.T.);
#93579=ADVANCED_FACE('',(#14300),#87927,.T.);
#93580=ADVANCED_FACE('',(#14301),#87928,.T.);
#93581=ADVANCED_FACE('',(#14302),#87929,.T.);
#93582=ADVANCED_FACE('',(#14303),#87930,.T.);
#93583=ADVANCED_FACE('',(#14304),#87931,.T.);
#93584=ADVANCED_FACE('',(#14305),#87932,.T.);
#93585=ADVANCED_FACE('',(#14306),#87933,.T.);
#93586=ADVANCED_FACE('',(#14307),#87934,.T.);
#93587=ADVANCED_FACE('',(#14308),#87935,.T.);
#93588=ADVANCED_FACE('',(#14309),#87936,.T.);
#93589=ADVANCED_FACE('',(#14310),#87937,.T.);
#93590=ADVANCED_FACE('',(#14311),#87938,.T.);
#93591=ADVANCED_FACE('',(#14312),#87939,.T.);
#93592=ADVANCED_FACE('',(#14313),#87940,.T.);
#93593=ADVANCED_FACE('',(#14314),#87941,.T.);
#93594=ADVANCED_FACE('',(#14315),#87942,.T.);
#93595=ADVANCED_FACE('',(#14316),#87943,.T.);
#93596=ADVANCED_FACE('',(#14317),#87944,.T.);
#93597=ADVANCED_FACE('',(#14318),#87945,.T.);
#93598=ADVANCED_FACE('',(#14319),#87946,.T.);
#93599=ADVANCED_FACE('',(#14320),#87947,.T.);
#93600=ADVANCED_FACE('',(#14321),#8660,.F.);
#93601=ADVANCED_FACE('',(#14322),#7199,.T.);
#93602=ADVANCED_FACE('',(#14323),#3202,.T.);
#93603=ADVANCED_FACE('',(#14324),#3203,.T.);
#93604=ADVANCED_FACE('',(#14325),#87948,.T.);
#93605=ADVANCED_FACE('',(#14326),#8661,.T.);
#93606=ADVANCED_FACE('',(#14327),#8662,.T.);
#93607=ADVANCED_FACE('',(#14328),#8663,.T.);
#93608=ADVANCED_FACE('',(#14329),#8664,.T.);
#93609=ADVANCED_FACE('',(#14330),#984,.T.);
#93610=ADVANCED_FACE('',(#14331),#985,.T.);
#93611=ADVANCED_FACE('',(#14332),#986,.T.);
#93612=ADVANCED_FACE('',(#14333),#987,.T.);
#93613=ADVANCED_FACE('',(#14334),#988,.T.);
#93614=ADVANCED_FACE('',(#14335),#989,.T.);
#93615=ADVANCED_FACE('',(#14336),#990,.T.);
#93616=ADVANCED_FACE('',(#14337),#991,.T.);
#93617=ADVANCED_FACE('',(#14338),#992,.T.);
#93618=ADVANCED_FACE('',(#14339),#993,.T.);
#93619=ADVANCED_FACE('',(#14340),#994,.T.);
#93620=ADVANCED_FACE('',(#14341),#995,.T.);
#93621=ADVANCED_FACE('',(#14342),#996,.T.);
#93622=ADVANCED_FACE('',(#14343),#997,.T.);
#93623=ADVANCED_FACE('',(#14344),#998,.T.);
#93624=ADVANCED_FACE('',(#14345),#999,.T.);
#93625=ADVANCED_FACE('',(#14346,#7696,#7697),#8665,.T.);
#93626=ADVANCED_FACE('',(#14347,#7698,#7699),#8666,.T.);
#93627=ADVANCED_FACE('',(#14348),#8667,.T.);
#93628=ADVANCED_FACE('',(#14349),#1000,.T.);
#93629=ADVANCED_FACE('',(#14350),#1001,.T.);
#93630=ADVANCED_FACE('',(#14351),#1002,.T.);
#93631=ADVANCED_FACE('',(#14352),#1003,.T.);
#93632=ADVANCED_FACE('',(#14353),#1004,.T.);
#93633=ADVANCED_FACE('',(#14354),#1005,.T.);
#93634=ADVANCED_FACE('',(#14355),#1006,.T.);
#93635=ADVANCED_FACE('',(#14356),#1007,.T.);
#93636=ADVANCED_FACE('',(#14357),#1008,.T.);
#93637=ADVANCED_FACE('',(#14358),#1009,.T.);
#93638=ADVANCED_FACE('',(#14359),#1010,.T.);
#93639=ADVANCED_FACE('',(#14360),#1011,.T.);
#93640=ADVANCED_FACE('',(#14361),#1012,.T.);
#93641=ADVANCED_FACE('',(#14362),#1013,.T.);
#93642=ADVANCED_FACE('',(#14363),#1014,.T.);
#93643=ADVANCED_FACE('',(#14364),#1015,.T.);
#93644=ADVANCED_FACE('',(#14365),#8668,.T.);
#93645=ADVANCED_FACE('',(#14366),#8669,.T.);
#93646=ADVANCED_FACE('',(#14367),#8670,.T.);
#93647=ADVANCED_FACE('',(#14368),#8671,.T.);
#93648=ADVANCED_FACE('',(#14369,#7700,#7701,#7702),#8672,.T.);
#93649=ADVANCED_FACE('',(#14370),#7200,.T.);
#93650=ADVANCED_FACE('',(#14371),#7201,.T.);
#93651=ADVANCED_FACE('',(#14372),#7202,.T.);
#93652=ADVANCED_FACE('',(#14373),#7203,.T.);
#93653=ADVANCED_FACE('',(#14374),#7204,.T.);
#93654=ADVANCED_FACE('',(#14375),#7205,.T.);
#93655=ADVANCED_FACE('',(#14376),#8673,.F.);
#93656=ADVANCED_FACE('',(#14377),#8674,.F.);
#93657=ADVANCED_FACE('',(#14378),#8675,.F.);
#93658=ADVANCED_FACE('',(#14379),#8676,.F.);
#93659=ADVANCED_FACE('',(#14380),#8677,.F.);
#93660=ADVANCED_FACE('',(#14381),#8678,.F.);
#93661=ADVANCED_FACE('',(#14382,#7703),#8679,.F.);
#93662=ADVANCED_FACE('',(#14383),#87949,.T.);
#93663=ADVANCED_FACE('',(#14384),#7206,.T.);
#93773=CLOSED_SHELL('',(#93564,#93565,#93566,#93567,#93568,#93569,#93570,
#93571,#93572,#93573,#93574,#93575,#93576,#93577,#93578,#93579,#93580,#93581,
#93582,#93583,#93584,#93585,#93586,#93587,#93588,#93589,#93590,#93591,#93592,
#93593,#93594,#93595,#93596,#93597,#93598,#93599,#93600,#93601,#93602,#93603,
#93604,#93605,#93606,#93607,#93608,#93609,#93610,#93611,#93612,#93613,#93614,
#93615,#93616,#93617,#93618,#93619,#93620,#93621,#93622,#93623,#93624,#93625,
#93626,#93627,#93628,#93629,#93630,#93631,#93632,#93633,#93634,#93635,#93636,
#93637,#93638,#93639,#93640,#93641,#93642,#93643,#93644,#93645,#93646,#93647,
#93648,#93649,#93650,#93651,#93652,#93653,#93654,#93655,#93656,#93657,#93658,
#93659,#93660,#93661,#93662,#93663));
#104637=AXIS2_PLACEMENT_3D('',#303016,#130441,#130442);
#104638=AXIS2_PLACEMENT_3D('',#303017,#130443,#130444);
#104639=AXIS2_PLACEMENT_3D('',#303039,#130446,#130447);
#104640=AXIS2_PLACEMENT_3D('',#303041,#130448,#130449);
#104641=AXIS2_PLACEMENT_3D('',#303054,#130450,#130451);
#104642=AXIS2_PLACEMENT_3D('',#303059,#130453,#130454);
#104643=AXIS2_PLACEMENT_3D('',#303120,#130455,#130456);
#104644=AXIS2_PLACEMENT_3D('',#303142,#130458,#130459);
#104645=AXIS2_PLACEMENT_3D('',#303155,#130460,#130461);
#104646=AXIS2_PLACEMENT_3D('',#303231,#130463,#130464);
#104647=AXIS2_PLACEMENT_3D('',#303309,#130466,#130467);
#104648=AXIS2_PLACEMENT_3D('',#303385,#130469,#130470);
#104649=AXIS2_PLACEMENT_3D('',#303461,#130472,#130473);
#104650=AXIS2_PLACEMENT_3D('',#303537,#130475,#130476);
#104651=AXIS2_PLACEMENT_3D('',#303613,#130478,#130479);
#104652=AXIS2_PLACEMENT_3D('',#303689,#130481,#130482);
#104653=AXIS2_PLACEMENT_3D('',#303765,#130484,#130485);
#104654=AXIS2_PLACEMENT_3D('',#303843,#130487,#130488);
#104655=AXIS2_PLACEMENT_3D('',#303921,#130490,#130491);
#104656=AXIS2_PLACEMENT_3D('',#303997,#130493,#130494);
#104657=AXIS2_PLACEMENT_3D('',#304073,#130496,#130497);
#104658=AXIS2_PLACEMENT_3D('',#304149,#130499,#130500);
#104659=AXIS2_PLACEMENT_3D('',#304225,#130502,#130503);
#104660=AXIS2_PLACEMENT_3D('',#304301,#130505,#130506);
#104661=AXIS2_PLACEMENT_3D('',#304303,#130507,#130508);
#104662=AXIS2_PLACEMENT_3D('',#304307,#130510,#130511);
#104663=AXIS2_PLACEMENT_3D('',#304325,#130513,#130514);
#104664=AXIS2_PLACEMENT_3D('',#304326,#130515,#130516);
#104665=AXIS2_PLACEMENT_3D('',#304332,#130518,#130519);
#104666=AXIS2_PLACEMENT_3D('',#304378,#130521,#130522);
#104667=AXIS2_PLACEMENT_3D('',#304424,#130524,#130525);
#104668=AXIS2_PLACEMENT_3D('',#304470,#130527,#130528);
#104669=AXIS2_PLACEMENT_3D('',#304516,#130530,#130531);
#104670=AXIS2_PLACEMENT_3D('',#304562,#130533,#130534);
#104671=AXIS2_PLACEMENT_3D('',#304608,#130536,#130537);
#104672=AXIS2_PLACEMENT_3D('',#304654,#130539,#130540);
#104673=AXIS2_PLACEMENT_3D('',#304700,#130542,#130543);
#104674=AXIS2_PLACEMENT_3D('',#304746,#130545,#130546);
#104675=AXIS2_PLACEMENT_3D('',#304792,#130548,#130549);
#104676=AXIS2_PLACEMENT_3D('',#304838,#130551,#130552);
#104677=AXIS2_PLACEMENT_3D('',#304884,#130554,#130555);
#104678=AXIS2_PLACEMENT_3D('',#304930,#130557,#130558);
#104679=AXIS2_PLACEMENT_3D('',#304976,#130560,#130561);
#104680=AXIS2_PLACEMENT_3D('',#305022,#130563,#130564);
#104681=AXIS2_PLACEMENT_3D('',#305027,#130566,#130567);
#104682=AXIS2_PLACEMENT_3D('',#305068,#130568,#130569);
#104683=AXIS2_PLACEMENT_3D('',#305070,#130570,#130571);
#104684=AXIS2_PLACEMENT_3D('',#305071,#130572,#130573);
#104685=AXIS2_PLACEMENT_3D('',#305073,#130574,#130575);
#104686=AXIS2_PLACEMENT_3D('',#306683,#130577,#130578);
#104687=AXIS2_PLACEMENT_3D('',#306684,#130579,#130580);
#104688=AXIS2_PLACEMENT_3D('',#306765,#130581,#130582);
#104689=AXIS2_PLACEMENT_3D('',#306814,#130583,#130584);
#104690=AXIS2_PLACEMENT_3D('',#306895,#130585,#130586);
#104691=AXIS2_PLACEMENT_3D('',#307696,#130603,#130604);
#104692=AXIS2_PLACEMENT_3D('',#307841,#130605,#130606);
#104693=AXIS2_PLACEMENT_3D('',#307986,#130607,#130608);
#104694=AXIS2_PLACEMENT_3D('',#308843,#130629,#130630);
#104695=AXIS2_PLACEMENT_3D('',#308849,#130634,#130635);
#104696=AXIS2_PLACEMENT_3D('',#308853,#130638,#130639);
#104697=AXIS2_PLACEMENT_3D('',#308857,#130642,#130643);
#104698=AXIS2_PLACEMENT_3D('',#308859,#130645,#130646);
#104699=AXIS2_PLACEMENT_3D('',#308862,#130647,#130648);
#104700=AXIS2_PLACEMENT_3D('',#308864,#130649,#130650);
#104701=AXIS2_PLACEMENT_3D('',#308866,#130651,#130652);
#104702=AXIS2_PLACEMENT_3D('',#308868,#130653,#130654);
#104703=AXIS2_PLACEMENT_3D('',#308870,#130655,#130656);
#104704=AXIS2_PLACEMENT_3D('',#308871,#130657,#130658);
#104705=AXIS2_PLACEMENT_3D('',#308872,#130659,#130660);
#104706=AXIS2_PLACEMENT_3D('',#308880,#130661,#130662);
#104707=AXIS2_PLACEMENT_3D('',#308888,#130663,#130664);
#104708=AXIS2_PLACEMENT_3D('',#308896,#130665,#130666);
#104709=AXIS2_PLACEMENT_3D('',#308904,#130667,#130668);
#104710=AXIS2_PLACEMENT_3D('',#308912,#130669,#130670);
#104711=AXIS2_PLACEMENT_3D('',#308920,#130671,#130672);
#104712=AXIS2_PLACEMENT_3D('',#308926,#130676,#130677);
#104713=AXIS2_PLACEMENT_3D('',#308930,#130680,#130681);
#104714=AXIS2_PLACEMENT_3D('',#308934,#130684,#130685);
#104715=AXIS2_PLACEMENT_3D('',#308938,#130688,#130689);
#104716=AXIS2_PLACEMENT_3D('',#308942,#130692,#130693);
#104717=AXIS2_PLACEMENT_3D('',#308944,#130695,#130696);
#104718=AXIS2_PLACEMENT_3D('',#308945,#130697,#130698);
#104719=AXIS2_PLACEMENT_3D('',#308946,#130699,#130700);
#130441=DIRECTION('axis',(0.,0.,1.));
#130442=DIRECTION('refdir',(1.,0.,0.));
#130443=DIRECTION('center_axis',(0.,0.,1.));
#130444=DIRECTION('ref_axis',(-1.,0.,0.));
#130445=DIRECTION('',(-0.513541252058171,-6.28906650563163E-17,-0.858064905723644));
#130446=DIRECTION('center_axis',(-9.49891985197351E-13,2.74163925470746E-14,
1.));
#130447=DIRECTION('ref_axis',(0.353289074262459,-0.935514206202543,3.61145267726798E-13));
#130448=DIRECTION('center_axis',(-9.49891985197351E-13,2.74163925470746E-14,
1.));
#130449=DIRECTION('ref_axis',(0.353289074262459,-0.935514206202543,3.61145267726798E-13));
#130450=DIRECTION('center_axis',(0.,0.,1.));
#130451=DIRECTION('ref_axis',(-1.,0.,0.));
#130452=DIRECTION('',(-0.513541252058171,-6.28906650563163E-17,-0.858064905723644));
#130453=DIRECTION('center_axis',(0.,0.,-1.));
#130454=DIRECTION('ref_axis',(-1.,0.,0.));
#130455=DIRECTION('center_axis',(0.,0.,1.));
#130456=DIRECTION('ref_axis',(0.,-1.,0.));
#130457=DIRECTION('',(0.,0.,-1.));
#130458=DIRECTION('center_axis',(0.,0.,1.));
#130459=DIRECTION('ref_axis',(0.,-1.,0.));
#130460=DIRECTION('center_axis',(0.,0.,1.));
#130461=DIRECTION('ref_axis',(0.,-1.,0.));
#130462=DIRECTION('',(0.,0.,-1.));
#130463=DIRECTION('center_axis',(0.,0.,1.));
#130464=DIRECTION('ref_axis',(0.,-1.,0.));
#130465=DIRECTION('',(0.,0.,-1.));
#130466=DIRECTION('center_axis',(0.,0.,1.));
#130467=DIRECTION('ref_axis',(0.,-1.,0.));
#130468=DIRECTION('',(0.,0.,-1.));
#130469=DIRECTION('center_axis',(0.,0.,1.));
#130470=DIRECTION('ref_axis',(0.,-1.,0.));
#130471=DIRECTION('',(0.,0.,-1.));
#130472=DIRECTION('center_axis',(0.,0.,1.));
#130473=DIRECTION('ref_axis',(0.,-1.,0.));
#130474=DIRECTION('',(0.,0.,-1.));
#130475=DIRECTION('center_axis',(0.,0.,1.));
#130476=DIRECTION('ref_axis',(0.,-1.,0.));
#130477=DIRECTION('',(0.,0.,-1.));
#130478=DIRECTION('center_axis',(0.,0.,1.));
#130479=DIRECTION('ref_axis',(0.,-1.,0.));
#130480=DIRECTION('',(0.,0.,-1.));
#130481=DIRECTION('center_axis',(0.,0.,1.));
#130482=DIRECTION('ref_axis',(0.,-1.,0.));
#130483=DIRECTION('',(0.,0.,-1.));
#130484=DIRECTION('center_axis',(0.,0.,1.));
#130485=DIRECTION('ref_axis',(0.,-1.,0.));
#130486=DIRECTION('',(0.,0.,-1.));
#130487=DIRECTION('center_axis',(0.,0.,1.));
#130488=DIRECTION('ref_axis',(0.,-1.,0.));
#130489=DIRECTION('',(0.,0.,-1.));
#130490=DIRECTION('center_axis',(0.,0.,1.));
#130491=DIRECTION('ref_axis',(0.,-1.,0.));
#130492=DIRECTION('',(0.,0.,-1.));
#130493=DIRECTION('center_axis',(0.,0.,1.));
#130494=DIRECTION('ref_axis',(0.,-1.,0.));
#130495=DIRECTION('',(0.,0.,-1.));
#130496=DIRECTION('center_axis',(0.,0.,1.));
#130497=DIRECTION('ref_axis',(0.,-1.,0.));
#130498=DIRECTION('',(0.,0.,-1.));
#130499=DIRECTION('center_axis',(0.,0.,1.));
#130500=DIRECTION('ref_axis',(0.,-1.,0.));
#130501=DIRECTION('',(0.,0.,-1.));
#130502=DIRECTION('center_axis',(0.,0.,1.));
#130503=DIRECTION('ref_axis',(0.,-1.,0.));
#130504=DIRECTION('',(0.,0.,-1.));
#130505=DIRECTION('center_axis',(0.,0.,1.));
#130506=DIRECTION('ref_axis',(0.,-1.,0.));
#130507=DIRECTION('center_axis',(0.,0.,1.));
#130508=DIRECTION('ref_axis',(0.,-1.,0.));
#130509=DIRECTION('',(0.,0.,-1.));
#130510=DIRECTION('center_axis',(0.,0.,-1.));
#130511=DIRECTION('ref_axis',(-1.,0.,0.));
#130512=DIRECTION('',(0.,0.,-1.));
#130513=DIRECTION('center_axis',(0.,0.,-1.));
#130514=DIRECTION('ref_axis',(-1.,0.,0.));
#130515=DIRECTION('center_axis',(0.,0.,-1.));
#130516=DIRECTION('ref_axis',(7.84913906999881E-16,1.,0.));
#130517=DIRECTION('',(0.,0.,1.));
#130518=DIRECTION('center_axis',(0.,0.,-1.));
#130519=DIRECTION('ref_axis',(7.84913906999881E-16,1.,0.));
#130520=DIRECTION('',(0.,0.,1.));
#130521=DIRECTION('center_axis',(0.,0.,-1.));
#130522=DIRECTION('ref_axis',(7.84913906999881E-16,1.,0.));
#130523=DIRECTION('',(0.,0.,1.));
#130524=DIRECTION('center_axis',(0.,0.,-1.));
#130525=DIRECTION('ref_axis',(7.84913906999881E-16,1.,0.));
#130526=DIRECTION('',(0.,0.,1.));
#130527=DIRECTION('center_axis',(0.,0.,-1.));
#130528=DIRECTION('ref_axis',(7.84913906999881E-16,1.,0.));
#130529=DIRECTION('',(0.,0.,1.));
#130530=DIRECTION('center_axis',(0.,0.,-1.));
#130531=DIRECTION('ref_axis',(7.84913906999881E-16,1.,0.));
#130532=DIRECTION('',(0.,0.,1.));
#130533=DIRECTION('center_axis',(0.,0.,-1.));
#130534=DIRECTION('ref_axis',(7.84913906999881E-16,1.,0.));
#130535=DIRECTION('',(0.,0.,1.));
#130536=DIRECTION('center_axis',(0.,0.,-1.));
#130537=DIRECTION('ref_axis',(7.84913906999881E-16,1.,0.));
#130538=DIRECTION('',(0.,0.,1.));
#130539=DIRECTION('center_axis',(0.,0.,-1.));
#130540=DIRECTION('ref_axis',(7.84913906999881E-16,1.,0.));
#130541=DIRECTION('',(0.,0.,1.));
#130542=DIRECTION('center_axis',(0.,0.,-1.));
#130543=DIRECTION('ref_axis',(7.84913906999881E-16,1.,0.));
#130544=DIRECTION('',(0.,0.,1.));
#130545=DIRECTION('center_axis',(0.,0.,-1.));
#130546=DIRECTION('ref_axis',(7.84913906999881E-16,1.,0.));
#130547=DIRECTION('',(0.,0.,1.));
#130548=DIRECTION('center_axis',(0.,0.,-1.));
#130549=DIRECTION('ref_axis',(7.84913906999881E-16,1.,0.));
#130550=DIRECTION('',(0.,0.,1.));
#130551=DIRECTION('center_axis',(0.,0.,-1.));
#130552=DIRECTION('ref_axis',(7.84913906999881E-16,1.,0.));
#130553=DIRECTION('',(0.,0.,1.));
#130554=DIRECTION('center_axis',(0.,0.,-1.));
#130555=DIRECTION('ref_axis',(7.84913906999881E-16,1.,0.));
#130556=DIRECTION('',(0.,0.,1.));
#130557=DIRECTION('center_axis',(0.,0.,-1.));
#130558=DIRECTION('ref_axis',(7.84913906999881E-16,1.,0.));
#130559=DIRECTION('',(0.,0.,1.));
#130560=DIRECTION('center_axis',(0.,0.,-1.));
#130561=DIRECTION('ref_axis',(7.84913906999881E-16,1.,0.));
#130562=DIRECTION('',(0.,0.,1.));
#130563=DIRECTION('center_axis',(0.,0.,-1.));
#130564=DIRECTION('ref_axis',(7.84913906999881E-16,1.,0.));
#130565=DIRECTION('',(0.,0.,1.));
#130566=DIRECTION('center_axis',(0.,0.,1.));
#130567=DIRECTION('ref_axis',(7.84913906999881E-16,1.,0.));
#130568=DIRECTION('center_axis',(0.,8.12506049434301E-17,1.));
#130569=DIRECTION('ref_axis',(0.,-1.,8.12506049434301E-17));
#130570=DIRECTION('center_axis',(0.,0.,1.));
#130571=DIRECTION('ref_axis',(0.,-1.,0.));
#130572=DIRECTION('center_axis',(0.,0.,1.));
#130573=DIRECTION('ref_axis',(0.,-1.,0.));
#130574=DIRECTION('center_axis',(0.,0.,1.));
#130575=DIRECTION('ref_axis',(7.84913906999881E-16,1.,0.));
#130576=DIRECTION('',(8.659560562355E-17,-0.707106781186553,-0.707106781186542));
#130577=DIRECTION('center_axis',(0.,0.,-1.));
#130578=DIRECTION('ref_axis',(7.84913906999881E-16,1.,0.));
#130579=DIRECTION('center_axis',(0.,0.,1.));
#130580=DIRECTION('ref_axis',(1.,0.,0.));
#130581=DIRECTION('center_axis',(0.,0.,1.));
#130582=DIRECTION('ref_axis',(1.,0.,0.));
#130583=DIRECTION('center_axis',(0.,0.,1.));
#130584=DIRECTION('ref_axis',(1.,0.,0.));
#130585=DIRECTION('center_axis',(0.,0.,1.));
#130586=DIRECTION('ref_axis',(1.,0.,0.));
#130587=DIRECTION('',(0.,0.,1.));
#130588=DIRECTION('',(0.,0.,1.));
#130589=DIRECTION('',(0.,0.,1.));
#130590=DIRECTION('',(0.,0.,1.));
#130591=DIRECTION('',(0.,0.,1.));
#130592=DIRECTION('',(0.,0.,1.));
#130593=DIRECTION('',(0.,0.,1.));
#130594=DIRECTION('',(0.,0.,1.));
#130595=DIRECTION('',(0.,0.,1.));
#130596=DIRECTION('',(0.,0.,1.));
#130597=DIRECTION('',(0.,0.,1.));
#130598=DIRECTION('',(0.,0.,1.));
#130599=DIRECTION('',(0.,0.,1.));
#130600=DIRECTION('',(0.,0.,1.));
#130601=DIRECTION('',(0.,0.,1.));
#130602=DIRECTION('',(0.,0.,1.));
#130603=DIRECTION('center_axis',(0.,0.,1.));
#130604=DIRECTION('ref_axis',(1.,0.,0.));
#130605=DIRECTION('center_axis',(0.,0.,1.));
#130606=DIRECTION('ref_axis',(1.,0.,0.));
#130607=DIRECTION('center_axis',(0.,0.,1.));
#130608=DIRECTION('ref_axis',(1.,0.,0.));
#130609=DIRECTION('',(0.,-1.,0.));
#130610=DIRECTION('',(1.,0.,0.));
#130611=DIRECTION('',(0.,1.,0.));
#130612=DIRECTION('',(-1.,0.,0.));
#130613=DIRECTION('',(0.,0.,1.));
#130614=DIRECTION('',(0.,0.,1.));
#130615=DIRECTION('',(0.,0.,1.));
#130616=DIRECTION('',(0.,0.,1.));
#130617=DIRECTION('',(0.,0.,1.));
#130618=DIRECTION('',(0.,0.,1.));
#130619=DIRECTION('',(0.,0.,1.));
#130620=DIRECTION('',(0.,0.,1.));
#130621=DIRECTION('',(0.,0.,1.));
#130622=DIRECTION('',(0.,0.,1.));
#130623=DIRECTION('',(0.,0.,1.));
#130624=DIRECTION('',(0.,0.,1.));
#130625=DIRECTION('',(0.,0.,1.));
#130626=DIRECTION('',(0.,0.,1.));
#130627=DIRECTION('',(0.,0.,1.));
#130628=DIRECTION('',(0.,0.,1.));
#130629=DIRECTION('center_axis',(1.,0.,0.));
#130630=DIRECTION('ref_axis',(0.,1.,0.));
#130631=DIRECTION('',(0.,0.,1.));
#130632=DIRECTION('',(0.,0.,1.));
#130633=DIRECTION('',(0.,1.,0.));
#130634=DIRECTION('center_axis',(0.,1.,0.));
#130635=DIRECTION('ref_axis',(1.,0.,0.));
#130636=DIRECTION('',(0.,0.,1.));
#130637=DIRECTION('',(-1.,0.,0.));
#130638=DIRECTION('center_axis',(-1.,0.,0.));
#130639=DIRECTION('ref_axis',(0.,0.,1.));
#130640=DIRECTION('',(0.,0.,1.));
#130641=DIRECTION('',(0.,-1.,0.));
#130642=DIRECTION('center_axis',(0.,-1.,0.));
#130643=DIRECTION('ref_axis',(0.,0.,-1.));
#130644=DIRECTION('',(1.,0.,0.));
#130645=DIRECTION('center_axis',(0.,0.,1.));
#130646=DIRECTION('ref_axis',(1.,0.,0.));
#130647=DIRECTION('center_axis',(0.,0.,1.));
#130648=DIRECTION('ref_axis',(1.,0.,0.));
#130649=DIRECTION('center_axis',(0.,0.,1.));
#130650=DIRECTION('ref_axis',(1.,0.,0.));
#130651=DIRECTION('center_axis',(0.,0.,1.));
#130652=DIRECTION('ref_axis',(1.,0.,0.));
#130653=DIRECTION('center_axis',(0.,0.,1.));
#130654=DIRECTION('ref_axis',(1.,0.,0.));
#130655=DIRECTION('center_axis',(0.,0.,1.));
#130656=DIRECTION('ref_axis',(1.,0.,0.));
#130657=DIRECTION('center_axis',(0.,0.,1.));
#130658=DIRECTION('ref_axis',(1.,0.,0.));
#130659=DIRECTION('center_axis',(0.,0.,-1.));
#130660=DIRECTION('ref_axis',(1.,0.,0.));
#130661=DIRECTION('center_axis',(0.,0.,-1.));
#130662=DIRECTION('ref_axis',(1.,0.,0.));
#130663=DIRECTION('center_axis',(0.,0.,-1.));
#130664=DIRECTION('ref_axis',(1.,0.,0.));
#130665=DIRECTION('center_axis',(0.,0.,-1.));
#130666=DIRECTION('ref_axis',(1.,0.,0.));
#130667=DIRECTION('center_axis',(0.,0.,-1.));
#130668=DIRECTION('ref_axis',(1.,0.,0.));
#130669=DIRECTION('center_axis',(0.,0.,-1.));
#130670=DIRECTION('ref_axis',(1.,0.,0.));
#130671=DIRECTION('center_axis',(0.5,0.866025403784439,0.));
#130672=DIRECTION('ref_axis',(0.,0.,-1.));
#130673=DIRECTION('',(0.,0.,-1.));
#130674=DIRECTION('',(0.866025403784439,-0.5,0.));
#130675=DIRECTION('',(0.,0.,-1.));
#130676=DIRECTION('center_axis',(-0.5,0.866025403784439,0.));
#130677=DIRECTION('ref_axis',(0.,0.,1.));
#130678=DIRECTION('',(0.866025403784439,0.5,0.));
#130679=DIRECTION('',(0.,0.,-1.));
#130680=DIRECTION('center_axis',(-1.,0.,0.));
#130681=DIRECTION('ref_axis',(0.,0.,1.));
#130682=DIRECTION('',(0.,1.,0.));
#130683=DIRECTION('',(0.,0.,-1.));
#130684=DIRECTION('center_axis',(-0.5,-0.866025403784439,0.));
#130685=DIRECTION('ref_axis',(-0.866025403784439,0.5,0.));
#130686=DIRECTION('',(-0.866025403784439,0.5,0.));
#130687=DIRECTION('',(0.,0.,-1.));
#130688=DIRECTION('center_axis',(0.5,-0.866025403784439,0.));
#130689=DIRECTION('ref_axis',(0.,0.,-1.));
#130690=DIRECTION('',(-0.866025403784439,-0.5,0.));
#130691=DIRECTION('',(0.,0.,-1.));
#130692=DIRECTION('center_axis',(1.,1.58138378814438E-16,0.));
#130693=DIRECTION('ref_axis',(-1.58138378814438E-16,1.,0.));
#130694=DIRECTION('',(1.58138378814438E-16,-1.,0.));
#130695=DIRECTION('center_axis',(0.,0.,1.));
#130696=DIRECTION('ref_axis',(1.,0.,0.));
#130697=DIRECTION('center_axis',(0.,0.,1.));
#130698=DIRECTION('ref_axis',(0.,-1.,0.));
#130699=DIRECTION('center_axis',(0.,0.,1.));
#130700=DIRECTION('ref_axis',(-1.,0.,0.));
#303016=CARTESIAN_POINT('',(0.,0.,0.));
#303017=CARTESIAN_POINT('Origin',(0.,0.,-6.25));
#303018=CARTESIAN_POINT('',(5.37130094929936,6.75842020936191E-16,-7.30047956616129));
#303019=CARTESIAN_POINT('',(5.01311188422819,-1.51535511969235E-8,-7.89896988241093));
#303020=CARTESIAN_POINT('',(6.,7.34788079488412E-16,-6.25));
#303021=CARTESIAN_POINT('',(-1.99181552565186,-4.4367514004807,-8.14921769587173));
#303022=CARTESIAN_POINT('Ctrl Pts',(5.37130094929936,-3.33760796777938E-14,
-7.30047956616129));
#303023=CARTESIAN_POINT('Ctrl Pts',(5.35949613657535,-0.24487406843198,
-7.32020397092237));
#303024=CARTESIAN_POINT('Ctrl Pts',(5.33089609710725,-0.489174973669408,
-7.3400128720385));
#303025=CARTESIAN_POINT('Ctrl Pts',(5.17387350532135,-1.32594283703992,
-7.40831624823914));
#303026=CARTESIAN_POINT('Ctrl Pts',(4.94337733797269,-2.00208110275183,
-7.46191832542485));
#303027=CARTESIAN_POINT('Ctrl Pts',(4.135529692896,-3.22829554366765,-7.5825649977898));
#303028=CARTESIAN_POINT('Ctrl Pts',(3.65537383524051,-3.71624330385309,
-7.63934640218176));
#303029=CARTESIAN_POINT('Ctrl Pts',(2.81761097171447,-4.2876964714026,-7.72097514658463));
#303030=CARTESIAN_POINT('Ctrl Pts',(2.52798755635282,-4.44587552657713,
-7.7478249552209));
#303031=CARTESIAN_POINT('Ctrl Pts',(1.62248349050186,-4.83055343071447,
-7.83060295463442));
#303032=CARTESIAN_POINT('Ctrl Pts',(0.979093877184556,-4.96673405732115,
-7.88693356223904));
#303033=CARTESIAN_POINT('Ctrl Pts',(-0.0815626816840825,-4.98311764351839,
-7.97601494030423));
#303034=CARTESIAN_POINT('Ctrl Pts',(-0.489396493730051,-4.93962656003035,
-8.00971505568742));
#303035=CARTESIAN_POINT('Ctrl Pts',(-1.27171916279866,-4.75351932140029,
-8.07963665620959));
#303036=CARTESIAN_POINT('Ctrl Pts',(-1.64199121952478,-4.61659114940763,
-8.11447673563966));
#303037=CARTESIAN_POINT('Ctrl Pts',(-1.99181552565213,-4.43675140048056,
-8.14921769587174));
#303038=CARTESIAN_POINT('',(-8.23019658238468E-15,-4.86334165753294,-8.14921769586694));
#303039=CARTESIAN_POINT('Origin',(2.7761126730752E-12,-8.43769498715119E-14,
-8.14921769586996));
#303040=CARTESIAN_POINT('',(1.71816547201427,-4.54972521023778,-8.14921769586694));
#303041=CARTESIAN_POINT('Origin',(2.7761126730752E-12,-8.43769498715119E-14,
-8.14921769586996));
#303042=CARTESIAN_POINT('Ctrl Pts',(5.01311188460799,-1.51897319028427E-8,
-7.89896988177634));
#303043=CARTESIAN_POINT('Ctrl Pts',(5.01031248911982,-0.111425970447792,
-7.90364733023118));
#303044=CARTESIAN_POINT('Ctrl Pts',(5.00379305356662,-0.222868907769304,
-7.90833333607711));
#303045=CARTESIAN_POINT('Ctrl Pts',(4.93276471993697,-0.993412490924391,
-7.94078816013389));
#303046=CARTESIAN_POINT('Ctrl Pts',(4.74158396418353,-1.63814017417777,
-7.9670716620526));
#303047=CARTESIAN_POINT('Ctrl Pts',(4.12882368574125,-2.78526381827432,
-8.02155068727517));
#303048=CARTESIAN_POINT('Ctrl Pts',(3.72380763625359,-3.28278277037162,
-8.04890588172946));
#303049=CARTESIAN_POINT('Ctrl Pts',(3.0083686262991,-3.8791542331357,-8.08784865603926));
#303050=CARTESIAN_POINT('Ctrl Pts',(2.76324026463121,-4.04886263939069,
-8.09985312775988));
#303051=CARTESIAN_POINT('Ctrl Pts',(2.25310822001618,-4.33623890495757,
-8.12443626150599));
#303052=CARTESIAN_POINT('Ctrl Pts',(1.99012163569433,-4.45498389569414,
-8.1367741716118));
#303053=CARTESIAN_POINT('Ctrl Pts',(1.7181654720148,-4.54972521023984,-8.14921769586818));
#303054=CARTESIAN_POINT('Origin',(0.,0.,-6.25));
#303055=CARTESIAN_POINT('',(6.00000000000001,7.34788079488412E-16,-6.24999999999999));
#303056=CARTESIAN_POINT('',(5.79150250913883,-4.07985132406587E-8,-6.59837392151535));
#303057=CARTESIAN_POINT('',(6.,7.34788079488412E-16,-6.25));
#303058=CARTESIAN_POINT('',(-4.69368212308316,3.73755911357259,-6.25));
#303059=CARTESIAN_POINT('Origin',(0.,0.,-6.25));
#303060=CARTESIAN_POINT('Ctrl Pts',(-4.69368212308327,3.73755911357246,
-6.24999999999999));
#303061=CARTESIAN_POINT('Ctrl Pts',(-4.47931229413755,3.98417297990529,
-6.2735175918551));
#303062=CARTESIAN_POINT('Ctrl Pts',(-4.24517515415671,4.21288061384112,
-6.29699494886437));
#303063=CARTESIAN_POINT('Ctrl Pts',(-3.73824535882191,4.63306114584445,
-6.34373678665324));
#303064=CARTESIAN_POINT('Ctrl Pts',(-3.46311344043465,4.8254397731834,-6.36673295318495));
#303065=CARTESIAN_POINT('Ctrl Pts',(-2.61709904150763,5.31420645490152,
-6.43586741835045));
#303066=CARTESIAN_POINT('Ctrl Pts',(-2.01132344467331,5.54175028025111,
-6.4832708210197));
#303067=CARTESIAN_POINT('Ctrl Pts',(-0.709373907000955,5.79860843459997,
-6.58134608458575));
#303068=CARTESIAN_POINT('Ctrl Pts',(0.0607328538516277,5.82805956485233,
-6.63458381103649));
#303069=CARTESIAN_POINT('Ctrl Pts',(1.59056128122726,5.5230058836078,-6.75065224080422));
#303070=CARTESIAN_POINT('Ctrl Pts',(2.27675244419754,5.24082004643196,-6.80704464760716));
#303071=CARTESIAN_POINT('Ctrl Pts',(3.19418049150465,4.63517684059687,-6.8892666820807));
#303072=CARTESIAN_POINT('Ctrl Pts',(3.48108835199279,4.40384543340971,-6.91585698981735));
#303073=CARTESIAN_POINT('Ctrl Pts',(4.25543222161972,3.63818404351202,-6.99831471866209));
#303074=CARTESIAN_POINT('Ctrl Pts',(4.6639348739115,3.03582746123758,-7.05511965050512));
#303075=CARTESIAN_POINT('Ctrl Pts',(5.08174624992373,2.04992573335704,-7.13811636816271));
#303076=CARTESIAN_POINT('Ctrl Pts',(5.18876418155107,1.71225479149455,-7.16453632905808));
#303077=CARTESIAN_POINT('Ctrl Pts',(5.35674037236568,0.91751942246152,-7.22703534262863));
#303078=CARTESIAN_POINT('Ctrl Pts',(5.39336840224904,0.457757959406786,
-7.26360753911587));
#303079=CARTESIAN_POINT('Ctrl Pts',(5.37130094929936,-3.12250225675825E-14,
-7.30047956616129));
#303080=CARTESIAN_POINT('Ctrl Pts',(5.79150251002447,-4.08715098570989E-8,
-6.59837392003555));
#303081=CARTESIAN_POINT('Ctrl Pts',(5.78622620886167,-0.242624984188651,
-6.60718997399902));
#303082=CARTESIAN_POINT('Ctrl Pts',(5.76569093304197,-0.48517843769391,
-6.61602762172233));
#303083=CARTESIAN_POINT('Ctrl Pts',(5.61802685922734,-1.47764885751981,
-6.65228846746928));
#303084=CARTESIAN_POINT('Ctrl Pts',(5.35891175563966,-2.20323592534325,
-6.67825170395312));
#303085=CARTESIAN_POINT('Ctrl Pts',(4.58795209849609,-3.4778117678666,-6.73266638985813));
#303086=CARTESIAN_POINT('Ctrl Pts',(4.09682911910025,-4.02200629394887,
-6.75961746925105));
#303087=CARTESIAN_POINT('Ctrl Pts',(2.91579372493104,-4.91318919925457,
-6.81237098041607));
#303088=CARTESIAN_POINT('Ctrl Pts',(2.23615222767148,-5.23945205078007,
-6.83949358047068));
#303089=CARTESIAN_POINT('Ctrl Pts',(0.803951054870913,-5.60382767875596,
-6.89466397257435));
#303090=CARTESIAN_POINT('Ctrl Pts',(0.066616853526438,-5.64568700227111,
-6.92051793742075));
#303091=CARTESIAN_POINT('Ctrl Pts',(-1.36792175401848,-5.44358556920285,
-6.9740664250011));
#303092=CARTESIAN_POINT('Ctrl Pts',(-2.05335593367427,-5.20623554562473,
-7.0015197208454));
#303093=CARTESIAN_POINT('Ctrl Pts',(-2.98371962683623,-4.66518039986776,
-7.04169659153851));
#303094=CARTESIAN_POINT('Ctrl Pts',(-3.27649310242692,-4.45498049694096,
-7.05459359477552));
#303095=CARTESIAN_POINT('Ctrl Pts',(-4.08296464203206,-3.74583790814793,
-7.09438665629067));
#303096=CARTESIAN_POINT('Ctrl Pts',(-4.52224764583201,-3.17326931077197,
-7.1220224387253));
#303097=CARTESIAN_POINT('Ctrl Pts',(-5.15782661187924,-1.88828578285408,
-7.17665427481457));
#303098=CARTESIAN_POINT('Ctrl Pts',(-5.3478870036423,-1.18502548968262,
-7.20265852585526));
#303099=CARTESIAN_POINT('Ctrl Pts',(-5.43745663373269,0.240850696861676,
-7.25798060499546));
#303100=CARTESIAN_POINT('Ctrl Pts',(-5.3428952326372,0.948072453679164,
-7.28567732776423));
#303101=CARTESIAN_POINT('Ctrl Pts',(-5.00327031004583,1.9442091185813,-7.32503387950306));
#303102=CARTESIAN_POINT('Ctrl Pts',(-4.86200640131429,2.25567825662979,
-7.33807215464932));
#303103=CARTESIAN_POINT('Ctrl Pts',(-4.34701152607719,3.15146660065799,
-7.3784316289358));
#303104=CARTESIAN_POINT('Ctrl Pts',(-3.88973731817415,3.677372363608,-7.40595644717349));
#303105=CARTESIAN_POINT('Ctrl Pts',(-3.07248932416454,4.31314430551931,
-7.44575193906138));
#303106=CARTESIAN_POINT('Ctrl Pts',(-2.78019273290024,4.49803618553494,
-7.45875196950415));
#303107=CARTESIAN_POINT('Ctrl Pts',(-1.86812467545593,4.95520711875464,
-7.49887716589848));
#303108=CARTESIAN_POINT('Ctrl Pts',(-1.21257768598591,5.13831190723762,
-7.52617650525911));
#303109=CARTESIAN_POINT('Ctrl Pts',(-0.197987061024375,5.21976008243166,
-7.56629157595421));
#303110=CARTESIAN_POINT('Ctrl Pts',(0.14823260987749,5.21371159144093,-7.57938335761268));
#303111=CARTESIAN_POINT('Ctrl Pts',(1.14507170889072,5.09521848164692,-7.61905190624652));
#303112=CARTESIAN_POINT('Ctrl Pts',(1.77812890210808,4.8932013671744,-7.64606356122794));
#303113=CARTESIAN_POINT('Ctrl Pts',(2.94977305341439,4.25392304181889,-7.69989480814926));
#303114=CARTESIAN_POINT('Ctrl Pts',(3.47603239672043,3.81558390378902,-7.72589291549634));
#303115=CARTESIAN_POINT('Ctrl Pts',(4.36266523902092,2.70877261234113,-7.78424215387609));
#303116=CARTESIAN_POINT('Ctrl Pts',(4.65063554164098,2.09183110209941,-7.8119962939325));
#303117=CARTESIAN_POINT('Ctrl Pts',(4.95957080834306,1.02920291987346,-7.85593681680382));
#303118=CARTESIAN_POINT('Ctrl Pts',(5.02604495679351,0.514782525821281,
-7.87736029543306));
#303119=CARTESIAN_POINT('Ctrl Pts',(5.01311188460799,-1.51897246170041E-8,
-7.89896988177633));
#303120=CARTESIAN_POINT('Origin',(0.,5.28128932132296E-15,28.75));
#303121=CARTESIAN_POINT('',(-5.85847138935259E-14,6.00000000000001,-34.28125));
#303122=CARTESIAN_POINT('',(-3.80863551318268E-8,6.,-34.4999999965812));
#303123=CARTESIAN_POINT('',(-7.34788079488412E-16,6.00000000000001,28.75));
#303124=CARTESIAN_POINT('',(4.25090439081149,-4.23436085615996,-34.9375));
#303125=CARTESIAN_POINT('Ctrl Pts',(4.25090439081131,-4.23436085616012,
-34.9375));
#303126=CARTESIAN_POINT('Ctrl Pts',(4.57842694135838,-3.90555868376502,
-34.9158612474513));
#303127=CARTESIAN_POINT('Ctrl Pts',(4.8666884707777,-3.53987524186764,-34.8939034477777));
#303128=CARTESIAN_POINT('Ctrl Pts',(5.35099960474064,-2.75288783728409,
-34.8504221559952));
#303129=CARTESIAN_POINT('Ctrl Pts',(5.54624537763172,-2.33469267044124,
-34.8290396542675));
#303130=CARTESIAN_POINT('Ctrl Pts',(5.93769197870665,-1.16099003000688,
-34.7733696884182));
#303131=CARTESIAN_POINT('Ctrl Pts',(6.03802727504269,-0.38280372816298,
-34.7368155254264));
#303132=CARTESIAN_POINT('Ctrl Pts',(5.93613876085929,1.16979111500093,-34.6635444479723));
#303133=CARTESIAN_POINT('Ctrl Pts',(5.73443158550596,1.92936928850432,-34.6291555807375));
#303134=CARTESIAN_POINT('Ctrl Pts',(5.04757392259691,3.33831174457208,-34.5563097868784));
#303135=CARTESIAN_POINT('Ctrl Pts',(4.56540424651573,3.97233357802226,-34.5187280711688));
#303136=CARTESIAN_POINT('Ctrl Pts',(3.39493264467983,5.00726959792219,-34.4467466779379));
#303137=CARTESIAN_POINT('Ctrl Pts',(2.72181234083079,5.40278223269688,-34.4121222158328));
#303138=CARTESIAN_POINT('Ctrl Pts',(1.35141069093833,5.885163881108,-34.3435799039178));
#303139=CARTESIAN_POINT('Ctrl Pts',(0.677750244888653,6.00000000000002,
-34.3116693862439));
#303140=CARTESIAN_POINT('Ctrl Pts',(-1.17128529097954E-13,6.00000000000001,
-34.28125));
#303141=CARTESIAN_POINT('',(6.,-4.85064251358796E-14,-34.9375));
#303142=CARTESIAN_POINT('Origin',(0.,1.06641418988252E-16,-34.9375));
#303143=CARTESIAN_POINT('Ctrl Pts',(-3.81631717626602E-8,6.00000000000001,
-34.4999999982871));
#303144=CARTESIAN_POINT('Ctrl Pts',(0.00902402059876882,6.0000000000574,
-34.5004050240772));
#303145=CARTESIAN_POINT('Ctrl Pts',(0.0180490097901645,5.99997964170809,
-34.500810388521));
#303146=CARTESIAN_POINT('Ctrl Pts',(0.823120666418123,5.99634673739877,
-34.53699730689));
#303147=CARTESIAN_POINT('Ctrl Pts',(1.61051049598886,5.83436739183676,-34.574699832785));
#303148=CARTESIAN_POINT('Ctrl Pts',(3.05567733514661,5.22127282706155,-34.648504052116));
#303149=CARTESIAN_POINT('Ctrl Pts',(3.70291154165463,4.78406868782487,-34.6825614856431));
#303150=CARTESIAN_POINT('Ctrl Pts',(4.80280196089368,3.68073736688949,-34.7551963264752));
#303151=CARTESIAN_POINT('Ctrl Pts',(5.24218143742912,3.02230172778511,-34.7925231893462));
#303152=CARTESIAN_POINT('Ctrl Pts',(5.84452203149045,1.56954177113762,-34.8646974890673));
#303153=CARTESIAN_POINT('Ctrl Pts',(6.00000000000006,0.788620520688176,
-34.9002829014713));
#303154=CARTESIAN_POINT('Ctrl Pts',(6.,-4.91551244152788E-13,-34.9375));
#303155=CARTESIAN_POINT('Origin',(0.,5.28128932132296E-15,28.75));
#303156=CARTESIAN_POINT('',(-3.67394039744206E-16,6.00000000000001,-32.53125));
#303157=CARTESIAN_POINT('',(5.89081071343833E-14,6.00000000000001,-32.75));
#303158=CARTESIAN_POINT('',(-7.34788079488412E-16,6.00000000000001,28.75));
#303159=CARTESIAN_POINT('Ctrl Pts',(-1.17128529097954E-13,6.00000000000001,
-34.28125));
#303160=CARTESIAN_POINT('Ctrl Pts',(-0.108384071515868,6.,-34.2763854101913));
#303161=CARTESIAN_POINT('Ctrl Pts',(-0.216868918889474,5.99706326538351,
-34.2714734698916));
#303162=CARTESIAN_POINT('Ctrl Pts',(-1.10632833147993,5.94876325515211,
-34.2308475902887));
#303163=CARTESIAN_POINT('Ctrl Pts',(-1.8715220700096,5.75404967145616,-34.1936639146874));
#303164=CARTESIAN_POINT('Ctrl Pts',(-3.27732969254155,5.08520215713945,
-34.1208131866992));
#303165=CARTESIAN_POINT('Ctrl Pts',(-3.90583688862295,4.6200222074111,-34.0867962988153));
#303166=CARTESIAN_POINT('Ctrl Pts',(-4.96419389426119,3.46223757396747,
-34.0132345504217));
#303167=CARTESIAN_POINT('Ctrl Pts',(-5.37827905946631,2.77570034754371,
-33.9755364210912));
#303168=CARTESIAN_POINT('Ctrl Pts',(-5.90897846093929,1.29838225353826,
-33.9044117656504));
#303169=CARTESIAN_POINT('Ctrl Pts',(-6.02719803969626,0.524254806297659,
-33.8684909777813));
#303170=CARTESIAN_POINT('Ctrl Pts',(-5.96210557152171,-1.0308328138026,
-33.7951022595577));
#303171=CARTESIAN_POINT('Ctrl Pts',(-5.77757864786675,-1.79691869170657,
-33.7604093625649));
#303172=CARTESIAN_POINT('Ctrl Pts',(-5.12277511184992,-3.22128116433398,
-33.6878639918628));
#303173=CARTESIAN_POINT('Ctrl Pts',(-4.65649941089954,-3.86477543194963,
-33.6503615071499));
#303174=CARTESIAN_POINT('Ctrl Pts',(-3.51221800515534,-4.92568780168271,
-33.5781148393894));
#303175=CARTESIAN_POINT('Ctrl Pts',(-2.84877639424579,-5.33690318824915,
-33.5437814648957));
#303176=CARTESIAN_POINT('Ctrl Pts',(-1.38572560561628,-5.89115588770843,
-33.4700326728546));
#303177=CARTESIAN_POINT('Ctrl Pts',(-0.597716088973461,-6.02233759768107,
-33.4334029790675));
#303178=CARTESIAN_POINT('Ctrl Pts',(0.972974403763956,-5.97179825915299,
-33.3621688264213));
#303179=CARTESIAN_POINT('Ctrl Pts',(1.74062231116078,-5.79475641957087,
-33.3251327135761));
#303180=CARTESIAN_POINT('Ctrl Pts',(3.16081248404929,-5.15859730436504,
-33.2521131610558));
#303181=CARTESIAN_POINT('Ctrl Pts',(3.80062254498545,-4.70713671292783,
-33.2180408575116));
#303182=CARTESIAN_POINT('Ctrl Pts',(4.88414625852493,-3.57386905460812,
-33.1447170559047));
#303183=CARTESIAN_POINT('Ctrl Pts',(5.31280041392579,-2.89855838340594,
-33.1070434212808));
#303184=CARTESIAN_POINT('Ctrl Pts',(5.87671476476011,-1.43676814578373,
-33.0355902597443));
#303185=CARTESIAN_POINT('Ctrl Pts',(6.0129458883674,-0.666805810236944,
-33.0002183385585));
#303186=CARTESIAN_POINT('Ctrl Pts',(5.98497004399974,0.890595063639399,
-32.9267204517406));
#303187=CARTESIAN_POINT('Ctrl Pts',(5.81781237721756,1.66315413256212,-32.8916324976544));
#303188=CARTESIAN_POINT('Ctrl Pts',(5.19528344649061,3.10252795163422,-32.8194092688793));
#303189=CARTESIAN_POINT('Ctrl Pts',(4.74507858515327,3.75511045874178,-32.7820055896562));
#303190=CARTESIAN_POINT('Ctrl Pts',(3.62730635389745,4.84159283638975,-32.7095180095524));
#303191=CARTESIAN_POINT('Ctrl Pts',(2.97357104700137,5.26841834326881,-32.6753813462562));
#303192=CARTESIAN_POINT('Ctrl Pts',(1.5397809252432,5.85046892585287,-32.6025404715633));
#303193=CARTESIAN_POINT('Ctrl Pts',(0.773378841668639,6.00000000000001,
-32.565961473548));
#303194=CARTESIAN_POINT('Ctrl Pts',(0.,6.00000000000001,-32.53125));
#303195=CARTESIAN_POINT('Ctrl Pts',(1.20892879040824E-13,6.00000000000001,
-32.75));
#303196=CARTESIAN_POINT('Ctrl Pts',(0.101226978026802,6.00000000000001,
-32.7545433588053));
#303197=CARTESIAN_POINT('Ctrl Pts',(0.202542059223401,5.99743830632742,
-32.7591280299677));
#303198=CARTESIAN_POINT('Ctrl Pts',(1.0952378532439,5.95217274272906,-32.7998549153593));
#303199=CARTESIAN_POINT('Ctrl Pts',(1.87087028470847,5.75566529874471,-32.8375332700768));
#303200=CARTESIAN_POINT('Ctrl Pts',(3.28576200148526,5.07989761547696,-32.9108926375521));
#303201=CARTESIAN_POINT('Ctrl Pts',(3.91422276511424,4.61307350891332,-32.9449516172195));
#303202=CARTESIAN_POINT('Ctrl Pts',(4.96197798508461,3.46238840871191,-33.0179482233254));
#303203=CARTESIAN_POINT('Ctrl Pts',(5.36989820990069,2.7881238855527,-33.0550067747929));
#303204=CARTESIAN_POINT('Ctrl Pts',(5.9079690533841,1.31185279064064,-33.1262959336857));
#303205=CARTESIAN_POINT('Ctrl Pts',(6.02925391706431,0.522762592374781,
-33.1628294437601));
#303206=CARTESIAN_POINT('Ctrl Pts',(5.95961829588552,-1.03971876991942,
-33.2365670923304));
#303207=CARTESIAN_POINT('Ctrl Pts',(5.77614425526705,-1.79839779288808,
-33.2709368978481));
#303208=CARTESIAN_POINT('Ctrl Pts',(5.12550864735129,-3.2169944522379,-33.34314651697));
#303209=CARTESIAN_POINT('Ctrl Pts',(4.65960067010865,-3.86108944277504,
-33.3806617367387));
#303210=CARTESIAN_POINT('Ctrl Pts',(3.51084852237016,-4.92775631107311,
-33.4532521238869));
#303211=CARTESIAN_POINT('Ctrl Pts',(2.84095246385544,-5.3420796293192,-33.4878951854373));
#303212=CARTESIAN_POINT('Ctrl Pts',(1.38408388046699,-5.8895313701482,-33.5612673216253));
#303213=CARTESIAN_POINT('Ctrl Pts',(0.611551412160819,-6.01898036856992,
-33.5972750113054));
#303214=CARTESIAN_POINT('Ctrl Pts',(-0.958066353514807,-5.97602948847404,
-33.6683503518475));
#303215=CARTESIAN_POINT('Ctrl Pts',(-1.73982057618241,-5.7968743721596,
-33.7060504154366));
#303216=CARTESIAN_POINT('Ctrl Pts',(-3.170196499209,-5.15265150375837,-33.7796447302089));
#303217=CARTESIAN_POINT('Ctrl Pts',(-3.80819541469486,-4.70081017847485,
-33.8136607523942));
#303218=CARTESIAN_POINT('Ctrl Pts',(-4.88252428158932,-3.57393764912711,
-33.8864853329209));
#303219=CARTESIAN_POINT('Ctrl Pts',(-5.30645780204214,-2.90751445746667,
-33.9236887001835));
#303220=CARTESIAN_POINT('Ctrl Pts',(-5.87645223250051,-1.44478940952579,
-33.9953462086932));
#303221=CARTESIAN_POINT('Ctrl Pts',(-6.01515533592036,-0.661874546528561,
-34.0312643808833));
#303222=CARTESIAN_POINT('Ctrl Pts',(-5.98251251181234,0.898857082688321,
-34.1049194548989));
#303223=CARTESIAN_POINT('Ctrl Pts',(-5.81692267237066,1.66186808788108,
-34.1395930812488));
#303224=CARTESIAN_POINT('Ctrl Pts',(-5.19902883015015,3.09723430781878,
-34.2115347278343));
#303225=CARTESIAN_POINT('Ctrl Pts',(-4.74704361554874,3.75344008909624,
-34.2491261279251));
#303226=CARTESIAN_POINT('Ctrl Pts',(-3.62283478247836,4.84570247476016,
-34.3220129326361));
#303227=CARTESIAN_POINT('Ctrl Pts',(-2.96439897541636,5.27428539262215,
-34.3563658839136));
#303228=CARTESIAN_POINT('Ctrl Pts',(-1.52961471346436,5.85243628070298,
-34.4291945079416));
#303229=CARTESIAN_POINT('Ctrl Pts',(-0.768275485445276,5.99999999511337,
-34.4655175797308));
#303230=CARTESIAN_POINT('Ctrl Pts',(-3.81631719281739E-8,6.00000000000001,
-34.4999999982871));
#303231=CARTESIAN_POINT('Origin',(0.,5.28128932132296E-15,28.75));
#303232=CARTESIAN_POINT('',(9.41032275168811E-15,6.00000000000001,-30.78125));
#303233=CARTESIAN_POINT('',(9.97088032893578E-14,6.00000000000001,-31.));
#303234=CARTESIAN_POINT('',(-7.34788079488412E-16,6.00000000000001,28.75));
#303235=CARTESIAN_POINT('Ctrl Pts',(0.,6.00000000000001,-32.53125));
#303236=CARTESIAN_POINT('Ctrl Pts',(-0.0207690573584315,6.00000000000001,
-32.5303178247888));
#303237=CARTESIAN_POINT('Ctrl Pts',(-0.0415430061147588,5.99989216163293,
-32.5293838573947));
#303238=CARTESIAN_POINT('Ctrl Pts',(-0.841006245186672,5.99158781913607,
-32.4933805358452));
#303239=CARTESIAN_POINT('Ctrl Pts',(-1.61068386481173,5.83198141208384,
-32.4565075903841));
#303240=CARTESIAN_POINT('Ctrl Pts',(-3.044601448773,5.22823200529503,-32.3833445536335));
#303241=CARTESIAN_POINT('Ctrl Pts',(-3.69549266007054,4.79033984663976,
-32.3491337385401));
#303242=CARTESIAN_POINT('Ctrl Pts',(-4.80334021408749,3.68137854692293,
-32.2760632228768));
#303243=CARTESIAN_POINT('Ctrl Pts',(-5.24597846606345,3.01734590148864,
-32.2384322725386));
#303244=CARTESIAN_POINT('Ctrl Pts',(-5.84212141658066,1.57115192461308,
-32.166680577062));
#303245=CARTESIAN_POINT('Ctrl Pts',(-5.99586509941762,0.805312094376112,
-32.1317548182574));
#303246=CARTESIAN_POINT('Ctrl Pts',(-6.00403147863122,-0.754142683708398,
-32.0581600022407));
#303247=CARTESIAN_POINT('Ctrl Pts',(-5.85382593447647,-1.53291003267978,
-32.022604158818));
#303248=CARTESIAN_POINT('Ctrl Pts',(-5.26264945206019,-2.9863796247127,
-31.9507124484071));
#303249=CARTESIAN_POINT('Ctrl Pts',(-4.82810908500552,-3.64736325627361,
-31.9134225368205));
#303250=CARTESIAN_POINT('Ctrl Pts',(-3.73622037314246,-4.75813199432988,
-31.8407256984623));
#303251=CARTESIAN_POINT('Ctrl Pts',(-3.09188414984736,-5.19994269877488,
-31.8066901827843));
#303252=CARTESIAN_POINT('Ctrl Pts',(-1.65133577154749,-5.82286643701931,
-31.7329499111875));
#303253=CARTESIAN_POINT('Ctrl Pts',(-0.865682176198026,-5.9902742219109,
-31.695246147753));
#303254=CARTESIAN_POINT('Ctrl Pts',(0.706644344028913,-6.00868616151848,
-31.6244070900408));
#303255=CARTESIAN_POINT('Ctrl Pts',(1.47804211685083,-5.86679277977569,
-31.5879686004718));
#303256=CARTESIAN_POINT('Ctrl Pts',(2.92554908503179,-5.29601993753442,
-31.5146765411862));
#303257=CARTESIAN_POINT('Ctrl Pts',(3.58761091395686,-4.87193281549254,
-31.4802414783041));
#303258=CARTESIAN_POINT('Ctrl Pts',(4.71962558921563,-3.78773895117872,
-31.4074461995991));
#303259=CARTESIAN_POINT('Ctrl Pts',(5.17605210346062,-3.1353364702396,-31.369876810361));
#303260=CARTESIAN_POINT('Ctrl Pts',(5.80434426291947,-1.70523417590895,
-31.2978476982129));
#303261=CARTESIAN_POINT('Ctrl Pts',(5.97560654373616,-0.943589180749387,
-31.2632804815045));
#303262=CARTESIAN_POINT('Ctrl Pts',(6.01997746580024,0.617720913462348,
-31.1895981081883));
#303263=CARTESIAN_POINT('Ctrl Pts',(5.88679218178514,1.40260600427601,-31.1534935782495));
#303264=CARTESIAN_POINT('Ctrl Pts',(5.32693106100196,2.86968313364672,-31.081950998121));
#303265=CARTESIAN_POINT('Ctrl Pts',(4.90807734750157,3.53864163612625,-31.0447917430663));
#303266=CARTESIAN_POINT('Ctrl Pts',(3.84216949904923,4.67313211014774,-30.9719099038645));
#303267=CARTESIAN_POINT('Ctrl Pts',(3.20719947099793,5.12974654011133,-30.9378895610532));
#303268=CARTESIAN_POINT('Ctrl Pts',(1.78171913024569,5.78405398749862,-30.8643679073598));
#303269=CARTESIAN_POINT('Ctrl Pts',(1.00187685407056,5.96876287124623,-30.8266726650034));
#303270=CARTESIAN_POINT('Ctrl Pts',(0.139109519067466,5.99879134583971,
-30.7875112627417));
#303271=CARTESIAN_POINT('Ctrl Pts',(0.0695316236776035,6.00000000000001,
-30.7843707798636));
#303272=CARTESIAN_POINT('Ctrl Pts',(1.95554335828646E-14,6.00000000000001,
-30.78125));
#303273=CARTESIAN_POINT('Ctrl Pts',(1.95468641273067E-13,6.00000000000001,
-31.));
#303274=CARTESIAN_POINT('Ctrl Pts',(0.192480391743009,6.00000000000001,
-31.0086390752714));
#303275=CARTESIAN_POINT('Ctrl Pts',(0.385175336776876,5.99073815588791,
-31.0174228488735));
#303276=CARTESIAN_POINT('Ctrl Pts',(1.36259758706729,5.89623557832433,-31.0626705418382));
#303277=CARTESIAN_POINT('Ctrl Pts',(2.12514322937052,5.66621663354107,-31.1002502330905));
#303278=CARTESIAN_POINT('Ctrl Pts',(3.50849430626312,4.92917067266951,-31.1730876072041));
#303279=CARTESIAN_POINT('Ctrl Pts',(4.11785741159083,4.43277444959469,-31.2074840261001));
#303280=CARTESIAN_POINT('Ctrl Pts',(5.11206217936272,3.23590118583016,-31.2807586367548));
#303281=CARTESIAN_POINT('Ctrl Pts',(5.48780835773937,2.54714948329529,-31.3172932455467));
#303282=CARTESIAN_POINT('Ctrl Pts',(5.96126157266137,1.04717135230941,-31.3880812004976));
#303283=CARTESIAN_POINT('Ctrl Pts',(6.04743504137724,0.248245656005264,
-31.4257846276549));
#303284=CARTESIAN_POINT('Ctrl Pts',(5.90508288133881,-1.31491660614123,
-31.499554409699));
#303285=CARTESIAN_POINT('Ctrl Pts',(5.6864221554242,-2.06485464078017,-31.5335989449693));
#303286=CARTESIAN_POINT('Ctrl Pts',(4.97179813757506,-3.44898577482212,
-31.6062676659712));
#303287=CARTESIAN_POINT('Ctrl Pts',(4.47923637511587,-4.06826307747327,
-31.6435747080998));
#303288=CARTESIAN_POINT('Ctrl Pts',(3.28282590619554,-5.08326089637558,
-31.7155143896323));
#303289=CARTESIAN_POINT('Ctrl Pts',(2.59016248889123,-5.46878178255341,
-31.7509991027567));
#303290=CARTESIAN_POINT('Ctrl Pts',(1.10635514205171,-5.94769239519725,
-31.8245807702451));
#303291=CARTESIAN_POINT('Ctrl Pts',(0.330695573118393,-6.04066858929894,
-31.8595643450552));
#303292=CARTESIAN_POINT('Ctrl Pts',(-1.22965422233335,-5.9256236563421,
-31.9312750839606));
#303293=CARTESIAN_POINT('Ctrl Pts',(-1.99889947408283,-5.71221688244377,
-31.9689132121872));
#303294=CARTESIAN_POINT('Ctrl Pts',(-3.39816416024533,-5.00561355812641,
-32.0420208798779));
#303295=CARTESIAN_POINT('Ctrl Pts',(-4.01711344159292,-4.52398864671584,
-32.0762069469204));
#303296=CARTESIAN_POINT('Ctrl Pts',(-5.03821886158916,-3.3500802270945,
-32.149350968764));
#303297=CARTESIAN_POINT('Ctrl Pts',(-5.43013455809175,-2.66841319466599,
-32.18624819355));
#303298=CARTESIAN_POINT('Ctrl Pts',(-5.93634537132962,-1.17910038073495,
-32.2571515107645));
#303299=CARTESIAN_POINT('Ctrl Pts',(-6.04013871036333,-0.383942995801495,
-32.2943807095057));
#303300=CARTESIAN_POINT('Ctrl Pts',(-5.93344113536867,1.18006674061518,
-32.3681904861132));
#303301=CARTESIAN_POINT('Ctrl Pts',(-5.73207110480485,1.93433663116224,
-32.4023495484525));
#303302=CARTESIAN_POINT('Ctrl Pts',(-5.04881105659906,3.33564669229781,
-32.474804145282));
#303303=CARTESIAN_POINT('Ctrl Pts',(-4.56921775066433,3.9672789462146,-32.5122231613382));
#303304=CARTESIAN_POINT('Ctrl Pts',(-3.39611509864136,5.00788017065549,
-32.5844938332572));
#303305=CARTESIAN_POINT('Ctrl Pts',(-2.7146732507898,5.40768074024111,-32.6195196436924));
#303306=CARTESIAN_POINT('Ctrl Pts',(-1.33988046218305,5.88711983323846,
-32.6882161303145));
#303307=CARTESIAN_POINT('Ctrl Pts',(-0.671954625988052,6.00000000000001,
-32.7198407378522));
#303308=CARTESIAN_POINT('Ctrl Pts',(1.17267306976032E-13,6.00000000000001,
-32.75));
#303309=CARTESIAN_POINT('Origin',(0.,5.28128932132296E-15,28.75));
#303310=CARTESIAN_POINT('',(1.04704806900171E-13,6.00000000000001,-29.03125));
#303311=CARTESIAN_POINT('',(4.71640292020203E-14,6.00000000000001,-29.25));
#303312=CARTESIAN_POINT('',(-7.34788079488412E-16,6.00000000000001,28.75));
#303313=CARTESIAN_POINT('Ctrl Pts',(1.94289029309402E-14,6.00000000000001,
-30.78125));
#303314=CARTESIAN_POINT('Ctrl Pts',(-0.704864443656357,6.00000000000001,
-30.7496136502932));
#303315=CARTESIAN_POINT('Ctrl Pts',(-1.40481278019294,5.8757909125551,-30.7163865671313));
#303316=CARTESIAN_POINT('Ctrl Pts',(-2.8007074185605,5.36339161903709,-30.6462622990238));
#303317=CARTESIAN_POINT('Ctrl Pts',(-3.47430190621078,4.95370253286064,
-30.6115065138825));
#303318=CARTESIAN_POINT('Ctrl Pts',(-4.63089515695248,3.89535469290408,
-30.5390162389076));
#303319=CARTESIAN_POINT('Ctrl Pts',(-5.10122445799473,3.25522376900886,
-30.5015297221078));
#303320=CARTESIAN_POINT('Ctrl Pts',(-5.76234994545687,1.84212165447154,
-30.4292389025261));
#303321=CARTESIAN_POINT('Ctrl Pts',(-5.95156915004192,1.0848499521348,-30.3949469527781));
#303322=CARTESIAN_POINT('Ctrl Pts',(-6.03309815537622,-0.478146796057514,
-30.3211849817774));
#303323=CARTESIAN_POINT('Ctrl Pts',(-5.91742199390294,-1.26919744498096,
-30.2844367168996));
#303324=CARTESIAN_POINT('Ctrl Pts',(-5.38958939797156,-2.74971122093979,
-30.2132695741452));
#303325=CARTESIAN_POINT('Ctrl Pts',(-4.98681025949129,-3.42640040904264,
-30.1762610591455));
#303326=CARTESIAN_POINT('Ctrl Pts',(-3.94760498399162,-4.58460705526198,
-30.1032144511309));
#303327=CARTESIAN_POINT('Ctrl Pts',(-3.32220122185289,-5.05620348553668,
-30.0691236742813));
#303328=CARTESIAN_POINT('Ctrl Pts',(-1.9123128295532,-5.74194964722611,
-29.9958433509657));
#303329=CARTESIAN_POINT('Ctrl Pts',(-1.13870354070256,-5.94393308235964,
-29.958175942521));
#303330=CARTESIAN_POINT('Ctrl Pts',(0.42496937034516,-6.03483497128459,
-29.8866681386596));
#303331=CARTESIAN_POINT('Ctrl Pts',(1.19961504217379,-5.92965560982826,
-29.8513819604272));
#303332=CARTESIAN_POINT('Ctrl Pts',(2.67449347367522,-5.42778080813352,
-29.7778661539947));
#303333=CARTESIAN_POINT('Ctrl Pts',(3.35957359596598,-5.03259151514035,
-29.7427009342106));
#303334=CARTESIAN_POINT('Ctrl Pts',(4.54027172258665,-4.00026220830159,
-29.6705353893156));
#303335=CARTESIAN_POINT('Ctrl Pts',(5.02410576631555,-3.37260995383446,
-29.6331506938396));
#303336=CARTESIAN_POINT('Ctrl Pts',(5.71757164042095,-1.97682878946513,
-29.5606240875025));
#303337=CARTESIAN_POINT('Ctrl Pts',(5.92455807718776,-1.22395815615349,
-29.526511838676));
#303338=CARTESIAN_POINT('Ctrl Pts',(6.0428954553716,0.340483743180655,-29.4526816671517));
#303339=CARTESIAN_POINT('Ctrl Pts',(5.94460390403452,1.13752054552757,-29.4152180994969));
#303340=CARTESIAN_POINT('Ctrl Pts',(5.44837127419153,2.63082072784357,-29.3444393322137));
#303341=CARTESIAN_POINT('Ctrl Pts',(5.061471000005,3.31471999799366,-29.3075960048891));
#303342=CARTESIAN_POINT('Ctrl Pts',(4.04873821818579,4.49579143546424,-29.2344107512955));
#303343=CARTESIAN_POINT('Ctrl Pts',(3.43276754758097,4.98202204428083,-29.2001680226396));
#303344=CARTESIAN_POINT('Ctrl Pts',(2.03843111779232,5.69815320480461,-29.1271426017013));
#303345=CARTESIAN_POINT('Ctrl Pts',(1.27124048780868,5.9167673788676,-29.0895207495745));
#303346=CARTESIAN_POINT('Ctrl Pts',(0.322588527977472,5.99350329256427,
-29.0458234474269));
#303347=CARTESIAN_POINT('Ctrl Pts',(0.161206502432719,6.00000000000001,
-29.0384854128966));
#303348=CARTESIAN_POINT('Ctrl Pts',(1.93907390144687E-13,6.00000000000001,
-29.03125));
#303349=CARTESIAN_POINT('Ctrl Pts',(9.68669588985449E-14,6.00000000000001,
-29.25));
#303350=CARTESIAN_POINT('Ctrl Pts',(0.286651477677494,6.00000000000001,
-29.2628657452839));
#303351=CARTESIAN_POINT('Ctrl Pts',(0.573540169208329,5.97945896409856,
-29.2760416941836));
#303352=CARTESIAN_POINT('Ctrl Pts',(1.63558733452117,5.82592456515333,-29.3259484781988));
#303353=CARTESIAN_POINT('Ctrl Pts',(2.38316140859931,5.56211378691976,-29.3633489998486));
#303354=CARTESIAN_POINT('Ctrl Pts',(3.73233274900629,4.76264945459428,-29.4355625567));
#303355=CARTESIAN_POINT('Ctrl Pts',(4.32136492355195,4.2354394021771,-29.4706633366508));
#303356=CARTESIAN_POINT('Ctrl Pts',(5.25857762796228,2.99123139186498,-29.5441642606426));
#303357=CARTESIAN_POINT('Ctrl Pts',(5.60044042765665,2.28803483898915,-29.5795215543397));
#303358=CARTESIAN_POINT('Ctrl Pts',(6.0023904933203,0.773765246573121,-29.6509839613422));
#303359=CARTESIAN_POINT('Ctrl Pts',(6.05200298287115,-0.0245078164848521,
-29.6886565890019));
#303360=CARTESIAN_POINT('Ctrl Pts',(5.84051654196882,-1.57806577620796,
-29.7619731184864));
#303361=CARTESIAN_POINT('Ctrl Pts',(5.58775672103756,-2.31924417928738,
-29.7960483467769));
#303362=CARTESIAN_POINT('Ctrl Pts',(4.81182247083947,-3.66814028245793,
-29.8690724998309));
#303363=CARTESIAN_POINT('Ctrl Pts',(4.29448652728783,-4.2622013513743,-29.9061040093557));
#303364=CARTESIAN_POINT('Ctrl Pts',(3.05281519195233,-5.22554202599166,
-29.9773269364519));
#303365=CARTESIAN_POINT('Ctrl Pts',(2.33786443112479,-5.58215914785155,
-30.0139763873589));
#303366=CARTESIAN_POINT('Ctrl Pts',(0.828066686841113,-5.99269296781362,
-30.0877274173048));
#303367=CARTESIAN_POINT('Ctrl Pts',(0.0495846113847159,-6.04943122111391,
-30.122053627619));
#303368=CARTESIAN_POINT('Ctrl Pts',(-1.49956460832676,-5.86265275286791,
-30.1943077664288));
#303369=CARTESIAN_POINT('Ctrl Pts',(-2.25480486348769,-5.61562537169326,
-30.2318076105281));
#303370=CARTESIAN_POINT('Ctrl Pts',(-3.62126633277269,-4.8472531835407,
-30.3043437711416));
#303371=CARTESIAN_POINT('Ctrl Pts',(-4.22054539170578,-4.33548353481681,
-30.3390470374932));
#303372=CARTESIAN_POINT('Ctrl Pts',(-5.18642183250232,-3.11495209027315,
-30.4124391058358));
#303373=CARTESIAN_POINT('Ctrl Pts',(-5.54530022786586,-2.41896863887779,
-30.4483424403002));
#303374=CARTESIAN_POINT('Ctrl Pts',(-5.98324466608953,-0.911644430772845,
-30.5194770761562));
#303375=CARTESIAN_POINT('Ctrl Pts',(-6.05123888368179,-0.11284038478345,
-30.5571747623118));
#303376=CARTESIAN_POINT('Ctrl Pts',(-5.87451724783255,1.44577205681473,
-30.6307298262308));
#303377=CARTESIAN_POINT('Ctrl Pts',(-5.63896641315693,2.19140848180257,
-30.6647471097636));
#303378=CARTESIAN_POINT('Ctrl Pts',(-4.89387689377796,3.55831024139031,
-30.7376031061344));
#303379=CARTESIAN_POINT('Ctrl Pts',(-4.38890566872202,4.16523404545883,
-30.7747827237829));
#303380=CARTESIAN_POINT('Ctrl Pts',(-3.16995377471245,5.15483455341167,
-30.8463780244946));
#303381=CARTESIAN_POINT('Ctrl Pts',(-2.46627405518811,5.52616432810409,
-30.8823964018584));
#303382=CARTESIAN_POINT('Ctrl Pts',(-1.15469560180341,5.91637509284195,
-30.9469544002939));
#303383=CARTESIAN_POINT('Ctrl Pts',(-0.578371165749778,6.00000000000001,
-30.9740410335283));
#303384=CARTESIAN_POINT('Ctrl Pts',(1.95815585968262E-13,6.00000000000001,
-31.));
#303385=CARTESIAN_POINT('Origin',(0.,5.28128932132296E-15,28.75));
#303386=CARTESIAN_POINT('',(7.15195468047347E-14,6.00000000000001,-27.28125));
#303387=CARTESIAN_POINT('',(-6.78587090085839E-15,6.,-27.5));
#303388=CARTESIAN_POINT('',(-7.34788079488412E-16,6.00000000000001,28.75));
#303389=CARTESIAN_POINT('Ctrl Pts',(1.95815585968262E-13,6.00000000000001,
-29.03125));
#303390=CARTESIAN_POINT('Ctrl Pts',(-0.610249439421955,6.00000000000001,
-29.0038602446397));
#303391=CARTESIAN_POINT('Ctrl Pts',(-1.21786201252579,5.90690156183558,
-28.9752311538903));
#303392=CARTESIAN_POINT('Ctrl Pts',(-2.55148792189418,5.48705543591433,
-28.9092514196746));
#303393=CARTESIAN_POINT('Ctrl Pts',(-3.24760583894352,5.10596548303448,
-28.8736082177562));
#303394=CARTESIAN_POINT('Ctrl Pts',(-4.45112089716229,4.09890357032682,
-28.8017744511858));
#303395=CARTESIAN_POINT('Ctrl Pts',(-4.94760843976345,3.48347646890437,
-28.7645055106421));
#303396=CARTESIAN_POINT('Ctrl Pts',(-5.67182017599792,2.10470908298376,
-28.6917756205893));
#303397=CARTESIAN_POINT('Ctrl Pts',(-5.89578562602353,1.35611449396653,
-28.6577486475297));
#303398=CARTESIAN_POINT('Ctrl Pts',(-6.04895800130868,-0.205663265311409,
-28.5840442038559));
#303399=CARTESIAN_POINT('Ctrl Pts',(-5.96850777040572,-1.00459381990524,
-28.5463405474231));
#303400=CARTESIAN_POINT('Ctrl Pts',(-5.50622535136872,-2.50693594684814,
-28.4754410292194));
#303401=CARTESIAN_POINT('Ctrl Pts',(-5.13579504561634,-3.1979756493988,
-28.4391149504284));
#303402=CARTESIAN_POINT('Ctrl Pts',(-4.15050879706537,-4.40232478825339,
-28.3658023055152));
#303403=CARTESIAN_POINT('Ctrl Pts',(-3.54431604105256,-4.90357289469593,
-28.3313186909329));
#303404=CARTESIAN_POINT('Ctrl Pts',(-2.16625974246611,-5.65054504877781,
-28.2585742047604));
#303405=CARTESIAN_POINT('Ctrl Pts',(-1.40598363649959,-5.88596336037959,
-28.2210176360802));
#303406=CARTESIAN_POINT('Ctrl Pts',(0.147279405670193,-6.04784927531251,
-28.148941873453));
#303407=CARTESIAN_POINT('Ctrl Pts',(0.924813814001573,-5.97853548635556,
-28.1144286638591));
#303408=CARTESIAN_POINT('Ctrl Pts',(2.42568354534179,-5.54424244603929,
-28.0407318602604));
#303409=CARTESIAN_POINT('Ctrl Pts',(3.13294184602698,-5.17756195704528,
-28.0045224284731));
#303410=CARTESIAN_POINT('Ctrl Pts',(4.35914453457563,-4.19626846643179,
-27.9330431560128));
#303411=CARTESIAN_POINT('Ctrl Pts',(4.86807798850928,-3.59340439537263,
-27.895908628745));
#303412=CARTESIAN_POINT('Ctrl Pts',(5.62299595244372,-2.23217790543008,
-27.8229966795709));
#303413=CARTESIAN_POINT('Ctrl Pts',(5.86401787523608,-1.48795013782962,
-27.7889703219834));
#303414=CARTESIAN_POINT('Ctrl Pts',(6.05182027084722,0.0691006475390994,
-27.7154889567727));
#303415=CARTESIAN_POINT('Ctrl Pts',(5.98968621790758,0.867780062776776,
-27.6777971522736));
#303416=CARTESIAN_POINT('Ctrl Pts',(5.56320596227397,2.37737110688484,-27.6065555384013));
#303417=CARTESIAN_POINT('Ctrl Pts',(5.20975555576252,3.07566435592076,-27.5708363558793));
#303418=CARTESIAN_POINT('Ctrl Pts',(4.25301324905677,4.30376937191957,-27.4974085042368));
#303419=CARTESIAN_POINT('Ctrl Pts',(3.65699459682159,4.82047213605789,-27.4625879156476));
#303420=CARTESIAN_POINT('Ctrl Pts',(2.29602198104218,5.59881858726608,-27.3901526526114));
#303421=CARTESIAN_POINT('Ctrl Pts',(1.54319585172335,5.85124120675132,-27.3526824808857));
#303422=CARTESIAN_POINT('Ctrl Pts',(0.50954384865693,5.98378966357065,-27.3043561986591));
#303423=CARTESIAN_POINT('Ctrl Pts',(0.254646309755558,6.00000000000001,
-27.2926792610153));
#303424=CARTESIAN_POINT('Ctrl Pts',(1.60010893424101E-13,6.00000000000001,
-27.28125));
#303425=CARTESIAN_POINT('Ctrl Pts',(-1.17961196366423E-15,6.,-27.5));
#303426=CARTESIAN_POINT('Ctrl Pts',(0.377235656919635,6.,-27.5169314245762));
#303427=CARTESIAN_POINT('Ctrl Pts',(0.754485140073713,5.96442592083391,
-27.5343822583682));
#303428=CARTESIAN_POINT('Ctrl Pts',(1.89456069066491,5.74645700806578,-27.5887308514134));
#303429=CARTESIAN_POINT('Ctrl Pts',(2.62638182574243,5.45099215112501,-27.6258859576961));
#303430=CARTESIAN_POINT('Ctrl Pts',(3.94112457471264,4.59230934778127,-27.6974178627425));
#303431=CARTESIAN_POINT('Ctrl Pts',(4.5099125490794,4.03516302190933,-27.7335399717867));
#303432=CARTESIAN_POINT('Ctrl Pts',(5.39088733266033,2.74527874512438,-27.8072248081781));
#303433=CARTESIAN_POINT('Ctrl Pts',(5.69952008114898,2.02822455227368,-27.8417826923468));
#303434=CARTESIAN_POINT('Ctrl Pts',(6.03075325171242,0.501778354246832,
-27.9138197457337));
#303435=CARTESIAN_POINT('Ctrl Pts',(6.04443204519531,-0.294262028749672,
-27.9513870072867));
#303436=CARTESIAN_POINT('Ctrl Pts',(5.76486704792437,-1.83659373028309,
-28.0241737398078));
#303437=CARTESIAN_POINT('Ctrl Pts',(5.47800526874849,-2.56869813601061,
-28.0586168264342));
#303438=CARTESIAN_POINT('Ctrl Pts',(4.64153171368649,-3.8807184948118,-28.1319123847809));
#303439=CARTESIAN_POINT('Ctrl Pts',(4.10050931867602,-4.44852880355724,
-28.1683316905335));
#303440=CARTESIAN_POINT('Ctrl Pts',(2.81712374957459,-5.35691334710362,
-28.2391810119292));
#303441=CARTESIAN_POINT('Ctrl Pts',(2.08295367998982,-5.68277256001296,
-28.2768847961935));
#303442=CARTESIAN_POINT('Ctrl Pts',(0.551193702838028,-6.02456364307832,
-28.3506190562634));
#303443=CARTESIAN_POINT('Ctrl Pts',(-0.229808331612538,-6.04536025298797,
-28.3846529572114));
#303444=CARTESIAN_POINT('Ctrl Pts',(-1.7658615910938,-5.7875341411008,-28.457355423015));
#303445=CARTESIAN_POINT('Ctrl Pts',(-2.50570328065487,-5.5077506064569,
-28.4946418289714));
#303446=CARTESIAN_POINT('Ctrl Pts',(-3.837810688472,-4.67850656084197,-28.5665237947856));
#303447=CARTESIAN_POINT('Ctrl Pts',(-4.4167879978859,-4.13633090591235,
-28.6020942203917));
#303448=CARTESIAN_POINT('Ctrl Pts',(-5.32600147259978,-2.86925199581966,
-28.6756916728271));
#303449=CARTESIAN_POINT('Ctrl Pts',(-5.65129429890576,-2.15910805588953,
-28.7106059519222));
#303450=CARTESIAN_POINT('Ctrl Pts',(-6.0180445264865,-0.638534087601508,
-28.7823658791792));
#303451=CARTESIAN_POINT('Ctrl Pts',(-6.0497371949765,0.158824111054979,
-28.8199953319561));
#303452=CARTESIAN_POINT('Ctrl Pts',(-5.80432700148254,1.7070087594602,-28.8930582805972));
#303453=CARTESIAN_POINT('Ctrl Pts',(-5.53464382422108,2.44372552721769,
-28.9272743091343));
#303454=CARTESIAN_POINT('Ctrl Pts',(-4.72859032973606,3.77447570968008,
-29.0004411392496));
#303455=CARTESIAN_POINT('Ctrl Pts',(-4.19938443770355,4.35562977310738,
-29.0373091259254));
#303456=CARTESIAN_POINT('Ctrl Pts',(-2.93563108841771,5.29277984299625,
-29.1081446408385));
#303457=CARTESIAN_POINT('Ctrl Pts',(-2.20955995394194,5.63467162059852,
-29.1455008693368));
#303458=CARTESIAN_POINT('Ctrl Pts',(-0.966427806999832,5.94153914542989,
-29.2057713778286));
#303459=CARTESIAN_POINT('Ctrl Pts',(-0.483589923497758,6.00000000000001,
-29.2282950891166));
#303460=CARTESIAN_POINT('Ctrl Pts',(9.95037385820297E-14,6.00000000000001,
-29.25));
#303461=CARTESIAN_POINT('Origin',(0.,5.28128932132296E-15,28.75));
#303462=CARTESIAN_POINT('',(9.83277999899942E-15,6.00000000000001,-25.53125));
#303463=CARTESIAN_POINT('',(-2.77760249601778E-14,6.00000000000001,-25.75));
#303464=CARTESIAN_POINT('',(-7.34788079488412E-16,6.00000000000001,28.75));
#303465=CARTESIAN_POINT('Ctrl Pts',(1.56402668594069E-13,6.00000000000001,
-27.28125));
#303466=CARTESIAN_POINT('Ctrl Pts',(-0.515599972979865,6.00000000000001,
-27.2581083857495));
#303467=CARTESIAN_POINT('Ctrl Pts',(-1.0300826338281,5.93354318425289,-27.2340477577944));
#303468=CARTESIAN_POINT('Ctrl Pts',(-2.29679405472947,5.59933751463919,
-27.172320262185));
#303469=CARTESIAN_POINT('Ctrl Pts',(-3.01531948397537,5.24743031318486,
-27.1354527228736));
#303470=CARTESIAN_POINT('Ctrl Pts',(-4.26412494016267,4.29247762847823,
-27.0643521519629));
#303471=CARTESIAN_POINT('Ctrl Pts',(-4.78531220279368,3.70254234769101,
-27.0273713313243));
#303472=CARTESIAN_POINT('Ctrl Pts',(-5.57096178642922,2.35943764443092,
-26.9542987968875));
#303473=CARTESIAN_POINT('Ctrl Pts',(-5.82916690872251,1.61968626176987,
-26.9201872998274));
#303474=CARTESIAN_POINT('Ctrl Pts',(-6.05159797685185,0.0678141053886751,
-26.8469503278835));
#303475=CARTESIAN_POINT('Ctrl Pts',(-6.00776923179659,-0.730206667473291,
-26.8092896064688));
#303476=CARTESIAN_POINT('Ctrl Pts',(-5.61716718813836,-2.24656139245816,
-26.737728796518));
#303477=CARTESIAN_POINT('Ctrl Pts',(-5.28065340098111,-2.95200885115185,
-26.7025241271465));
#303478=CARTESIAN_POINT('Ctrl Pts',(-4.35246985184518,-4.20362012985325,
-26.6289910099454));
#303479=CARTESIAN_POINT('Ctrl Pts',(-3.76667509345661,-4.73566915601005,
-26.5937474028814));
#303480=CARTESIAN_POINT('Ctrl Pts',(-2.42298861909404,-5.54480086236121,
-26.5216390401035));
#303481=CARTESIAN_POINT('Ctrl Pts',(-1.67788280009698,-5.8138083469795,
-26.484273515561));
#303482=CARTESIAN_POINT('Ctrl Pts',(-0.1372705771751,-6.04811974682917,
-26.4117093532099));
#303483=CARTESIAN_POINT('Ctrl Pts',(0.642927897219295,-6.01541556988549,
-26.3776183515732));
#303484=CARTESIAN_POINT('Ctrl Pts',(2.16950435979991,-5.65037716134794,
-26.3037777190948));
#303485=CARTESIAN_POINT('Ctrl Pts',(2.89901934420476,-5.31309077866264,
-26.2661856841095));
#303486=CARTESIAN_POINT('Ctrl Pts',(4.16954515512449,-4.38411016073118,
-26.1954742137953));
#303487=CARTESIAN_POINT('Ctrl Pts',(4.70236067534888,-3.80699612262179,
-26.1586603459099));
#303488=CARTESIAN_POINT('Ctrl Pts',(5.51768033346227,-2.48194352687644,
-26.0854540122438));
#303489=CARTESIAN_POINT('Ctrl Pts',(5.79259576457618,-1.7466224230031,-26.051177754673));
#303490=CARTESIAN_POINT('Ctrl Pts',(6.04843928027968,-0.20017839722435,
-25.9781969506402));
#303491=CARTESIAN_POINT('Ctrl Pts',(6.02225281868307,0.596819500941055,
-25.9405845014012));
#303492=CARTESIAN_POINT('Ctrl Pts',(5.66634373735787,2.11923799365917,-25.8687375261336));
#303493=CARTESIAN_POINT('Ctrl Pts',(5.34614199354874,2.83150153213201,-25.8339416536829));
#303494=CARTESIAN_POINT('Ctrl Pts',(4.44554852974558,4.10556993485991,-25.7603164565406));
#303495=CARTESIAN_POINT('Ctrl Pts',(3.86967628599886,4.65232884939375,-25.7245857730241));
#303496=CARTESIAN_POINT('Ctrl Pts',(2.5428539596324,5.49062280133483,-25.6528090391118));
#303497=CARTESIAN_POINT('Ctrl Pts',(1.8054379564654,5.77523896294413,-25.6155610291488));
#303498=CARTESIAN_POINT('Ctrl Pts',(0.691935818399132,5.97008963046896,
-25.5627422685962));
#303499=CARTESIAN_POINT('Ctrl Pts',(0.345904466615894,6.00000000000001,
-25.5467751903674));
#303500=CARTESIAN_POINT('Ctrl Pts',(4.42701431069281E-14,6.00000000000001,
-25.53125));
#303501=CARTESIAN_POINT('Ctrl Pts',(-7.72992780895265E-14,6.00000000000001,
-25.75));
#303502=CARTESIAN_POINT('Ctrl Pts',(0.468122861239281,6.00000000000001,
-25.7710107045081));
#303503=CARTESIAN_POINT('Ctrl Pts',(0.935658867261643,5.94521908422345,
-25.7927939576161));
#303504=CARTESIAN_POINT('Ctrl Pts',(2.15006328245386,5.65535233061078,-25.8515271547163));
#303505=CARTESIAN_POINT('Ctrl Pts',(2.8648072218771,5.32904983641039,-25.888365502735));
#303506=CARTESIAN_POINT('Ctrl Pts',(4.14348544173313,4.41179809432033,-25.9591328580284));
#303507=CARTESIAN_POINT('Ctrl Pts',(4.69118642268346,3.82432388055873,-25.9966181218902));
#303508=CARTESIAN_POINT('Ctrl Pts',(5.51417090692893,2.48845339563324,-26.0704500946619));
#303509=CARTESIAN_POINT('Ctrl Pts',(5.78875318796602,1.75750763251673,-26.1045585433572));
#303510=CARTESIAN_POINT('Ctrl Pts',(6.04709949106524,0.220551590446189,
-26.1770915842196));
#303511=CARTESIAN_POINT('Ctrl Pts',(6.02406943819719,-0.571552026603184,
-26.2144730593237));
#303512=CARTESIAN_POINT('Ctrl Pts',(5.6746508052643,-2.10051584936312,-26.2866289261136));
#303513=CARTESIAN_POINT('Ctrl Pts',(5.35218037901748,-2.82276500625205,
-26.3218072890385));
#303514=CARTESIAN_POINT('Ctrl Pts',(4.45306886958014,-4.09512251548566,
-26.3953260566928));
#303515=CARTESIAN_POINT('Ctrl Pts',(3.88784123991802,-4.63513569953974,
-26.4305981980043));
#303516=CARTESIAN_POINT('Ctrl Pts',(2.56886747369248,-5.47976480362057,
-26.5021150535304));
#303517=CARTESIAN_POINT('Ctrl Pts',(1.82413919618432,-5.7705596910345,-26.5397813658791));
#303518=CARTESIAN_POINT('Ctrl Pts',(0.280280424224938,-6.04348549428708,
-26.6130543694334));
#303519=CARTESIAN_POINT('Ctrl Pts',(-0.502909218070725,-6.02904208015853,
-26.6471484862228));
#303520=CARTESIAN_POINT('Ctrl Pts',(-2.02419019540456,-5.70184808991998,
-26.7201995442795));
#303521=CARTESIAN_POINT('Ctrl Pts',(-2.74754178218265,-5.39068842638131,
-26.7572033953967));
#303522=CARTESIAN_POINT('Ctrl Pts',(-4.04426038676789,-4.50231719623974,
-26.8283592810692));
#303523=CARTESIAN_POINT('Ctrl Pts',(-4.60250180003155,-3.92988985996744,
-26.8651276125343));
#303524=CARTESIAN_POINT('Ctrl Pts',(-5.45439599366001,-2.61680010808329,
-26.9388917553293));
#303525=CARTESIAN_POINT('Ctrl Pts',(-5.74592617895212,-1.89272959036154,
-26.9731770597458));
#303526=CARTESIAN_POINT('Ctrl Pts',(-6.04059162878921,-0.360751196876833,
-27.0454751921409));
#303527=CARTESIAN_POINT('Ctrl Pts',(-6.03580606113762,0.433520368449108,
-27.0829589784866));
#303528=CARTESIAN_POINT('Ctrl Pts',(-5.72115497813815,1.96937350683204,
-27.1554399703925));
#303529=CARTESIAN_POINT('Ctrl Pts',(-5.41649047631603,2.6966028159408,-27.1902065518807));
#303530=CARTESIAN_POINT('Ctrl Pts',(-4.54866121558117,3.98888755690702,
-27.2636183915751));
#303531=CARTESIAN_POINT('Ctrl Pts',(-3.99551283052029,4.54282944451347,
-27.2994194535087));
#303532=CARTESIAN_POINT('Ctrl Pts',(-2.69416048978434,5.41952961295404,
-27.3706131116443));
#303533=CARTESIAN_POINT('Ctrl Pts',(-1.9545299925419,5.72796048538167,-27.4083078123562));
#303534=CARTESIAN_POINT('Ctrl Pts',(-0.78814350312714,5.96117321500919,
-27.4640596219032));
#303535=CARTESIAN_POINT('Ctrl Pts',(-0.394104857598537,6.00000000000001,
-27.4823114370311));
#303536=CARTESIAN_POINT('Ctrl Pts',(-3.33066907387547E-15,6.00000000000001,
-27.5));
#303537=CARTESIAN_POINT('Origin',(0.,5.28128932132296E-15,28.75));
#303538=CARTESIAN_POINT('',(-8.03487180356169E-15,6.00000000000001,-23.78125));
#303539=CARTESIAN_POINT('',(-1.19751063656468E-13,6.00000000000001,-24.));
#303540=CARTESIAN_POINT('',(-7.34788079488412E-16,6.00000000000001,28.75));
#303541=CARTESIAN_POINT('Ctrl Pts',(3.31679128606766E-14,6.00000000000001,
-25.53125));
#303542=CARTESIAN_POINT('Ctrl Pts',(-0.424871467655015,6.00000000000001,
-25.5121805428127));
#303543=CARTESIAN_POINT('Ctrl Pts',(-0.849492094009211,5.95487440164865,
-25.4924642624639));
#303544=CARTESIAN_POINT('Ctrl Pts',(-2.04357041809809,5.69697560214102,
-25.4351095583023));
#303545=CARTESIAN_POINT('Ctrl Pts',(-2.77946209252457,5.37646734180537,
-25.397406538171));
#303546=CARTESIAN_POINT('Ctrl Pts',(-4.06842357584219,4.47781098282506,
-25.3264488230175));
#303547=CARTESIAN_POINT('Ctrl Pts',(-4.61319027180827,3.91427068836823,
-25.2902295636634));
#303548=CARTESIAN_POINT('Ctrl Pts',(-5.45934039323248,2.60831583895651,
-25.2168971647068));
#303549=CARTESIAN_POINT('Ctrl Pts',(-5.75169131396413,1.87770392850516,
-25.1823638393329));
#303550=CARTESIAN_POINT('Ctrl Pts',(-6.04210854266238,0.337325462177737,
-25.109669285173));
#303551=CARTESIAN_POINT('Ctrl Pts',(-6.03414577828957,-0.458212785890218,
-25.0721257207018));
#303552=CARTESIAN_POINT('Ctrl Pts',(-5.71421415547629,-1.98642443711181,
-25.0000053508862));
#303553=CARTESIAN_POINT('Ctrl Pts',(-5.41087198181499,-2.70565746338242,
-24.9655418924847));
#303554=CARTESIAN_POINT('Ctrl Pts',(-4.53888313243973,-4.00274287099822,
-24.8918313815121));
#303555=CARTESIAN_POINT('Ctrl Pts',(-3.9733481599669,-4.56462612152847,
-24.8555178639272));
#303556=CARTESIAN_POINT('Ctrl Pts',(-2.66416049607204,-5.43255081936865,
-24.7841005094968));
#303557=CARTESIAN_POINT('Ctrl Pts',(-1.93493481390922,-5.73291475230064,
-24.7469904497704));
#303558=CARTESIAN_POINT('Ctrl Pts',(-0.408310660204593,-6.03607995383764,
-24.6740499943789));
#303559=CARTESIAN_POINT('Ctrl Pts',(0.374153358504102,-6.03829357754675,
-24.6400153658748));
#303560=CARTESIAN_POINT('Ctrl Pts',(1.9140313804275,-5.74154198020781,-24.5665735703691));
#303561=CARTESIAN_POINT('Ctrl Pts',(2.65529281663034,-5.4385950621266,-24.5288856427459));
#303562=CARTESIAN_POINT('Ctrl Pts',(3.96218395129926,-4.57186551408942,
-24.4575887924404));
#303563=CARTESIAN_POINT('Ctrl Pts',(4.51910798429228,-4.0222652428609,-24.4219625218225));
#303564=CARTESIAN_POINT('Ctrl Pts',(5.39671051287872,-2.7361803294309,-24.3485162873228));
#303565=CARTESIAN_POINT('Ctrl Pts',(5.70693322891675,-2.01049405427323,
-24.3136305583248));
#303566=CARTESIAN_POINT('Ctrl Pts',(6.03247247102471,-0.476747960636583,
-24.241249003461));
#303567=CARTESIAN_POINT('Ctrl Pts',(6.04297780476799,0.316889074752779,
-24.2037951622696));
#303568=CARTESIAN_POINT('Ctrl Pts',(5.75967743453439,1.85048055115758,-24.1314209042039));
#303569=CARTESIAN_POINT('Ctrl Pts',(5.47345416616638,2.57671226734841,-24.0972009530275));
#303570=CARTESIAN_POINT('Ctrl Pts',(4.63060265135997,3.89695887401926,-24.0234144001431));
#303571=CARTESIAN_POINT('Ctrl Pts',(4.07565211473755,4.47410856406866,-23.9864296082687));
#303572=CARTESIAN_POINT('Ctrl Pts',(2.78456422924563,5.37158127780049,-23.9153937155443));
#303573=CARTESIAN_POINT('Ctrl Pts',(2.06388598663886,5.6875268386056,-23.8784400574907));
#303574=CARTESIAN_POINT('Ctrl Pts',(0.874224439928393,5.95220036785164,
-23.8211847928979));
#303575=CARTESIAN_POINT('Ctrl Pts',(0.437278592210077,6.00000000000001,
-23.8008763247309));
#303576=CARTESIAN_POINT('Ctrl Pts',(-4.16333634234434E-15,6.00000000000001,
-23.78125));
#303577=CARTESIAN_POINT('Ctrl Pts',(-2.38281616660174E-13,6.,-24.));
#303578=CARTESIAN_POINT('Ctrl Pts',(0.562550298860549,6.00000000000002,
-24.0252488803239));
#303579=CARTESIAN_POINT('Ctrl Pts',(1.1233551042289,5.92088791056928,-24.0515731358351));
#303580=CARTESIAN_POINT('Ctrl Pts',(2.41071026870567,5.54884547697468,-24.1147789683531));
#303581=CARTESIAN_POINT('Ctrl Pts',(3.10683165180809,5.19121363532752,-24.1504820805078));
#303582=CARTESIAN_POINT('Ctrl Pts',(4.33846198761852,4.2198397478983,-24.2217331841809));
#303583=CARTESIAN_POINT('Ctrl Pts',(4.85774809512149,3.60991749279142,-24.259424364326));
#303584=CARTESIAN_POINT('Ctrl Pts',(5.62013568794327,2.23937998964814,-24.3328990059842));
#303585=CARTESIAN_POINT('Ctrl Pts',(5.86211841709987,1.49543160766457,-24.3669266075694));
#303586=CARTESIAN_POINT('Ctrl Pts',(6.05047063792894,-0.0496575713316277,
-24.4398434727813));
#303587=CARTESIAN_POINT('Ctrl Pts',(5.99258710491169,-0.836440604727685,
-24.4769738554007));
#303588=CARTESIAN_POINT('Ctrl Pts',(5.57639177404937,-2.35084427814086,
-24.5484425900419));
#303589=CARTESIAN_POINT('Ctrl Pts',(5.21923032242104,-3.06306108589369,
-24.5846696335685));
#303590=CARTESIAN_POINT('Ctrl Pts',(4.25938687942677,-4.29601921088136,
-24.6583687981531));
#303591=CARTESIAN_POINT('Ctrl Pts',(3.67074897074401,-4.80871760926913,
-24.6928733281883));
#303592=CARTESIAN_POINT('Ctrl Pts',(2.31850296533907,-5.58979575758995,
-24.7649567530249));
#303593=CARTESIAN_POINT('Ctrl Pts',(1.56493274222149,-5.84570310131582,
-24.8025111407221));
#303594=CARTESIAN_POINT('Ctrl Pts',(0.0108649931927007,-6.05038621000914,
-24.875247146657));
#303595=CARTESIAN_POINT('Ctrl Pts',(-0.774206948697535,-6.00065650544021,
-24.9097390673429));
#303596=CARTESIAN_POINT('Ctrl Pts',(-2.27896334720533,-5.60443537022234,
-24.983055100494));
#303597=CARTESIAN_POINT('Ctrl Pts',(-2.98456358044658,-5.26265704441739,
-25.0193627830976));
#303598=CARTESIAN_POINT('Ctrl Pts',(-4.24091987830039,-4.31819521272542,
-25.0902722707001));
#303599=CARTESIAN_POINT('Ctrl Pts',(-4.77518588066601,-3.71883157954491,
-25.1279758557517));
#303600=CARTESIAN_POINT('Ctrl Pts',(-5.56839113636215,-2.36482273658844,
-25.2016742944687));
#303601=CARTESIAN_POINT('Ctrl Pts',(-5.82675235100875,-1.62736996328308,
-25.2357000858749));
#303602=CARTESIAN_POINT('Ctrl Pts',(-6.05028457959359,-0.0861277442399659,
-25.3084354028214));
#303603=CARTESIAN_POINT('Ctrl Pts',(-6.00986496171919,0.703516433178524,
-25.3457008104321));
#303604=CARTESIAN_POINT('Ctrl Pts',(-5.62719500215083,2.22544989670628,
-25.417524895883));
#303605=CARTESIAN_POINT('Ctrl Pts',(-5.28753359193716,2.94278461795138,
-25.4531828441067));
#303606=CARTESIAN_POINT('Ctrl Pts',(-4.35829222660762,4.19571637994054,
-25.5267957198342));
#303607=CARTESIAN_POINT('Ctrl Pts',(-3.78144475897279,4.72222451038447,
-25.5616436241724));
#303608=CARTESIAN_POINT('Ctrl Pts',(-2.44580348839665,5.53553560979869,
-25.6334518444767));
#303609=CARTESIAN_POINT('Ctrl Pts',(-1.69651006241038,5.8091243938572,-25.6710721315185));
#303610=CARTESIAN_POINT('Ctrl Pts',(-0.612088581728065,5.97660254263791,
-25.7221864857074));
#303611=CARTESIAN_POINT('Ctrl Pts',(-0.305934362215538,6.,-25.7362687832285));
#303612=CARTESIAN_POINT('Ctrl Pts',(-8.5417783957098E-14,6.,-25.75));
#303613=CARTESIAN_POINT('Origin',(0.,5.28128932132296E-15,28.75));
#303614=CARTESIAN_POINT('',(-7.12481952681565E-14,6.00000000000001,-22.03125));
#303615=CARTESIAN_POINT('',(-9.35567391692183E-14,6.00000000000001,-22.25));
#303616=CARTESIAN_POINT('',(-7.34788079488412E-16,6.00000000000001,28.75));
#303617=CARTESIAN_POINT('Ctrl Pts',(-2.4980018054066E-15,6.00000000000001,
-23.78125));
#303618=CARTESIAN_POINT('Ctrl Pts',(-0.335678938243623,6.00000000000001,
-23.7661837608457));
#303619=CARTESIAN_POINT('Ctrl Pts',(-0.671516877978854,5.97183185980311,
-23.7506995998679));
#303620=CARTESIAN_POINT('Ctrl Pts',(-1.78399880945041,5.78301956731754,
-23.6980146887665));
#303621=CARTESIAN_POINT('Ctrl Pts',(-2.53020766877619,5.49764207970405,
-23.6603609273815));
#303622=CARTESIAN_POINT('Ctrl Pts',(-3.8544843350439,4.66286957682803,-23.588749804504));
#303623=CARTESIAN_POINT('Ctrl Pts',(-4.42338717316591,4.12711664154783,
-23.5536209266038));
#303624=CARTESIAN_POINT('Ctrl Pts',(-5.33202476696476,2.86087582747025,
-23.4800714468375));
#303625=CARTESIAN_POINT('Ctrl Pts',(-5.65992614642843,2.14016759121118,
-23.4447501972058));
#303626=CARTESIAN_POINT('Ctrl Pts',(-6.0198832742675,0.613385006056967,
-23.3726972688164));
#303627=CARTESIAN_POINT('Ctrl Pts',(-6.04843144717586,-0.17797995869111,
-23.3353506526777));
#303628=CARTESIAN_POINT('Ctrl Pts',(-5.80111053815611,-1.71634487147645,
-23.2627511234614));
#303629=CARTESIAN_POINT('Ctrl Pts',(-5.53166742647866,-2.44936002522379,
-23.2286780048958));
#303630=CARTESIAN_POINT('Ctrl Pts',(-4.71759406830737,-3.79188557378601,
-23.1548391310901));
#303631=CARTESIAN_POINT('Ctrl Pts',(-4.17324741617074,-4.38385846244696,
-23.1171380935287));
#303632=CARTESIAN_POINT('Ctrl Pts',(-2.90022435542836,-5.3097653973734,
-23.0464747038104));
#303633=CARTESIAN_POINT('Ctrl Pts',(-2.18817042753906,-5.6406633513231,
-23.0097017276048));
#303634=CARTESIAN_POINT('Ctrl Pts',(-0.677268637078028,-6.01220148828043,
-22.9364698319252));
#303635=CARTESIAN_POINT('Ctrl Pts',(0.107166082282369,-6.04928022076788,
-22.9021587469481));
#303636=CARTESIAN_POINT('Ctrl Pts',(1.65778944458732,-5.82022117327913,
-22.8292218525854));
#303637=CARTESIAN_POINT('Ctrl Pts',(2.40838629926702,-5.55184163046472,
-22.7916190320049));
#303638=CARTESIAN_POINT('Ctrl Pts',(3.74897402294149,-4.74802073922283,
-22.7197271994846));
#303639=CARTESIAN_POINT('Ctrl Pts',(4.32931016190671,-4.22558757161908,
-22.6849901296395));
#303640=CARTESIAN_POINT('Ctrl Pts',(5.26760358278042,-2.97853795055449,
-22.6113507357543));
#303641=CARTESIAN_POINT('Ctrl Pts',(5.61243739670297,-2.26270345189369,
-22.5755329901724));
#303642=CARTESIAN_POINT('Ctrl Pts',(6.00505048721559,-0.742956757380043,
-22.5038121041637));
#303643=CARTESIAN_POINT('Ctrl Pts',(6.05065732510423,0.0458787591654085,
-22.466584859409));
#303644=CARTESIAN_POINT('Ctrl Pts',(5.83755064987419,1.58831186705197,-22.3937933412526));
#303645=CARTESIAN_POINT('Ctrl Pts',(5.58404404604623,2.32769785635364,-22.3597759082447));
#303646=CARTESIAN_POINT('Ctrl Pts',(4.79997695723648,3.68666091872496,-22.2861418040706));
#303647=CARTESIAN_POINT('Ctrl Pts',(4.27014167758665,4.28919961095268,-22.2484399008116));
#303648=CARTESIAN_POINT('Ctrl Pts',(3.02110325597171,5.24170194126841,-22.1774264213415));
#303649=CARTESIAN_POINT('Ctrl Pts',(2.31832001262212,5.58820722058684,-22.141308201694));
#303650=CARTESIAN_POINT('Ctrl Pts',(1.05648178820591,5.9300776639719,-22.0796876512508));
#303651=CARTESIAN_POINT('Ctrl Pts',(0.528871597020288,6.00000000000002,
-22.054987283025));
#303652=CARTESIAN_POINT('Ctrl Pts',(-1.62925228863742E-13,6.00000000000001,
-22.03125));
#303653=CARTESIAN_POINT('Ctrl Pts',(-1.95399252334028E-13,6.00000000000001,
-22.25));
#303654=CARTESIAN_POINT('Ctrl Pts',(0.656191862353245,6.00000000000003,
-22.2794517838416));
#303655=CARTESIAN_POINT('Ctrl Pts',(1.3088204429588,5.89235411864679,-22.3103134730883));
#303656=CARTESIAN_POINT('Ctrl Pts',(2.66420982212309,5.43144549898009,-22.3778688426481));
#303657=CARTESIAN_POINT('Ctrl Pts',(3.34166154948581,5.04300495159892,-22.4126546193864));
#303658=CARTESIAN_POINT('Ctrl Pts',(4.52376996083162,4.0198446987934,-22.4845092129917));
#303659=CARTESIAN_POINT('Ctrl Pts',(5.01300408269997,3.39019222799627,-22.5221200696207));
#303660=CARTESIAN_POINT('Ctrl Pts',(5.71415884595264,1.98829432878365,-22.5950934940657));
#303661=CARTESIAN_POINT('Ctrl Pts',(5.92350949341426,1.2316432847712,-22.6293754796774));
#303662=CARTESIAN_POINT('Ctrl Pts',(6.04178496665432,-0.319651749022043,
-22.7025852156724));
#303663=CARTESIAN_POINT('Ctrl Pts',(5.94947753572463,-1.09962436224066,
-22.7393941964615));
#303664=CARTESIAN_POINT('Ctrl Pts',(5.46672872976866,-2.5977463093425,-22.8100945531612));
#303665=CARTESIAN_POINT('Ctrl Pts',(5.07430203729619,-3.29926283752869,
-22.8477079238963));
#303666=CARTESIAN_POINT('Ctrl Pts',(4.05298994766479,-4.49131097267786,
-22.9215502467933));
#303667=CARTESIAN_POINT('Ctrl Pts',(3.44069211491054,-4.97596767892926,
-22.9556380070889));
#303668=CARTESIAN_POINT('Ctrl Pts',(2.05614934249828,-5.69103060964564,
-23.0282082820789));
#303669=CARTESIAN_POINT('Ctrl Pts',(1.29513526144091,-5.91085755822875,
-23.0655705991662));
#303670=CARTESIAN_POINT('Ctrl Pts',(-0.267634289993002,-6.04507160849594,
-23.1376694933283));
#303671=CARTESIAN_POINT('Ctrl Pts',(-1.05430233439035,-5.9584376020307,
-23.1729262486461));
#303672=CARTESIAN_POINT('Ctrl Pts',(-2.54063295535784,-5.49042836134954,
-23.2464621896157));
#303673=CARTESIAN_POINT('Ctrl Pts',(-3.22726175325772,-5.11706468944888,
-23.281653690679));
#303674=CARTESIAN_POINT('Ctrl Pts',(-4.43384493330011,-4.11915413759816,
-23.3532231684686));
#303675=CARTESIAN_POINT('Ctrl Pts',(-4.93793618465934,-3.49902022137446,
-23.3908827340176));
#303676=CARTESIAN_POINT('Ctrl Pts',(-5.66927354555103,-2.11233708108698,
-23.464112503659));
#303677=CARTESIAN_POINT('Ctrl Pts',(-5.89472741732509,-1.36191398326544,
-23.4982276591553));
#303678=CARTESIAN_POINT('Ctrl Pts',(-6.04757394140331,0.186562965779997,
-23.5713044022405));
#303679=CARTESIAN_POINT('Ctrl Pts',(-5.97218525221358,0.970078970704557,
-23.6082806051026));
#303680=CARTESIAN_POINT('Ctrl Pts',(-5.52223138513339,2.47644746769361,
-23.6793701384108));
#303681=CARTESIAN_POINT('Ctrl Pts',(-5.1472713583218,3.18333137095973,-23.7162575928246));
#303682=CARTESIAN_POINT('Ctrl Pts',(-4.15637220130421,4.39575702607239,
-23.7900342937022));
#303683=CARTESIAN_POINT('Ctrl Pts',(-3.55577783328524,4.89434051268096,
-23.8242822318611));
#303684=CARTESIAN_POINT('Ctrl Pts',(-2.18703255785244,5.64227648233448,
-23.8966228680967));
#303685=CARTESIAN_POINT('Ctrl Pts',(-1.42950610207241,5.88004402157154,
-23.9340902841137));
#303686=CARTESIAN_POINT('Ctrl Pts',(-0.432193866804079,5.98833909651615,
-23.9804318375719));
#303687=CARTESIAN_POINT('Ctrl Pts',(-0.215975941419464,6.,-23.9903063766764));
#303688=CARTESIAN_POINT('Ctrl Pts',(-2.333550019884E-13,6.00000000000001,
-24.));
#303689=CARTESIAN_POINT('Origin',(0.,5.28128932132296E-15,28.75));
#303690=CARTESIAN_POINT('',(-9.03475007386612E-14,6.00000000000001,-20.28125));
#303691=CARTESIAN_POINT('',(-1.94920572052551E-14,6.00000000000001,-20.5));
#303692=CARTESIAN_POINT('',(-7.34788079488412E-16,6.00000000000001,28.75));
#303693=CARTESIAN_POINT('Ctrl Pts',(-1.57304724801577E-13,6.00000000000001,
-22.03125));
#303694=CARTESIAN_POINT('Ctrl Pts',(-0.247873021895561,6.,-22.0201247436842));
#303695=CARTESIAN_POINT('Ctrl Pts',(-0.496002946576206,5.98464052621168,
-22.0087639645042));
#303696=CARTESIAN_POINT('Ctrl Pts',(-1.52456266669614,5.85628831960672,
-21.9607274339426));
#303697=CARTESIAN_POINT('Ctrl Pts',(-2.27935912362775,5.6057945493989,-21.9231969572814));
#303698=CARTESIAN_POINT('Ctrl Pts',(-3.63658527559146,4.83459846183184,
-21.851034122486));
#303699=CARTESIAN_POINT('Ctrl Pts',(-4.22880540848471,4.32611718065054,
-21.8166162324363));
#303700=CARTESIAN_POINT('Ctrl Pts',(-5.19795128892809,3.09928099276133,
-21.7428927596501));
#303701=CARTESIAN_POINT('Ctrl Pts',(-5.56044007690697,2.38864648574926,
-21.7064765766973));
#303702=CARTESIAN_POINT('Ctrl Pts',(-5.9867757063381,0.8766083832202,-21.6351194796338));
#303703=CARTESIAN_POINT('Ctrl Pts',(-6.0499263152208,0.0907660482333399,
-21.5980334910728));
#303704=CARTESIAN_POINT('Ctrl Pts',(-5.87223060423317,-1.455392310674,-21.525066168419));
#303705=CARTESIAN_POINT('Ctrl Pts',(-5.63520842710562,-2.20129232723029,
-21.4910212850226));
#303706=CARTESIAN_POINT('Ctrl Pts',(-4.8821456275804,-3.57673174904142,
-21.4176181515899));
#303707=CARTESIAN_POINT('Ctrl Pts',(-4.36741253731134,-4.18976557690947,
-21.3799344694682));
#303708=CARTESIAN_POINT('Ctrl Pts',(-3.14329011578986,-5.16916925119684,
-21.3085850543928));
#303709=CARTESIAN_POINT('Ctrl Pts',(-2.45002533896817,-5.53155019941288,
-21.2730457649249));
#303710=CARTESIAN_POINT('Ctrl Pts',(-0.957187551194655,-5.97457647883464,
-21.199582098388));
#303711=CARTESIAN_POINT('Ctrl Pts',(-0.171029298425594,-6.04834889542311,
-21.1646313763769));
#303712=CARTESIAN_POINT('Ctrl Pts',(1.38893230643956,-5.88968803969353,
-21.0923019950446));
#303713=CARTESIAN_POINT('Ctrl Pts',(2.14755740121632,-5.65734375361809,
-21.0548643580485));
#303714=CARTESIAN_POINT('Ctrl Pts',(3.52113213764988,-4.91933400793448,
-20.9824517191035));
#303715=CARTESIAN_POINT('Ctrl Pts',(4.12527633807941,-4.42496301159265,
-20.9482619411319));
#303716=CARTESIAN_POINT('Ctrl Pts',(5.12539903961644,-3.21868849573097,
-20.8744642354037));
#303717=CARTESIAN_POINT('Ctrl Pts',(5.50565256972684,-2.51341682920263,
-20.8373648208451));
#303718=CARTESIAN_POINT('Ctrl Pts',(5.96558036928433,-1.00951013376385,
-20.7663914664955));
#303719=CARTESIAN_POINT('Ctrl Pts',(6.04612404274221,-0.227033301870451,
-20.729464304971));
#303720=CARTESIAN_POINT('Ctrl Pts',(5.90378336153341,1.32235028147315,-20.6563447754034));
#303721=CARTESIAN_POINT('Ctrl Pts',(5.68322161727553,2.07467398036568,-20.6221873757411));
#303722=CARTESIAN_POINT('Ctrl Pts',(4.96442531708872,3.45955244748875,-20.5493743862554));
#303723=CARTESIAN_POINT('Ctrl Pts',(4.47065980115618,4.07765474955389,-20.5120788141737));
#303724=CARTESIAN_POINT('Ctrl Pts',(3.27207338608969,5.09022865022444,-20.4401713181278));
#303725=CARTESIAN_POINT('Ctrl Pts',(2.57835365451257,5.47439645533847,-20.4046390020441));
#303726=CARTESIAN_POINT('Ctrl Pts',(1.23785258780516,5.90379474609851,-20.3382113885289));
#303727=CARTESIAN_POINT('Ctrl Pts',(0.62034706770823,6.00000000000002,-20.3090929660486));
#303728=CARTESIAN_POINT('Ctrl Pts',(-1.47798440153224E-13,6.00000000000001,
-20.28125));
#303729=CARTESIAN_POINT('Ctrl Pts',(-3.76088049591772E-14,6.00000000000001,
-20.5));
#303730=CARTESIAN_POINT('Ctrl Pts',(0.751667244622775,6.00000000000001,
-20.5337369944364));
#303731=CARTESIAN_POINT('Ctrl Pts',(1.49709646348268,5.85874691471607,-20.5692539491075));
#303732=CARTESIAN_POINT('Ctrl Pts',(2.91697016964531,5.29994718308846,-20.6411311400109));
#303733=CARTESIAN_POINT('Ctrl Pts',(3.57513286629982,4.88022499191249,-20.6753457987847));
#303734=CARTESIAN_POINT('Ctrl Pts',(4.7050259366176,3.80534525963323,-20.7477266155594));
#303735=CARTESIAN_POINT('Ctrl Pts',(5.16257605915517,3.15685666003015,-20.7851777420668));
#303736=CARTESIAN_POINT('Ctrl Pts',(5.79984105333037,1.72427323992447,-20.8575504815529));
#303737=CARTESIAN_POINT('Ctrl Pts',(5.97493881429629,0.954659623675638,
-20.8924470748686));
#303738=CARTESIAN_POINT('Ctrl Pts',(6.01987134289518,-0.601709779497567,
-20.9658962838423));
#303739=CARTESIAN_POINT('Ctrl Pts',(5.89186530074486,-1.37358364193026,
-21.0015076337564));
#303740=CARTESIAN_POINT('Ctrl Pts',(5.34311178807529,-2.84252935860833,
-21.0728134403276));
#303741=CARTESIAN_POINT('Ctrl Pts',(4.92108859791892,-3.5230141412278,-21.1105006834493));
#303742=CARTESIAN_POINT('Ctrl Pts',(3.84903999758734,-4.66753875550232,
-21.1839359619654));
#303743=CARTESIAN_POINT('Ctrl Pts',(3.21440337745087,-5.12529377974754,
-21.217972170754));
#303744=CARTESIAN_POINT('Ctrl Pts',(1.8007497746658,-5.77646175250193,-21.2909172223232));
#303745=CARTESIAN_POINT('Ctrl Pts',(1.0341775543896,-5.96160739771503,-21.3280232357259));
#303746=CARTESIAN_POINT('Ctrl Pts',(-0.535211348682595,-6.02801740479988,
-21.3994304165227));
#303747=CARTESIAN_POINT('Ctrl Pts',(-1.32301831633981,-5.9053511948978,
-21.43576117391));
#303748=CARTESIAN_POINT('Ctrl Pts',(-2.79061117887403,-5.36755070584623,
-21.509473899263));
#303749=CARTESIAN_POINT('Ctrl Pts',(-3.45851012257618,-4.96354983867725,
-21.5439294686769));
#303750=CARTESIAN_POINT('Ctrl Pts',(-4.61488432690181,-3.91454190531348,
-21.6160570730109));
#303751=CARTESIAN_POINT('Ctrl Pts',(-5.08849735367067,-3.27535965659795,
-21.6535984574679));
#303752=CARTESIAN_POINT('Ctrl Pts',(-5.75808020596784,-1.85804308932178,
-21.7262847835302));
#303753=CARTESIAN_POINT('Ctrl Pts',(-5.95053647815811,-1.09494819472666,
-21.7608264843129));
#303754=CARTESIAN_POINT('Ctrl Pts',(-6.03260156551894,0.459014061554021,
-21.8341620936266));
#303755=CARTESIAN_POINT('Ctrl Pts',(-5.9226277498516,1.23502253689428,-21.8703640934126));
#303756=CARTESIAN_POINT('Ctrl Pts',(-5.40715008322945,2.71927554296194,
-21.9413312834925));
#303757=CARTESIAN_POINT('Ctrl Pts',(-4.99979132457304,3.41082384765497,
-21.9790341493098));
#303758=CARTESIAN_POINT('Ctrl Pts',(-3.95300016548896,4.57966689906188,
-22.0526972776334));
#303759=CARTESIAN_POINT('Ctrl Pts',(-3.3296347280991,5.05104938957677,-22.086717524614));
#303760=CARTESIAN_POINT('Ctrl Pts',(-1.93049251833636,5.73464181947698,
-22.1594841196669));
#303761=CARTESIAN_POINT('Ctrl Pts',(-1.16654129184404,5.93735242962764,
-22.1967286510459));
#303762=CARTESIAN_POINT('Ctrl Pts',(-0.256820521077725,5.99588198305167,
-22.2384130996943));
#303763=CARTESIAN_POINT('Ctrl Pts',(-0.128344782741232,6.,-22.2442395158865));
#303764=CARTESIAN_POINT('Ctrl Pts',(-1.91166527052644E-13,6.00000000000001,
-22.25));
#303765=CARTESIAN_POINT('Origin',(0.,5.28128932132296E-15,28.75));
#303766=CARTESIAN_POINT('',(-3.9716265690857E-14,6.00000000000001,-18.53125));
#303767=CARTESIAN_POINT('',(-3.67394039744206E-16,6.00000000000001,-18.75));
#303768=CARTESIAN_POINT('',(-7.34788079488412E-16,6.00000000000001,28.75));
#303769=CARTESIAN_POINT('Ctrl Pts',(-1.47763745683704E-13,6.00000000000001,
-20.28125));
#303770=CARTESIAN_POINT('Ctrl Pts',(-0.151341421450277,6.,-20.2744573603978));
#303771=CARTESIAN_POINT('Ctrl Pts',(-0.302844493584432,5.99427408416176,
-20.2675739625073));
#303772=CARTESIAN_POINT('Ctrl Pts',(-1.24236034038075,5.92295011427716,
-20.2243656396503));
#303773=CARTESIAN_POINT('Ctrl Pts',(-2.01098178465626,5.70795123698633,
-20.1867322915282));
#303774=CARTESIAN_POINT('Ctrl Pts',(-3.40874545772043,4.99843626968568,
-20.1136495321756));
#303775=CARTESIAN_POINT('Ctrl Pts',(-4.02678653947944,4.5154055432828,-20.079447029591));
#303776=CARTESIAN_POINT('Ctrl Pts',(-5.04534034063016,3.33930747050941,
-20.0062901872633));
#303777=CARTESIAN_POINT('Ctrl Pts',(-5.43572687334624,2.65695546252764,
-19.9694092280431));
#303778=CARTESIAN_POINT('Ctrl Pts',(-5.93889519613326,1.16642195364104,
-19.8985437012015));
#303779=CARTESIAN_POINT('Ctrl Pts',(-6.04101219096814,0.370690431713295,
-19.8612438667696));
#303780=CARTESIAN_POINT('Ctrl Pts',(-5.93076718624805,-1.19345347347955,
-19.7874277583809));
#303781=CARTESIAN_POINT('Ctrl Pts',(-5.7276852635711,-1.94729765908645,
-19.7532839443771));
#303782=CARTESIAN_POINT('Ctrl Pts',(-5.04131269253674,-3.34692773546802,
-19.6808071500655));
#303783=CARTESIAN_POINT('Ctrl Pts',(-4.56042397818458,-3.97735030277139,
-19.6433983859095));
#303784=CARTESIAN_POINT('Ctrl Pts',(-3.38500376937153,-5.01543481853053,
-19.5711595140265));
#303785=CARTESIAN_POINT('Ctrl Pts',(-2.70245368343677,-5.4138325992579,
-19.5360921922617));
#303786=CARTESIAN_POINT('Ctrl Pts',(-1.23056392229115,-5.92333804168213,
-19.4625992457995));
#303787=CARTESIAN_POINT('Ctrl Pts',(-0.456262618514595,-6.03257604821388,
-19.4272034499686));
#303788=CARTESIAN_POINT('Ctrl Pts',(1.10846582193937,-5.94969996581479,
-19.3557653139141));
#303789=CARTESIAN_POINT('Ctrl Pts',(1.88348680883554,-5.75152486160218,
-19.3180900825478));
#303790=CARTESIAN_POINT('Ctrl Pts',(3.29686085754974,-5.07271961556052,
-19.244754534603));
#303791=CARTESIAN_POINT('Ctrl Pts',(3.92439310707554,-4.60444447817209,
-19.2106868126757));
#303792=CARTESIAN_POINT('Ctrl Pts',(4.96955304918596,-3.45146912203818,
-19.1376747561693));
#303793=CARTESIAN_POINT('Ctrl Pts',(5.37591212001511,-2.77646359988469,
-19.1006312186925));
#303794=CARTESIAN_POINT('Ctrl Pts',(5.91087352636686,-1.298898771716,-19.0293789186388));
#303795=CARTESIAN_POINT('Ctrl Pts',(6.03045617527048,-0.509212114109225,
-18.9927810731533));
#303796=CARTESIAN_POINT('Ctrl Pts',(5.95721002747372,1.05342816605473,-18.9190359248263));
#303797=CARTESIAN_POINT('Ctrl Pts',(5.7719916699652,1.81168071604723,-18.884690775451));
#303798=CARTESIAN_POINT('Ctrl Pts',(5.11816962927493,3.22861464934185,-18.8124562497169));
#303799=CARTESIAN_POINT('Ctrl Pts',(4.6509165381178,3.87150983857004,-18.7749495256425));
#303800=CARTESIAN_POINT('Ctrl Pts',(3.49978141236025,4.93565584114126,-18.7023892825157));
#303801=CARTESIAN_POINT('Ctrl Pts',(2.82876329496631,5.34857491435388,-18.6677130065915));
#303802=CARTESIAN_POINT('Ctrl Pts',(1.42608294779958,5.87195791157714,-18.5971239972846));
#303803=CARTESIAN_POINT('Ctrl Pts',(0.715656660019808,6.00000000000002,
-18.5633707355119));
#303804=CARTESIAN_POINT('Ctrl Pts',(-7.63278329429795E-14,6.00000000000001,
-18.53125));
#303805=CARTESIAN_POINT('Ctrl Pts',(0.,6.00000000000001,-18.75));
#303806=CARTESIAN_POINT('Ctrl Pts',(0.0625576798651179,6.00000000000001,
-18.7528077691461));
#303807=CARTESIAN_POINT('Ctrl Pts',(0.125154581959141,5.99902163936348,
-18.7556315664582));
#303808=CARTESIAN_POINT('Ctrl Pts',(0.967737410896536,5.97264035166073,
-18.7938338417149));
#303809=CARTESIAN_POINT('Ctrl Pts',(1.73547339036332,5.7962914090571,-18.830863802741));
#303810=CARTESIAN_POINT('Ctrl Pts',(3.15621783845425,5.1614171433603,-18.9038894953428));
#303811=CARTESIAN_POINT('Ctrl Pts',(3.7964695325015,4.71049503639122,-18.9379657218031));
#303812=CARTESIAN_POINT('Ctrl Pts',(4.88096931989516,3.57819103271377,-19.0112798068587));
#303813=CARTESIAN_POINT('Ctrl Pts',(5.31018654380289,2.90332477675006,-19.0489520928996));
#303814=CARTESIAN_POINT('Ctrl Pts',(5.8753917453225,1.44214909582631,-19.1204175979676));
#303815=CARTESIAN_POINT('Ctrl Pts',(6.01232352562349,0.672350327266813,
-19.1557700009456));
#303816=CARTESIAN_POINT('Ctrl Pts',(5.98579268880053,-0.885136459007744,
-19.2292719421979));
#303817=CARTESIAN_POINT('Ctrl Pts',(5.81931204714878,-1.65794558834559,
-19.2643770423195));
#303818=CARTESIAN_POINT('Ctrl Pts',(5.19803815918352,-3.09789282705286,
-19.3365873502453));
#303819=CARTESIAN_POINT('Ctrl Pts',(4.74845942672044,-3.75081969854014,
-19.3739868089024));
#303820=CARTESIAN_POINT('Ctrl Pts',(3.63172083244038,-4.83828467655621,
-19.4464832321469));
#303821=CARTESIAN_POINT('Ctrl Pts',(2.9783622869238,-5.26571334302712,-19.4806141611536));
#303822=CARTESIAN_POINT('Ctrl Pts',(1.54139711553658,-5.8505717235476,-19.5536384882869));
#303823=CARTESIAN_POINT('Ctrl Pts',(0.770788081296015,-6.00089330918489,
-19.5903917798261));
#303824=CARTESIAN_POINT('Ctrl Pts',(-0.80324358287202,-5.99907723165657,
-19.6610653463289));
#303825=CARTESIAN_POINT('Ctrl Pts',(-1.59143129627999,-5.83963662859492,
-19.6987666602242));
#303826=CARTESIAN_POINT('Ctrl Pts',(-3.03874051749023,-5.23113632868795,
-19.7726000361462));
#303827=CARTESIAN_POINT('Ctrl Pts',(-3.68732366708566,-4.79608062870309,
-19.8066704794307));
#303828=CARTESIAN_POINT('Ctrl Pts',(-4.79093238880868,-3.69622675941705,
-19.8792756948774));
#303829=CARTESIAN_POINT('Ctrl Pts',(-5.23256165534556,-3.03899004588078,
-19.9166191904337));
#303830=CARTESIAN_POINT('Ctrl Pts',(-5.83791511633105,-1.59183537170407,
-19.9886630567254));
#303831=CARTESIAN_POINT('Ctrl Pts',(-5.99579642745818,-0.815865254731442,
-20.0239971500552));
#303832=CARTESIAN_POINT('Ctrl Pts',(-6.00398471018805,0.742684723690697,
-20.0975492661709));
#303833=CARTESIAN_POINT('Ctrl Pts',(-5.85816251601702,1.51039810786933,
-20.1326660504154));
#303834=CARTESIAN_POINT('Ctrl Pts',(-5.27658788872336,2.96370756497431,
-20.2042852996448));
#303835=CARTESIAN_POINT('Ctrl Pts',(-4.84025153538123,3.63288532261787,
-20.2419378793285));
#303836=CARTESIAN_POINT('Ctrl Pts',(-3.74338724710428,4.75289780919206,
-20.3151256591363));
#303837=CARTESIAN_POINT('Ctrl Pts',(-3.097519322501,5.19695573390423,-20.3492633345057));
#303838=CARTESIAN_POINT('Ctrl Pts',(-1.66977786964651,5.81544118927583,
-20.4223640693831));
#303839=CARTESIAN_POINT('Ctrl Pts',(-0.900973720731938,5.98296395990984,
-20.4593132579278));
#303840=CARTESIAN_POINT('Ctrl Pts',(-0.0810795530095108,5.99958931099151,
-20.4963549265385));
#303841=CARTESIAN_POINT('Ctrl Pts',(-0.0405309741502277,6.00000000000001,
-20.4981808529516));
#303842=CARTESIAN_POINT('Ctrl Pts',(-3.82493263310218E-14,6.00000000000001,
-20.5));
#303843=CARTESIAN_POINT('Origin',(0.,5.28128932132296E-15,28.75));
#303844=CARTESIAN_POINT('',(-1.02900123223315E-14,6.,-16.78125));
#303845=CARTESIAN_POINT('',(9.87720526123303E-14,6.00000000000001,-17.));
#303846=CARTESIAN_POINT('',(-7.34788079488412E-16,6.00000000000001,28.75));
#303847=CARTESIAN_POINT('Ctrl Pts',(-7.86977433022255E-14,6.00000000000001,
-18.53125));
#303848=CARTESIAN_POINT('Ctrl Pts',(-0.0591815161736599,6.,-18.5285937628204));
#303849=CARTESIAN_POINT('Ctrl Pts',(-0.118397665734984,5.99912439105894,
-18.5259232018973));
#303850=CARTESIAN_POINT('Ctrl Pts',(-0.971344796056654,5.97386191467371,
-18.4872720628927));
#303851=CARTESIAN_POINT('Ctrl Pts',(-1.75252380605554,5.79302235819084,
-18.4495732517552));
#303852=CARTESIAN_POINT('Ctrl Pts',(-3.18142084004477,5.14574194746944,
-18.3760007246305));
#303853=CARTESIAN_POINT('Ctrl Pts',(-3.81850338647645,4.69245511397807,
-18.3419843197056));
#303854=CARTESIAN_POINT('Ctrl Pts',(-4.89028640478282,3.56327240875473,
-18.2691421571158));
#303855=CARTESIAN_POINT('Ctrl Pts',(-5.31268370124598,2.8960777624856,-18.231951949522));
#303856=CARTESIAN_POINT('Ctrl Pts',(-5.87961294008907,1.43203112109182,
-18.1603290088255));
#303857=CARTESIAN_POINT('Ctrl Pts',(-6.01664803826308,0.648519325586922,
-18.1243553507422));
#303858=CARTESIAN_POINT('Ctrl Pts',(-5.98045895803983,-0.912389514358998,
-18.0506919136813));
#303859=CARTESIAN_POINT('Ctrl Pts',(-5.81315367720038,-1.67498819720559,
-18.016051448691));
#303860=CARTESIAN_POINT('Ctrl Pts',(-5.19211398101436,-3.10876791568235,
-17.9440831108857));
#303861=CARTESIAN_POINT('Ctrl Pts',(-4.73878323141223,-3.7638272730509,
-17.9064981568775));
#303862=CARTESIAN_POINT('Ctrl Pts',(-3.61221176537734,-4.85365451609604,
-17.8336387876631));
#303863=CARTESIAN_POINT('Ctrl Pts',(-2.95268028276217,-5.2808804537495,
-17.7992619693778));
#303864=CARTESIAN_POINT('Ctrl Pts',(-1.50820722228345,-5.85915920969641,
-17.7259966193809));
#303865=CARTESIAN_POINT('Ctrl Pts',(-0.737182559925239,-6.00506156514386,
-17.6894106944917));
#303866=CARTESIAN_POINT('Ctrl Pts',(0.835968013690152,-5.99454619998606,
-17.6186498092636));
#303867=CARTESIAN_POINT('Ctrl Pts',(1.62283774721748,-5.83092716781848,
-17.5809467146831));
#303868=CARTESIAN_POINT('Ctrl Pts',(3.06661496728735,-5.21486446529017,
-17.5071615801235));
#303869=CARTESIAN_POINT('Ctrl Pts',(3.71297579564821,-4.77627073019087,
-17.4731116171325));
#303870=CARTESIAN_POINT('Ctrl Pts',(4.8104566336335,-3.67069316263874,-17.400457855095));
#303871=CARTESIAN_POINT('Ctrl Pts',(5.24837854165107,-3.01148563919624,
-17.3631419536501));
#303872=CARTESIAN_POINT('Ctrl Pts',(5.84631551067217,-1.56101531678997,
-17.2911772241996));
#303873=CARTESIAN_POINT('Ctrl Pts',(6.00018354690918,-0.783579769628771,
-17.2557292120879));
#303874=CARTESIAN_POINT('Ctrl Pts',(5.99981868468909,0.775448512298382,
-17.1821545235585));
#303875=CARTESIAN_POINT('Ctrl Pts',(5.84985309194878,1.54218372945034,-17.1471398889382));
#303876=CARTESIAN_POINT('Ctrl Pts',(5.26065622016204,2.99178389100055,-17.0754508247896));
#303877=CARTESIAN_POINT('Ctrl Pts',(4.82101861067321,3.65827939799473,-17.0378090784958));
#303878=CARTESIAN_POINT('Ctrl Pts',(3.71840534420017,4.7725230781345,-16.9646820780105));
#303879=CARTESIAN_POINT('Ctrl Pts',(3.0699121665964,5.2133618283659,-16.9305083211487));
#303880=CARTESIAN_POINT('Ctrl Pts',(1.63893320564537,5.82415510192505,-16.8573744552194));
#303881=CARTESIAN_POINT('Ctrl Pts',(0.869662874250451,5.9875431625253,-16.8204646409149));
#303882=CARTESIAN_POINT('Ctrl Pts',(0.0604305076310009,5.99977183602817,
-16.7839656229107));
#303883=CARTESIAN_POINT('Ctrl Pts',(0.0302102150732426,6.00000000000001,
-16.7826059216065));
#303884=CARTESIAN_POINT('Ctrl Pts',(0.,6.00000000000001,-16.78125));
#303885=CARTESIAN_POINT('Ctrl Pts',(2.40155118014229E-13,6.00000000000001,
-17.));
#303886=CARTESIAN_POINT('Ctrl Pts',(0.149839070834264,6.00000000000001,
-17.0067252097723));
#303887=CARTESIAN_POINT('Ctrl Pts',(0.29984142897883,5.99438720189135,-17.013539601656));
#303888=CARTESIAN_POINT('Ctrl Pts',(1.23126125053171,5.92438123344339,-17.0563653306895));
#303889=CARTESIAN_POINT('Ctrl Pts',(1.99378277856738,5.71306256869026,-17.0936712272069));
#303890=CARTESIAN_POINT('Ctrl Pts',(3.3856398038237,5.01362882161217,-17.1663418613708));
#303891=CARTESIAN_POINT('Ctrl Pts',(4.00345032815514,4.53557099792926,-17.2003857335309));
#303892=CARTESIAN_POINT('Ctrl Pts',(5.03766420273522,3.35484842220266,-17.2741535349205));
#303893=CARTESIAN_POINT('Ctrl Pts',(5.43768812582968,2.65795542972892,-17.3118569970205));
#303894=CARTESIAN_POINT('Ctrl Pts',(5.93664279052796,1.16630144852512,-17.3826484198299));
#303895=CARTESIAN_POINT('Ctrl Pts',(6.0376698073148,0.388270682262536,-17.4191764744786));
#303896=CARTESIAN_POINT('Ctrl Pts',(5.93720336712971,-1.16442414842643,
-17.4924522706097));
#303897=CARTESIAN_POINT('Ctrl Pts',(5.73615945908819,-1.92425541901812,
-17.5268512437108));
#303898=CARTESIAN_POINT('Ctrl Pts',(5.05054144881868,-3.33380380872942,
-17.5996857850032));
#303899=CARTESIAN_POINT('Ctrl Pts',(4.56898506298219,-3.96820028743554,
-17.6372647923931));
#303900=CARTESIAN_POINT('Ctrl Pts',(3.39952375656374,-5.00415180210665,
-17.709256932137));
#303901=CARTESIAN_POINT('Ctrl Pts',(2.72677857386028,-5.40027560207936,
-17.7438683302719));
#303902=CARTESIAN_POINT('Ctrl Pts',(1.25428390249301,-5.920119876792,-17.8175392014876));
#303903=CARTESIAN_POINT('Ctrl Pts',(0.466727693143441,-6.03350134537977,
-17.8535633533743));
#303904=CARTESIAN_POINT('Ctrl Pts',(-1.10112874673013,-5.94971903273988,
-17.9251550989244));
#303905=CARTESIAN_POINT('Ctrl Pts',(-1.86642583924248,-5.75569549769191,
-17.9623333501411));
#303906=CARTESIAN_POINT('Ctrl Pts',(-3.27280399884356,-5.08812162592839,
-18.035191111525));
#303907=CARTESIAN_POINT('Ctrl Pts',(-3.9017540577933,-4.62347698782573,
-18.0692085445849));
#303908=CARTESIAN_POINT('Ctrl Pts',(-4.96110379436915,-3.46664759703071,
-18.1427613596476));
#303909=CARTESIAN_POINT('Ctrl Pts',(-5.37576543940734,-2.7805448114744,
-18.180458893232));
#303910=CARTESIAN_POINT('Ctrl Pts',(-5.90777261316549,-1.30382779769193,
-18.2515968761224));
#303911=CARTESIAN_POINT('Ctrl Pts',(-6.02670083067333,-0.529862767402638,
-18.2874943676283));
#303912=CARTESIAN_POINT('Ctrl Pts',(-5.96306756539131,1.02531963810942,
-18.3608875590274));
#303913=CARTESIAN_POINT('Ctrl Pts',(-5.77922274327131,1.79166177857745,
-18.3955943244606));
#303914=CARTESIAN_POINT('Ctrl Pts',(-5.12568929132447,3.21662469276153,
-18.4681273887681));
#303915=CARTESIAN_POINT('Ctrl Pts',(-4.66004482307642,3.86048509497539,
-18.5056263425187));
#303916=CARTESIAN_POINT('Ctrl Pts',(-3.51680399465396,4.922414739695,-18.577882984766));
#303917=CARTESIAN_POINT('Ctrl Pts',(-2.85374503878448,5.33424812827792,
-18.6122068083788));
#303918=CARTESIAN_POINT('Ctrl Pts',(-1.44965307897512,5.86766072759046,
-18.683005439964));
#303919=CARTESIAN_POINT('Ctrl Pts',(-0.727564949466366,6.00000000000001,
-18.7173447861033));
#303920=CARTESIAN_POINT('Ctrl Pts',(-3.60822483003176E-15,6.00000000000001,
-18.75));
#303921=CARTESIAN_POINT('Origin',(0.,5.28128932132296E-15,28.75));
#303922=CARTESIAN_POINT('',(7.74869955620949E-14,6.00000000000001,-15.03125));
#303923=CARTESIAN_POINT('',(8.5709584838225E-14,6.00000000000001,-15.25));
#303924=CARTESIAN_POINT('',(-7.34788079488412E-16,6.00000000000001,28.75));
#303925=CARTESIAN_POINT('Ctrl Pts',(-2.77555756156289E-15,6.,-16.78125));
#303926=CARTESIAN_POINT('Ctrl Pts',(-0.762995914369974,6.,-16.7470045421831));
#303927=CARTESIAN_POINT('Ctrl Pts',(-1.51937474040237,5.85445698505616,
-16.7109335760792));
#303928=CARTESIAN_POINT('Ctrl Pts',(-2.94654565841153,5.28357027467349,
-16.6385525968161));
#303929=CARTESIAN_POINT('Ctrl Pts',(-3.60240026688677,4.86014142112396,
-16.6043810427931));
#303930=CARTESIAN_POINT('Ctrl Pts',(-4.72598043643502,3.77920016817781,
-16.5319439136972));
#303931=CARTESIAN_POINT('Ctrl Pts',(-5.17970425282934,3.1285664882428,-16.494517027221));
#303932=CARTESIAN_POINT('Ctrl Pts',(-5.8092898938032,1.69243114615325,-16.4222216952709));
#303933=CARTESIAN_POINT('Ctrl Pts',(-5.98025194768284,0.921280430733282,
-16.3872276722945));
#303934=CARTESIAN_POINT('Ctrl Pts',(-6.01635011330383,-0.635631715023033,
-16.3137528498556));
#303935=CARTESIAN_POINT('Ctrl Pts',(-5.88405811920462,-1.4065114945738,
-16.278268627381));
#303936=CARTESIAN_POINT('Ctrl Pts',(-5.32740290463626,-2.87174215114001,
-16.2068854740689));
#303937=CARTESIAN_POINT('Ctrl Pts',(-4.90191964302404,-3.54954068251286,
-16.1692048116772));
#303938=CARTESIAN_POINT('Ctrl Pts',(-3.82388772255212,-4.68821226796535,
-16.0958270276199));
#303939=CARTESIAN_POINT('Ctrl Pts',(-3.18655783477906,-5.14269353849257,
-16.0617742944772));
#303940=CARTESIAN_POINT('Ctrl Pts',(-1.76949133222635,-5.78605770987929,
-15.9887898675571));
#303941=CARTESIAN_POINT('Ctrl Pts',(-1.002349018499,-5.96698758165948,-15.9517197467449));
#303942=CARTESIAN_POINT('Ctrl Pts',(0.567728586615961,-6.02514302424957,
-15.8804020340791));
#303943=CARTESIAN_POINT('Ctrl Pts',(1.35564413377838,-5.89805180320577,
-15.8439180358184));
#303944=CARTESIAN_POINT('Ctrl Pts',(2.82088234409026,-5.35170012385111,
-15.7701862891916));
#303945=CARTESIAN_POINT('Ctrl Pts',(3.486466596131,-4.94394913206419,-15.7357966941946));
#303946=CARTESIAN_POINT('Ctrl Pts',(4.63656757456683,-3.88874666387088,
-15.6636065985564));
#303947=CARTESIAN_POINT('Ctrl Pts',(5.10637394239805,-3.2473143931632,-15.6260849024967));
#303948=CARTESIAN_POINT('Ctrl Pts',(5.76828544948956,-1.8263270111654,-15.5534712225508));
#303949=CARTESIAN_POINT('Ctrl Pts',(5.9566277070017,-1.0616775585047,-15.5188533859303));
#303950=CARTESIAN_POINT('Ctrl Pts',(6.02988463147326,0.492873969955938,
-15.4454899672962));
#303951=CARTESIAN_POINT('Ctrl Pts',(5.91563081234682,1.26790813161792,-15.4094362565975));
#303952=CARTESIAN_POINT('Ctrl Pts',(5.39225127407362,2.74857516884805,-15.3383867864066));
#303953=CARTESIAN_POINT('Ctrl Pts',(4.98139695353482,3.43753260359899,-15.3006858752191));
#303954=CARTESIAN_POINT('Ctrl Pts',(3.92859923421987,4.60064881530623,-15.2270747788359));
#303955=CARTESIAN_POINT('Ctrl Pts',(3.30256757325392,5.06881789833565,-15.193058499304));
#303956=CARTESIAN_POINT('Ctrl Pts',(1.89995959949218,5.74477422197141,-15.1202477106475));
#303957=CARTESIAN_POINT('Ctrl Pts',(1.13535431743488,5.94334142844029,-15.0830342480049));
#303958=CARTESIAN_POINT('Ctrl Pts',(0.236119305774866,5.99651893777345,
-15.0418984811186));
#303959=CARTESIAN_POINT('Ctrl Pts',(0.118002034649196,6.00000000000001,
-15.0365462717411));
#303960=CARTESIAN_POINT('Ctrl Pts',(1.47416800988509E-13,6.00000000000001,
-15.03125));
#303961=CARTESIAN_POINT('Ctrl Pts',(1.46965772884755E-13,6.00000000000001,
-15.25));
#303962=CARTESIAN_POINT('Ctrl Pts',(0.239244323353593,6.00000000000001,
-15.2607379754322));
#303963=CARTESIAN_POINT('Ctrl Pts',(0.478743560224347,5.98569123812276,
-15.2716960615625));
#303964=CARTESIAN_POINT('Ctrl Pts',(1.49888728445648,5.86286612757501,-15.3192742544649));
#303965=CARTESIAN_POINT('Ctrl Pts',(2.25444285070019,5.61581264251811,-15.3567886313169));
#303966=CARTESIAN_POINT('Ctrl Pts',(3.61480890219032,4.85090024903875,-15.429000756656));
#303967=CARTESIAN_POINT('Ctrl Pts',(4.20929919129207,4.34509667563156,-15.4633680510008));
#303968=CARTESIAN_POINT('Ctrl Pts',(5.18434125342705,3.12215321735148,-15.5371064557438));
#303969=CARTESIAN_POINT('Ctrl Pts',(5.55020848663417,2.41252824406093,-15.5736463796502));
#303970=CARTESIAN_POINT('Ctrl Pts',(5.98295890856739,0.902007856180706,
-15.6449318517253));
#303971=CARTESIAN_POINT('Ctrl Pts',(6.04943761408849,0.116778643172001,
-15.6819889054305));
#303972=CARTESIAN_POINT('Ctrl Pts',(5.87848705715856,-1.43003326182809,
-15.7549870706616));
#303973=CARTESIAN_POINT('Ctrl Pts',(5.64460477390343,-2.1771648796185,-15.7890468905164));
#303974=CARTESIAN_POINT('Ctrl Pts',(4.89744175132958,-3.55568208160752,
-15.8624038777688));
#303975=CARTESIAN_POINT('Ctrl Pts',(4.38559395946307,-4.17066467448128,
-15.9000819273598));
#303976=CARTESIAN_POINT('Ctrl Pts',(3.1662280353415,-5.15512186862005,-15.9714923429295));
#303977=CARTESIAN_POINT('Ctrl Pts',(2.47476798475488,-5.52049650357891,
-16.0069325140209));
#303978=CARTESIAN_POINT('Ctrl Pts',(0.983693207862198,-5.97033057503644,
-16.0804163318438));
#303979=CARTESIAN_POINT('Ctrl Pts',(0.197391021470089,-6.04760579088883,
-16.1154462703826));
#303980=CARTESIAN_POINT('Ctrl Pts',(-1.3633589140374,-5.89561518199393,
-16.1877137598355));
#303981=CARTESIAN_POINT('Ctrl Pts',(-2.12265616753833,-5.66668645028802,
-16.2251317550863));
#303982=CARTESIAN_POINT('Ctrl Pts',(-3.49924836607179,-4.93493292272614,
-16.2975885899212));
#303983=CARTESIAN_POINT('Ctrl Pts',(-4.10562278276477,-4.4432136474317,
-16.3317460828671));
#303984=CARTESIAN_POINT('Ctrl Pts',(-5.11154083410974,-3.24081677352315,
-16.4055564996032));
#303985=CARTESIAN_POINT('Ctrl Pts',(-5.49512206213318,-2.53656496888065,
-16.4427927569157));
#303986=CARTESIAN_POINT('Ctrl Pts',(-5.96130427935292,-1.03422257730741,
-16.5136922876079));
#303987=CARTESIAN_POINT('Ctrl Pts',(-6.04507636618779,-0.252414557192574,
-16.5505878861269));
#303988=CARTESIAN_POINT('Ctrl Pts',(-5.9093273272881,1.29751549309194,-16.623733204922));
#303989=CARTESIAN_POINT('Ctrl Pts',(-5.69183561586978,2.05102812652172,
-16.657920888541));
#303990=CARTESIAN_POINT('Ctrl Pts',(-4.97543154461942,3.44529752823625,
-16.7310260623448));
#303991=CARTESIAN_POINT('Ctrl Pts',(-4.4786810474085,4.07019095030031,-16.7686637179511));
#303992=CARTESIAN_POINT('Ctrl Pts',(-3.28419150975437,5.08066070730256,
-16.8403772346117));
#303993=CARTESIAN_POINT('Ctrl Pts',(-2.60210904155631,5.46150942826808,
-16.8753568518416));
#303994=CARTESIAN_POINT('Ctrl Pts',(-1.26309840810919,5.89980686100247,
-16.9418473495661));
#303995=CARTESIAN_POINT('Ctrl Pts',(-0.633071948168211,6.00000000000001,
-16.9715859046061));
#303996=CARTESIAN_POINT('Ctrl Pts',(2.37448949391705E-13,6.00000000000001,
-17.));
#303997=CARTESIAN_POINT('Origin',(0.,5.28128932132296E-15,28.75));
#303998=CARTESIAN_POINT('',(9.14341723089484E-14,6.00000000000001,-13.28125));
#303999=CARTESIAN_POINT('',(6.50211092512395E-15,6.00000000000001,-13.5));
#304000=CARTESIAN_POINT('',(-7.34788079488412E-16,6.00000000000001,28.75));
#304001=CARTESIAN_POINT('Ctrl Pts',(1.46549439250521E-13,6.,-15.03125));
#304002=CARTESIAN_POINT('Ctrl Pts',(-0.66735187386771,6.,-15.0012973226459));
#304003=CARTESIAN_POINT('Ctrl Pts',(-1.33087327795904,5.88866100281656,
-14.9698928741171));
#304004=CARTESIAN_POINT('Ctrl Pts',(-2.69406578468223,5.41668316456592,
-14.9018258515768));
#304005=CARTESIAN_POINT('Ctrl Pts',(-3.36927694279044,5.02458086822543,
-14.8671259278388));
#304006=CARTESIAN_POINT('Ctrl Pts',(-4.545372492241,3.99531773232578,-14.795205119886));
#304007=CARTESIAN_POINT('Ctrl Pts',(-5.03095626552528,3.36339510574058,
-14.7576088470367));
#304008=CARTESIAN_POINT('Ctrl Pts',(-5.7247193048184,1.95784216770291,-14.6847009145714));
#304009=CARTESIAN_POINT('Ctrl Pts',(-5.93011958458863,1.19967591081642,
-14.6503658949762));
#304010=CARTESIAN_POINT('Ctrl Pts',(-6.03992846624795,-0.352356705974768,
-14.5771213504791));
#304011=CARTESIAN_POINT('Ctrl Pts',(-5.94344657136843,-1.1314072910134,
-14.5404193980675));
#304012=CARTESIAN_POINT('Ctrl Pts',(-5.45288773164758,-2.62677185445911,
-14.469719199516));
#304013=CARTESIAN_POINT('Ctrl Pts',(-5.05660369673818,-3.32634294818924,
-14.4320172297277));
#304014=CARTESIAN_POINT('Ctrl Pts',(-4.0287896424963,-4.5130527616718,-14.3581983631882));
#304015=CARTESIAN_POINT('Ctrl Pts',(-3.41379145975777,-4.9944802221304,
-14.3241346393133));
#304016=CARTESIAN_POINT('Ctrl Pts',(-2.02565547621593,-5.70189879844987,
-14.25151457081));
#304017=CARTESIAN_POINT('Ctrl Pts',(-1.26389202499577,-5.91756242934041,
-14.2141793348777));
#304018=CARTESIAN_POINT('Ctrl Pts',(0.299762092627998,-6.04364376330619,
-14.1421593409458));
#304019=CARTESIAN_POINT('Ctrl Pts',(1.08658867426295,-5.95271641631752,
-14.1067912133187));
#304020=CARTESIAN_POINT('Ctrl Pts',(2.57072633147742,-5.47637605377605,
-14.0332322033617));
#304021=CARTESIAN_POINT('Ctrl Pts',(3.25513422151646,-5.09935195025191,
-13.9981468843864));
#304022=CARTESIAN_POINT('Ctrl Pts',(4.45581733815711,-4.09529386357075,
-13.926506358527));
#304023=CARTESIAN_POINT('Ctrl Pts',(4.95632750342893,-3.47282417207507,
-13.8888569501452));
#304024=CARTESIAN_POINT('Ctrl Pts',(5.68037470491989,-2.0824231669912,-13.8156874564946));
#304025=CARTESIAN_POINT('Ctrl Pts',(5.90194277265011,-1.33048982502385,
-13.7815393512917));
#304026=CARTESIAN_POINT('Ctrl Pts',(6.04644434796632,0.218710856532157,
-13.7084284533456));
#304027=CARTESIAN_POINT('Ctrl Pts',(5.96696002944824,1.00140412246603,-13.6714910777235));
#304028=CARTESIAN_POINT('Ctrl Pts',(5.5090831597919,2.50582032466959,-13.6004936783954));
#304029=CARTESIAN_POINT('Ctrl Pts',(5.12991944744186,3.21142492404718,-13.563438477574));
#304030=CARTESIAN_POINT('Ctrl Pts',(4.13169520542801,4.41896754161158,-13.4896450178015));
#304031=CARTESIAN_POINT('Ctrl Pts',(3.52828162141067,4.91420636676231,-13.4554439484537));
#304032=CARTESIAN_POINT('Ctrl Pts',(2.15569821673854,5.65426229804528,-13.3830459631315));
#304033=CARTESIAN_POINT('Ctrl Pts',(1.39729636086131,5.88772412806485,-13.3456020482254));
#304034=CARTESIAN_POINT('Ctrl Pts',(0.41062612721705,5.98947399864505,-13.2998335893983));
#304035=CARTESIAN_POINT('Ctrl Pts',(0.205196689547594,6.00000000000001,
-13.2904598194023));
#304036=CARTESIAN_POINT('Ctrl Pts',(1.60357838119296E-13,6.00000000000001,
-13.28125));
#304037=CARTESIAN_POINT('Ctrl Pts',(-1.38777878078145E-16,6.00000000000001,
-13.5));
#304038=CARTESIAN_POINT('Ctrl Pts',(0.327777791193107,6.00000000000001,
-13.5147116128805));
#304039=CARTESIAN_POINT('Ctrl Pts',(0.655733943217833,5.97314225488786,
-13.5298229065593));
#304040=CARTESIAN_POINT('Ctrl Pts',(1.76080102696931,5.79008139572056,-13.5820911428346));
#304041=CARTESIAN_POINT('Ctrl Pts',(2.50784671930172,5.50783221520244,-13.6197368425539));
#304042=CARTESIAN_POINT('Ctrl Pts',(3.83516240013118,4.67875298122624,-13.6914013383341));
#304043=CARTESIAN_POINT('Ctrl Pts',(4.40618039353526,4.14545661396193,-13.7264515580286));
#304044=CARTESIAN_POINT('Ctrl Pts',(5.32030200711686,2.88274754157419,-13.8000183191284));
#304045=CARTESIAN_POINT('Ctrl Pts',(5.65133170850177,2.16293172541357,-13.835425502794));
#304046=CARTESIAN_POINT('Ctrl Pts',(6.0173450674626,0.637422317825967,-13.90741834655));
#304047=CARTESIAN_POINT('Ctrl Pts',(6.04906161240216,-0.153501012269999,
-13.9447441207756));
#304048=CARTESIAN_POINT('Ctrl Pts',(5.80808025958564,-1.69265443149444,
-14.0173808617066));
#304049=CARTESIAN_POINT('Ctrl Pts',(5.54159120090127,-2.4268558179121,-14.0514375150167));
#304050=CARTESIAN_POINT('Ctrl Pts',(4.73308137588808,-3.77246607804078,
-14.1252398343965));
#304051=CARTESIAN_POINT('Ctrl Pts',(4.19141704377373,-4.36642845683353,
-14.1629424247462));
#304052=CARTESIAN_POINT('Ctrl Pts',(2.92283134564345,-5.29730868071715,
-14.2336726042976));
#304053=CARTESIAN_POINT('Ctrl Pts',(2.21250088012577,-5.63111929827263,
-14.2703170673848));
#304054=CARTESIAN_POINT('Ctrl Pts',(0.703234222332097,-6.00926253915792,
-14.3435718980254));
#304055=CARTESIAN_POINT('Ctrl Pts',(-0.0813751723367943,-6.04972473594463,
-14.377927200096));
#304056=CARTESIAN_POINT('Ctrl Pts',(-1.6329431622039,-5.82719528272542,
-14.4508112688191));
#304057=CARTESIAN_POINT('Ctrl Pts',(-2.38435662489997,-5.5621557904809,
-14.4884020320523));
#304058=CARTESIAN_POINT('Ctrl Pts',(-3.72809186809351,-4.7644223507681,
-14.5603463589942));
#304059=CARTESIAN_POINT('Ctrl Pts',(-4.31065812373274,-4.24459900497216,
-14.5950166285999));
#304060=CARTESIAN_POINT('Ctrl Pts',(-5.25473931733798,-3.00132172450994,
-14.6686725436814));
#304061=CARTESIAN_POINT('Ctrl Pts',(-5.60288211475291,-2.28645239165933,
-14.7045962342353));
#304062=CARTESIAN_POINT('Ctrl Pts',(-6.00184118239683,-0.768121793220075,
-14.7762502909063));
#304063=CARTESIAN_POINT('Ctrl Pts',(-6.05075533966853,0.0201800109101076,
-14.8134523483535));
#304064=CARTESIAN_POINT('Ctrl Pts',(-5.84430619638249,1.56335120441045,
-14.8862786987318));
#304065=CARTESIAN_POINT('Ctrl Pts',(-5.59389917079461,2.30396805033726,
-14.9202947230065));
#304066=CARTESIAN_POINT('Ctrl Pts',(-4.81566514298174,3.66607000268275,
-14.9938868647953));
#304067=CARTESIAN_POINT('Ctrl Pts',(-4.28866309072003,4.27061589916235,
-15.03158681112));
#304068=CARTESIAN_POINT('Ctrl Pts',(-3.04430197290824,5.22822388667977,
-15.1026654784338));
#304069=CARTESIAN_POINT('Ctrl Pts',(-2.34331405581276,5.57773485223415,
-15.1386672715034));
#304070=CARTESIAN_POINT('Ctrl Pts',(-1.07453784633482,5.92765342078551,
-15.2007165872237));
#304071=CARTESIAN_POINT('Ctrl Pts',(-0.537960873596693,6.00000000000001,
-15.2258547640204));
#304072=CARTESIAN_POINT('Ctrl Pts',(1.61121116448726E-13,6.00000000000001,
-15.25));
#304073=CARTESIAN_POINT('Origin',(0.,5.28128932132296E-15,28.75));
#304074=CARTESIAN_POINT('',(2.04492876719775E-14,6.00000000000001,-11.53125));
#304075=CARTESIAN_POINT('',(-6.44949795900495E-16,6.00000000000001,-11.75));
#304076=CARTESIAN_POINT('',(-7.34788079488412E-16,6.00000000000001,28.75));
#304077=CARTESIAN_POINT('Ctrl Pts',(1.57512891618694E-13,6.00000000000001,
-13.28125));
#304078=CARTESIAN_POINT('Ctrl Pts',(-0.573980629105695,6.00000000000001,
-13.2554880934792));
#304079=CARTESIAN_POINT('Ctrl Pts',(-1.14603217573204,5.91763999221552,
-13.2286116862984));
#304080=CARTESIAN_POINT('Ctrl Pts',(-2.4419267062499,5.53513980010466,-13.1648700734188));
#304081=CARTESIAN_POINT('Ctrl Pts',(-3.13578102190386,5.17373789630424,
-13.1292976708043));
#304082=CARTESIAN_POINT('Ctrl Pts',(-4.36145501139311,4.19598829988954,
-13.0579683686895));
#304083=CARTESIAN_POINT('Ctrl Pts',(-4.87712915420713,3.58359392864256,
-13.0202829968094));
#304084=CARTESIAN_POINT('Ctrl Pts',(-5.63211775910767,2.20916311949069,
-12.9468649516664));
#304085=CARTESIAN_POINT('Ctrl Pts',(-5.87016462544125,1.46366565576377,
-12.9128242727264));
#304086=CARTESIAN_POINT('Ctrl Pts',(-6.0500616200403,-0.0822755225612855,
-12.8398671994015));
#304087=CARTESIAN_POINT('Ctrl Pts',(-5.98799810878256,-0.868314983456971,
-12.8027719079449));
#304088=CARTESIAN_POINT('Ctrl Pts',(-5.56375655704784,-2.38084496844363,
-12.7313915976408));
#304089=CARTESIAN_POINT('Ctrl Pts',(-5.20236924062146,-3.0918075866398,
-12.6950151226897));
#304090=CARTESIAN_POINT('Ctrl Pts',(-4.23514621504392,-4.31991116899216,
-12.6212965995673));
#304091=CARTESIAN_POINT('Ctrl Pts',(-3.64366648286652,-4.82926489771456,
-12.5868614836686));
#304092=CARTESIAN_POINT('Ctrl Pts',(-2.28746711962188,-5.60250684109875,
-12.5147148987157));
#304093=CARTESIAN_POINT('Ctrl Pts',(-1.53292126968421,-5.8541210542095,
-12.477179330227));
#304094=CARTESIAN_POINT('Ctrl Pts',(0.0222798434847502,-6.05041700754087,
-12.4045147683223));
#304095=CARTESIAN_POINT('Ctrl Pts',(0.807561443282626,-5.99632148589134,
-12.3699506676802));
#304096=CARTESIAN_POINT('Ctrl Pts',(2.31017703688754,-5.59159109628828,
-12.296606626736));
#304097=CARTESIAN_POINT('Ctrl Pts',(3.01354411696049,-5.2460644128885,-12.2604498204306));
#304098=CARTESIAN_POINT('Ctrl Pts',(4.26410133507651,-4.29522557818065,
-12.1894577225396));
#304099=CARTESIAN_POINT('Ctrl Pts',(4.79485640139218,-3.69334236966529,
-12.1517553313286));
#304100=CARTESIAN_POINT('Ctrl Pts',(5.58081886858524,-2.33540318145575,
-12.078107742142));
#304101=CARTESIAN_POINT('Ctrl Pts',(5.83533250109748,-1.59641767050439,
-12.0440891931576));
#304102=CARTESIAN_POINT('Ctrl Pts',(6.05060200132583,-0.0542281005932625,
-11.9713091682056));
#304103=CARTESIAN_POINT('Ctrl Pts',(6.00607047451364,0.734777899607572,
-11.934073877874));
#304104=CARTESIAN_POINT('Ctrl Pts',(5.61551958022899,2.25498133873888,-11.8623314368728));
#304105=CARTESIAN_POINT('Ctrl Pts',(5.27175974242709,2.97112818183415,-11.8265474550426));
#304106=CARTESIAN_POINT('Ctrl Pts',(4.3353453527759,4.21940059916099,-11.752913497935));
#304107=CARTESIAN_POINT('Ctrl Pts',(3.75573331455707,4.74268032871428,-11.7181540580097));
#304108=CARTESIAN_POINT('Ctrl Pts',(2.41617000682841,5.54847427122919,-11.646279430568));
#304109=CARTESIAN_POINT('Ctrl Pts',(1.66584109193327,5.81793662423257,-11.6086728449161));
#304110=CARTESIAN_POINT('Ctrl Pts',(0.591316333642613,5.97816519706421,
-11.558108407162));
#304111=CARTESIAN_POINT('Ctrl Pts',(0.295541259485836,6.00000000000001,
-11.5445147443378));
#304112=CARTESIAN_POINT('Ctrl Pts',(8.16707812489881E-14,6.00000000000001,
-11.53125));
#304113=CARTESIAN_POINT('Ctrl Pts',(-1.45716771982052E-15,6.00000000000001,
-11.75));
#304114=CARTESIAN_POINT('Ctrl Pts',(0.416845576792399,6.00000000000001,
-11.7687092320514));
#304115=CARTESIAN_POINT('Ctrl Pts',(0.833493300982548,5.95656316824371,
-11.7880430377037));
#304116=CARTESIAN_POINT('Ctrl Pts',(2.02039612084546,5.70518972109559,-11.8449805231463));
#304117=CARTESIAN_POINT('Ctrl Pts',(2.75728128825485,5.38782752092871,-11.8826822540648));
#304118=CARTESIAN_POINT('Ctrl Pts',(4.04949626850756,4.49489052928717,-11.9537025881064));
#304119=CARTESIAN_POINT('Ctrl Pts',(4.59645541967849,3.93385564503483,-11.9898084787577));
#304120=CARTESIAN_POINT('Ctrl Pts',(5.44827395812056,2.63146422558047,-12.0631620642225));
#304121=CARTESIAN_POINT('Ctrl Pts',(5.74384238938711,1.90173151395159,-12.0977522350444));
#304122=CARTESIAN_POINT('Ctrl Pts',(6.04060669966887,0.36251640842141,-12.1703918871161));
#304123=CARTESIAN_POINT('Ctrl Pts',(6.03598507272798,-0.432709508607057,
-12.2079207118553));
#304124=CARTESIAN_POINT('Ctrl Pts',(5.7226670320772,-1.96193118601187,-12.2800887474913));
#304125=CARTESIAN_POINT('Ctrl Pts',(5.42241874027092,-2.68243489957792,
-12.3145011806245));
#304126=CARTESIAN_POINT('Ctrl Pts',(4.55568892318795,-3.98372213282641,
-12.3882262348037));
#304127=CARTESIAN_POINT('Ctrl Pts',(3.99206020552507,-4.54837147961571,
-12.4246552386242));
#304128=CARTESIAN_POINT('Ctrl Pts',(2.68612979394882,-5.42167675647812,
-12.4960048649511));
#304129=CARTESIAN_POINT('Ctrl Pts',(1.95843226440761,-5.72488742607485,
-12.5330878516889));
#304130=CARTESIAN_POINT('Ctrl Pts',(0.433189775767892,-6.03437164221625,
-12.6060584462626));
#304131=CARTESIAN_POINT('Ctrl Pts',(-0.349468372851078,-6.0397987907425,
-12.6401047497293));
#304132=CARTESIAN_POINT('Ctrl Pts',(-1.8904147258544,-5.74931568846158,
-12.7135030794629));
#304133=CARTESIAN_POINT('Ctrl Pts',(-2.63260735637681,-5.44956408199337,
-12.7511862034793));
#304134=CARTESIAN_POINT('Ctrl Pts',(-3.94270090736319,-4.58864472992702,
-12.8225420554432));
#304135=CARTESIAN_POINT('Ctrl Pts',(-4.50181657165394,-4.0415696806281,
-12.8580707922009));
#304136=CARTESIAN_POINT('Ctrl Pts',(-5.38509416954836,-2.75909556727989,
-12.9315365891624));
#304137=CARTESIAN_POINT('Ctrl Pts',(-5.69854638141101,-2.03431059711724,
-12.9664954757139));
#304138=CARTESIAN_POINT('Ctrl Pts',(-6.03039733330066,-0.501806972866215,
-13.038818395145));
#304139=CARTESIAN_POINT('Ctrl Pts',(-6.04421585770172,0.291443690587449,
-13.0762540024177));
#304140=CARTESIAN_POINT('Ctrl Pts',(-5.76750740744192,1.8259476416692,-13.1486713225888));
#304141=CARTESIAN_POINT('Ctrl Pts',(-5.4843606631894,2.55342877114943,-13.1828575540103));
#304142=CARTESIAN_POINT('Ctrl Pts',(-4.64675548347716,3.87781462041123,
-13.2566566129115));
#304143=CARTESIAN_POINT('Ctrl Pts',(-4.09371675122386,4.45769755329096,
-13.2937702714903));
#304144=CARTESIAN_POINT('Ctrl Pts',(-2.80590088304983,5.36042237566801,
-13.3647358998891));
#304145=CARTESIAN_POINT('Ctrl Pts',(-2.08678176698081,5.67912400530407,
-13.4016597725162));
#304146=CARTESIAN_POINT('Ctrl Pts',(-0.890512478632302,5.95039638288354,
-13.4593078448214));
#304147=CARTESIAN_POINT('Ctrl Pts',(-0.445453596806061,6.00000000000001,
-13.4800067574786));
#304148=CARTESIAN_POINT('Ctrl Pts',(-7.21644966006352E-15,6.00000000000001,
-13.5));
#304149=CARTESIAN_POINT('Origin',(0.,5.28128932132296E-15,28.75));
#304150=CARTESIAN_POINT('',(-2.93478478418988E-15,6.00000000000001,-9.78125));
#304151=CARTESIAN_POINT('',(-6.83338598285155E-14,6.00000000000001,-10.));
#304152=CARTESIAN_POINT('',(-7.34788079488412E-16,6.00000000000001,28.75));
#304153=CARTESIAN_POINT('Ctrl Pts',(7.74380559676047E-14,6.00000000000001,
-11.53125));
#304154=CARTESIAN_POINT('Ctrl Pts',(-0.478944394585049,6.00000000000001,
-11.5097535938561));
#304155=CARTESIAN_POINT('Ctrl Pts',(-0.957199281274125,5.94265698294226,
-11.4874518824837));
#304156=CARTESIAN_POINT('Ctrl Pts',(-2.18016139292464,5.64376182111039,
-11.4282029269918));
#304157=CARTESIAN_POINT('Ctrl Pts',(-2.8927901865173,5.31385278926475,-11.3914069174792));
#304158=CARTESIAN_POINT('Ctrl Pts',(-4.16707304774843,4.38968577054325,
-11.320735990777));
#304159=CARTESIAN_POINT('Ctrl Pts',(-4.7122067867575,3.79858157252758,-11.2830659584832));
#304160=CARTESIAN_POINT('Ctrl Pts',(-5.52817353808929,2.4572253914444,-11.2092192096192));
#304161=CARTESIAN_POINT('Ctrl Pts',(-5.79864984016499,1.72462569233648,
-11.1751396704854));
#304162=CARTESIAN_POINT('Ctrl Pts',(-6.04818769601602,0.186540241838315,
-11.1025533298373));
#304163=CARTESIAN_POINT('Ctrl Pts',(-6.02074829091575,-0.604976250624933,
-11.065199562703));
#304164=CARTESIAN_POINT('Ctrl Pts',(-5.66290961022047,-2.1322007963153,
-10.9931257770211));
#304165=CARTESIAN_POINT('Ctrl Pts',(-5.33610124725688,-2.85322000262038,
-10.9578339280619));
#304166=CARTESIAN_POINT('Ctrl Pts',(-4.4293802801778,-4.1206933283928,-10.8842905570082));
#304167=CARTESIAN_POINT('Ctrl Pts',(-3.8612167765651,-4.65730412455171,
-10.8491335297397));
#304168=CARTESIAN_POINT('Ctrl Pts',(-2.5380046111267,-5.49406311947361,
-10.7775412150547));
#304169=CARTESIAN_POINT('Ctrl Pts',(-1.79209090127394,-5.78053228501042,
-10.7398847805265));
#304170=CARTESIAN_POINT('Ctrl Pts',(-0.246868659707394,-6.04498528485984,
-10.6666741422391));
#304171=CARTESIAN_POINT('Ctrl Pts',(0.536570867436116,-6.02618227783149,
-10.632548976392));
#304172=CARTESIAN_POINT('Ctrl Pts',(2.05589147767883,-5.69043622770825,
-10.559461187726));
#304173=CARTESIAN_POINT('Ctrl Pts',(2.77711115164746,-5.37545375198148,
-10.5224972736616));
#304174=CARTESIAN_POINT('Ctrl Pts',(4.06933731651797,-4.47981446503917,
-10.4514370291489));
#304175=CARTESIAN_POINT('Ctrl Pts',(4.6249530196992,-3.90361749743191,-10.4144965398214));
#304176=CARTESIAN_POINT('Ctrl Pts',(5.46963106611957,-2.58481422655512,
-10.3407144265787));
#304177=CARTESIAN_POINT('Ctrl Pts',(5.75692585399269,-1.85901826685715,
-10.3064820132932));
#304178=CARTESIAN_POINT('Ctrl Pts',(6.04252155509357,-0.325748505886516,
-10.234122937834));
#304179=CARTESIAN_POINT('Ctrl Pts',(6.0331706455049,0.468019907972567,-10.1966628965434));
#304180=CARTESIAN_POINT('Ctrl Pts',(5.70982978291748,2.00219512628821,-10.1242610901454));
#304181=CARTESIAN_POINT('Ctrl Pts',(5.40073061139426,2.72819414196556,-10.0894001367273));
#304182=CARTESIAN_POINT('Ctrl Pts',(4.52510304641024,4.01553378463539,-10.0159607808973));
#304183=CARTESIAN_POINT('Ctrl Pts',(3.96894184952754,4.56601213198919,-9.98029988335034));
#304184=CARTESIAN_POINT('Ctrl Pts',(2.66316757061658,5.43476013554676,-9.90902372494367));
#304185=CARTESIAN_POINT('Ctrl Pts',(1.92223293760542,5.73881717093973,-9.87133427597963));
#304186=CARTESIAN_POINT('Ctrl Pts',(0.765970530564992,5.96333217942141,
-9.8161637062234));
#304187=CARTESIAN_POINT('Ctrl Pts',(0.382990950460819,6.00000000000001,
-9.79843973875384));
#304188=CARTESIAN_POINT('Ctrl Pts',(2.08166817117217E-16,6.00000000000001,
-9.78125));
#304189=CARTESIAN_POINT('Ctrl Pts',(-1.61953783717195E-13,6.00000000000001,
-10.));
#304190=CARTESIAN_POINT('Ctrl Pts',(0.506806976524611,6.00000000000002,
-10.0227469592026));
#304191=CARTESIAN_POINT('Ctrl Pts',(1.01260390412922,5.93579069372547,-10.0463849702122));
#304192=CARTESIAN_POINT('Ctrl Pts',(2.27288361303783,5.60917766018831,-10.1077130660897));
#304193=CARTESIAN_POINT('Ctrl Pts',(2.99348358036239,5.26001392829972,-10.1447111295798));
#304194=CARTESIAN_POINT('Ctrl Pts',(4.24641366615186,4.30994255992357,-10.2157397471939));
#304195=CARTESIAN_POINT('Ctrl Pts',(4.76982050763015,3.72241176721537,-10.2526903345165));
#304196=CARTESIAN_POINT('Ctrl Pts',(5.56109371518005,2.38268610160769,-10.325789852975));
#304197=CARTESIAN_POINT('Ctrl Pts',(5.82245658329901,1.64376593499296,-10.3599263163893));
#304198=CARTESIAN_POINT('Ctrl Pts',(6.0512218582964,0.0928902020369393,
-10.4331162644633));
#304199=CARTESIAN_POINT('Ctrl Pts',(6.01073950667083,-0.704965909147716,
-10.4707692150558));
#304200=CARTESIAN_POINT('Ctrl Pts',(5.62670873719465,-2.22250515293938,
-10.5423859255975));
#304201=CARTESIAN_POINT('Ctrl Pts',(5.29328924334698,-2.9292511354159,-10.5775064834447));
#304202=CARTESIAN_POINT('Ctrl Pts',(4.37033294396524,-4.18513628552011,
-10.6510577761562));
#304203=CARTESIAN_POINT('Ctrl Pts',(3.78641460417051,-4.7199811781779,-10.6863878479209));
#304204=CARTESIAN_POINT('Ctrl Pts',(2.44591141916343,-5.53468177772513,
-10.7584345485147));
#304205=CARTESIAN_POINT('Ctrl Pts',(1.7022457118447,-5.80667789793638,-10.7957790209596));
#304206=CARTESIAN_POINT('Ctrl Pts',(0.162872612909248,-6.04749624303929,
-10.868382460803));
#304207=CARTESIAN_POINT('Ctrl Pts',(-0.617551262279904,-6.01808563333494,
-10.9024537334159));
#304208=CARTESIAN_POINT('Ctrl Pts',(-2.1460587063946,-5.65936981510677,
-10.9762888294743));
#304209=CARTESIAN_POINT('Ctrl Pts',(-2.8773821779996,-5.32492488610066,
-11.0139900585689));
#304210=CARTESIAN_POINT('Ctrl Pts',(-4.15170856301579,-4.40092878990582,
-11.0846604461239));
#304211=CARTESIAN_POINT('Ctrl Pts',(-4.68668143124714,-3.82624308537361,
-11.1214198826724));
#304212=CARTESIAN_POINT('Ctrl Pts',(-5.50753211944379,-2.50447647075609,
-11.1946541847529));
#304213=CARTESIAN_POINT('Ctrl Pts',(-5.78554098360329,-1.76998424880603,
-11.2289697386716));
#304214=CARTESIAN_POINT('Ctrl Pts',(-6.04754045729825,-0.224586729143651,
-11.3019011552991));
#304215=CARTESIAN_POINT('Ctrl Pts',(-6.02460146093533,0.572181149457134,
-11.3395027493034));
#304216=CARTESIAN_POINT('Ctrl Pts',(-5.67509238313919,2.09566706085101,
-11.4114000988956));
#304217=CARTESIAN_POINT('Ctrl Pts',(-5.35789365274268,2.80917758532298,
-11.4461300445477));
#304218=CARTESIAN_POINT('Ctrl Pts',(-4.46238861113384,4.08736038724291,
-11.5197711795635));
#304219=CARTESIAN_POINT('Ctrl Pts',(-3.88835145901532,4.6368193454047,-11.5555998510682));
#304220=CARTESIAN_POINT('Ctrl Pts',(-2.56465550571106,5.4804292886302,-11.627313789211));
#304221=CARTESIAN_POINT('Ctrl Pts',(-1.8286808935447,5.76787930195984,-11.6645384323918));
#304222=CARTESIAN_POINT('Ctrl Pts',(-0.708218790008448,5.96866285305186,
-11.7177560974923));
#304223=CARTESIAN_POINT('Ctrl Pts',(-0.354058654631202,6.00000000000001,
-11.7341088261503));
#304224=CARTESIAN_POINT('Ctrl Pts',(-2.28983498828939E-15,6.00000000000001,
-11.75));
#304225=CARTESIAN_POINT('Origin',(0.,5.28128932132296E-15,28.75));
#304226=CARTESIAN_POINT('',(-1.90330186412546E-14,6.00000000000001,-8.03125));
#304227=CARTESIAN_POINT('',(-1.09203944922529E-13,6.00000000000001,-8.25));
#304228=CARTESIAN_POINT('',(-7.34788079488412E-16,6.00000000000001,28.75));
#304229=CARTESIAN_POINT('Ctrl Pts',(6.80011602582908E-15,6.00000000000001,
-9.78125));
#304230=CARTESIAN_POINT('Ctrl Pts',(-0.388602026377374,6.00000000000001,
-9.76380841997154));
#304231=CARTESIAN_POINT('Ctrl Pts',(-0.777166054444378,5.9622499020027,
-9.74581802315442));
#304232=CARTESIAN_POINT('Ctrl Pts',(-1.92676662500396,5.73568003297688,
-9.69091648912202));
#304233=CARTESIAN_POINT('Ctrl Pts',(-2.65652048244608,5.43630645796336,
-9.65379716608499));
#304234=CARTESIAN_POINT('Ctrl Pts',(-3.96683623993474,4.57025182575815,
-9.5823564513502));
#304235=CARTESIAN_POINT('Ctrl Pts',(-4.53303160142738,4.00932852398643,
-9.54608237298229));
#304236=CARTESIAN_POINT('Ctrl Pts',(-5.40684351104387,2.71370187661587,
-9.47237698684475));
#304237=CARTESIAN_POINT('Ctrl Pts',(-5.71125860824631,1.99491010941579,
-9.43789511054481));
#304238=CARTESIAN_POINT('Ctrl Pts',(-6.03348298153471,0.467052589512942,
-9.36579145312735));
#304239=CARTESIAN_POINT('Ctrl Pts',(-6.04260469747069,-0.328590751166323,
-9.32824292905656));
#304240=CARTESIAN_POINT('Ctrl Pts',(-5.75438844535648,-1.86936901721857,
-9.2555295072849));
#304241=CARTESIAN_POINT('Ctrl Pts',(-5.46315202926576,-2.60028471515326,
-9.22101519242572));
#304242=CARTESIAN_POINT('Ctrl Pts',(-4.61896599239245,-3.9074724955742,
-9.14769020261236));
#304243=CARTESIAN_POINT('Ctrl Pts',(-4.07495912894505,-4.471880200415,-9.11143100203713));
#304244=CARTESIAN_POINT('Ctrl Pts',(-2.78712718969374,-5.37251473323832,
-9.04049513571143));
#304245=CARTESIAN_POINT('Ctrl Pts',(-2.05158235279043,-5.69411111262987,
-9.00279181424585));
#304246=CARTESIAN_POINT('Ctrl Pts',(-0.518250505640008,-6.02750935739265,
-8.92910939967429));
#304247=CARTESIAN_POINT('Ctrl Pts',(0.263032496357224,-6.04402808210129,
-8.89508641893388));
#304248=CARTESIAN_POINT('Ctrl Pts',(1.79739454407277,-5.77776187457389,
-8.82233677486526));
#304249=CARTESIAN_POINT('Ctrl Pts',(2.53530645242296,-5.49412713587424,
-8.78508081966443));
#304250=CARTESIAN_POINT('Ctrl Pts',(3.86320679732842,-4.65767263690705,
-8.71328252652601));
#304251=CARTESIAN_POINT('Ctrl Pts',(4.4397120908807,-4.11184665082716,-8.67758508419934));
#304252=CARTESIAN_POINT('Ctrl Pts',(5.34206193972246,-2.83920041590143,
-8.60396546431831));
#304253=CARTESIAN_POINT('Ctrl Pts',(5.66330063348323,-2.1273680295604,-8.5691461518703));
#304254=CARTESIAN_POINT('Ctrl Pts',(6.02141876131934,-0.605321673871035,
-8.49731673873819));
#304255=CARTESIAN_POINT('Ctrl Pts',(6.04872666814296,0.191752635061683,
-8.45970068347199));
#304256=CARTESIAN_POINT('Ctrl Pts',(5.7950085307118,1.73855461207809,-8.38670298676888));
#304257=CARTESIAN_POINT('Ctrl Pts',(5.52116004088795,2.47416095481492,-8.35243964785031));
#304258=CARTESIAN_POINT('Ctrl Pts',(4.70772808498026,3.80037871309697,-8.27924119192351));
#304259=CARTESIAN_POINT('Ctrl Pts',(4.17564627581371,4.37831843098813,-8.24241615238277));
#304260=CARTESIAN_POINT('Ctrl Pts',(2.90649933401595,5.30896766302181,-8.17167922360083));
#304261=CARTESIAN_POINT('Ctrl Pts',(2.17768679266873,5.64719520584165,-8.13413593561579));
#304262=CARTESIAN_POINT('Ctrl Pts',(0.943246395536786,5.94432176111744,
-8.07439759373647));
#304263=CARTESIAN_POINT('Ctrl Pts',(0.471941141175927,6.00000000000001,
-8.05243207992706));
#304264=CARTESIAN_POINT('Ctrl Pts',(7.63278329429795E-15,6.00000000000001,
-8.03125));
#304265=CARTESIAN_POINT('Ctrl Pts',(-2.34257058195908E-13,6.00000000000001,
-8.25));
#304266=CARTESIAN_POINT('Ctrl Pts',(0.601647630917533,6.00000000000003,
-8.27700368137915));
#304267=CARTESIAN_POINT('Ctrl Pts',(1.20082592209495,5.9095079146255,-8.30521620791198));
#304268=CARTESIAN_POINT('Ctrl Pts',(2.52855355862817,5.49773655197143,-8.37081345366251));
#304269=CARTESIAN_POINT('Ctrl Pts',(3.22671330303811,5.11927365697742,-8.40655413950261));
#304270=CARTESIAN_POINT('Ctrl Pts',(4.4344121015205,4.11691443543296,-8.47832441230436));
#304271=CARTESIAN_POINT('Ctrl Pts',(4.93320525707645,3.50377324199252,-8.51557003339302));
#304272=CARTESIAN_POINT('Ctrl Pts',(5.66306913910022,2.12819291474537,-8.58833502833265));
#304273=CARTESIAN_POINT('Ctrl Pts',(5.8901663336146,1.3803946904201,-8.62235550546283));
#304274=CARTESIAN_POINT('Ctrl Pts',(6.04971570472001,-0.180546511890212,
-8.6960204697897));
#304275=CARTESIAN_POINT('Ctrl Pts',(5.97263858541093,-0.979461368579639,
-8.73372338539672));
#304276=CARTESIAN_POINT('Ctrl Pts',(5.51694325189492,-2.48317467545613,
-8.80468761322603));
#304277=CARTESIAN_POINT('Ctrl Pts',(5.14964343591734,-3.17555790368862,
-8.84089500505658));
#304278=CARTESIAN_POINT('Ctrl Pts',(4.16961317154647,-4.38430093711925,
-8.91422961085586));
#304279=CARTESIAN_POINT('Ctrl Pts',(3.56529066470427,-4.88840332562846,
-8.94876868456539));
#304280=CARTESIAN_POINT('Ctrl Pts',(2.19036461375986,-5.6411978714834,-9.02145758607322));
#304281=CARTESIAN_POINT('Ctrl Pts',(1.43143927045969,-5.87977906581147,
-9.05899965400121));
#304282=CARTESIAN_POINT('Ctrl Pts',(-0.12072927485402,-6.04843331813573,
-9.13112499737227));
#304283=CARTESIAN_POINT('Ctrl Pts',(-0.898524678529774,-5.98253848692881,
-9.16558302680733));
#304284=CARTESIAN_POINT('Ctrl Pts',(-2.40183152527019,-5.55470177551167,
-9.23929506037957));
#304285=CARTESIAN_POINT('Ctrl Pts',(-3.11118581935181,-5.19075376816449,
-9.27562041898045));
#304286=CARTESIAN_POINT('Ctrl Pts',(-4.34161915907198,-4.21433886457743,
-9.34703078329607));
#304287=CARTESIAN_POINT('Ctrl Pts',(-4.85285758834909,-3.61386310603759,
-9.38413806365142));
#304288=CARTESIAN_POINT('Ctrl Pts',(-5.61351687637761,-2.25597851663534,
-9.4570816796323));
#304289=CARTESIAN_POINT('Ctrl Pts',(-5.85773998176046,-1.51257877292681,
-9.49111738726339));
#304290=CARTESIAN_POINT('Ctrl Pts',(-6.05201376863221,0.0435386693816897,
-9.56455470553419));
#304291=CARTESIAN_POINT('Ctrl Pts',(-5.99330170963915,0.842125999098481,
-9.60224216427281));
#304292=CARTESIAN_POINT('Ctrl Pts',(-5.57352042624842,2.35301795961981,
-9.67354517184851));
#304293=CARTESIAN_POINT('Ctrl Pts',(-5.22323802825824,3.05265547123128,
-9.70916118036732));
#304294=CARTESIAN_POINT('Ctrl Pts',(-4.27183094512667,4.28517180180405,
-9.78260945995225));
#304295=CARTESIAN_POINT('Ctrl Pts',(-3.67771878891341,4.80475048924421,
-9.8175026488078));
#304296=CARTESIAN_POINT('Ctrl Pts',(-2.3199614111963,5.58889423094391,-9.88987814650373));
#304297=CARTESIAN_POINT('Ctrl Pts',(-1.56855801761912,5.84444793696307,
-9.92733012342345));
#304298=CARTESIAN_POINT('Ctrl Pts',(-0.527084730838563,5.98265377315508,
-9.9760899508761));
#304299=CARTESIAN_POINT('Ctrl Pts',(-0.263417336813236,6.,-9.98817706998664));
#304300=CARTESIAN_POINT('Ctrl Pts',(-1.62023172656234E-13,6.00000000000001,
-10.));
#304301=CARTESIAN_POINT('Origin',(0.,5.28128932132296E-15,28.75));
#304302=CARTESIAN_POINT('',(7.34788079488411E-16,6.,28.75));
#304303=CARTESIAN_POINT('Origin',(0.,5.28128932132296E-15,28.75));
#304304=CARTESIAN_POINT('',(-7.34788079488411E-16,6.,-6.25));
#304305=CARTESIAN_POINT('',(-7.34788079488412E-16,6.00000000000001,28.75));
#304306=CARTESIAN_POINT('',(-0.683563368987403,5.96093458449081,-6.25));
#304307=CARTESIAN_POINT('Origin',(0.,0.,-6.25));
#304308=CARTESIAN_POINT('',(-1.00356855195047E-13,6.00000000000001,-6.28124999999999));
#304309=CARTESIAN_POINT('Ctrl Pts',(-2.33216224110322E-13,6.00000000000001,
-6.28124999999999));
#304310=CARTESIAN_POINT('Ctrl Pts',(-0.227963499279154,6.,-6.27101834049654));
#304311=CARTESIAN_POINT('Ctrl Pts',(-0.456179827689892,5.98700953252767,
-6.26058588897497));
#304312=CARTESIAN_POINT('Ctrl Pts',(-0.683563368987794,5.96093458449077,
-6.24999999999997));
#304313=CARTESIAN_POINT('',(-3.94387125597461E-14,6.00000000000001,-6.50000000000001));
#304314=CARTESIAN_POINT('',(-7.34788079488412E-16,6.00000000000001,28.75));
#304315=CARTESIAN_POINT('Ctrl Pts',(-4.69368212308332,3.7375591135724,-6.24999999999999));
#304316=CARTESIAN_POINT('Ctrl Pts',(-4.40357806234582,4.10187609220501,
-6.27195673881733));
#304317=CARTESIAN_POINT('Ctrl Pts',(-4.07203711875145,4.43118894332342,
-6.29372645570828));
#304318=CARTESIAN_POINT('Ctrl Pts',(-3.34186406804379,5.0045981835736,-6.33587340548671));
#304319=CARTESIAN_POINT('Ctrl Pts',(-2.94615269925129,5.24731162971662,
-6.35679146205122));
#304320=CARTESIAN_POINT('Ctrl Pts',(-1.80697107584555,5.77616674464259,
-6.41563369018026));
#304321=CARTESIAN_POINT('Ctrl Pts',(-1.02830160855357,5.96422013354298,
-6.45332506752402));
#304322=CARTESIAN_POINT('Ctrl Pts',(-0.157047722683405,5.9984596369681,
-6.49292878150876));
#304323=CARTESIAN_POINT('Ctrl Pts',(-0.078495223191784,6.,-6.49647690793095));
#304324=CARTESIAN_POINT('Ctrl Pts',(-7.81426370400037E-14,6.00000000000001,
-6.50000000000001));
#304325=CARTESIAN_POINT('Origin',(0.,0.,-6.25));
#304326=CARTESIAN_POINT('Origin',(-3.81730450148946E-15,-2.22044604925031E-15,
-37.015625));
#304327=CARTESIAN_POINT('',(-4.41289208089522E-15,-4.86334165753294,-8.25));
#304328=CARTESIAN_POINT('',(-8.23019658238468E-15,-4.86334165753294,-37.015625));
#304329=CARTESIAN_POINT('Ctrl Pts',(-5.9558757940577E-16,-4.86334165753294,
-8.25));
#304330=CARTESIAN_POINT('Ctrl Pts',(0.887704914026675,-4.86334165753294,
-8.20084520853896));
#304331=CARTESIAN_POINT('Ctrl Pts',(1.71816547201427,-4.54972521023778,
-8.14921769586694));
#304332=CARTESIAN_POINT('Origin',(-3.81730450148946E-15,-2.22044604925031E-15,
-37.015625));
#304333=CARTESIAN_POINT('',(-4.41289208089522E-15,-4.86334165753294,-10.));
#304334=CARTESIAN_POINT('',(-4.41289208089522E-15,-4.86334165753294,-9.78125));
#304335=CARTESIAN_POINT('',(-8.23019658238468E-15,-4.86334165753294,-37.015625));
#304336=CARTESIAN_POINT('Ctrl Pts',(-5.9558757940577E-16,-4.86334165753294,
-10.));
#304337=CARTESIAN_POINT('Ctrl Pts',(1.58019549404244,-4.86334165753293,
-9.9125));
#304338=CARTESIAN_POINT('Ctrl Pts',(2.85860050315749,-3.93452605039577,
-9.825));
#304339=CARTESIAN_POINT('Ctrl Pts',(4.13700551227254,-3.0057104432586,-9.7375));
#304340=CARTESIAN_POINT('Ctrl Pts',(4.62531277436637,-1.5028552216293,-9.65));
#304341=CARTESIAN_POINT('Ctrl Pts',(5.1136200364602,2.01466554122251E-15,
-9.56249999999999));
#304342=CARTESIAN_POINT('Ctrl Pts',(4.62531277436638,1.5028552216293,-9.475));
#304343=CARTESIAN_POINT('Ctrl Pts',(4.13700551227254,3.00571044325861,-9.38749999999999));
#304344=CARTESIAN_POINT('Ctrl Pts',(2.8586005031575,3.93452605039578,-9.3));
#304345=CARTESIAN_POINT('Ctrl Pts',(1.58019549404244,4.86334165753294,-9.21249999999999));
#304346=CARTESIAN_POINT('Ctrl Pts',(0.,4.86334165753294,-9.125));
#304347=CARTESIAN_POINT('Ctrl Pts',(-1.58019549404244,4.86334165753294,
-9.03749999999999));
#304348=CARTESIAN_POINT('Ctrl Pts',(-2.8586005031575,3.93452605039578,-8.95));
#304349=CARTESIAN_POINT('Ctrl Pts',(-4.13700551227254,3.00571044325861,
-8.8625));
#304350=CARTESIAN_POINT('Ctrl Pts',(-4.62531277436637,1.5028552216293,-8.775));
#304351=CARTESIAN_POINT('Ctrl Pts',(-5.1136200364602,3.29446615486983E-15,
-8.6875));
#304352=CARTESIAN_POINT('Ctrl Pts',(-4.62531277436638,-1.5028552216293,
-8.6));
#304353=CARTESIAN_POINT('Ctrl Pts',(-4.13700551227254,-3.0057104432586,
-8.51249999999999));
#304354=CARTESIAN_POINT('Ctrl Pts',(-2.8586005031575,-3.93452605039577,
-8.425));
#304355=CARTESIAN_POINT('Ctrl Pts',(-1.58019549404244,-4.86334165753293,
-8.33749999999999));
#304356=CARTESIAN_POINT('Ctrl Pts',(-5.9558757940577E-16,-4.86334165753294,
-8.25));
#304357=CARTESIAN_POINT('Ctrl Pts',(-5.9558757940577E-16,-4.86334165753294,
-9.78125));
#304358=CARTESIAN_POINT('Ctrl Pts',(1.58019549404244,-4.86334165753293,
-9.69375));
#304359=CARTESIAN_POINT('Ctrl Pts',(2.85860050315749,-3.93452605039577,
-9.60625));
#304360=CARTESIAN_POINT('Ctrl Pts',(4.13700551227254,-3.0057104432586,-9.51875));
#304361=CARTESIAN_POINT('Ctrl Pts',(4.62531277436637,-1.5028552216293,-9.43125));
#304362=CARTESIAN_POINT('Ctrl Pts',(5.1136200364602,2.021496774149E-15,
-9.34375000000001));
#304363=CARTESIAN_POINT('Ctrl Pts',(4.62531277436638,1.5028552216293,-9.25625));
#304364=CARTESIAN_POINT('Ctrl Pts',(4.13700551227254,3.00571044325861,-9.16875000000001));
#304365=CARTESIAN_POINT('Ctrl Pts',(2.8586005031575,3.93452605039578,-9.08125));
#304366=CARTESIAN_POINT('Ctrl Pts',(1.58019549404244,4.86334165753294,-8.99375000000001));
#304367=CARTESIAN_POINT('Ctrl Pts',(0.,4.86334165753294,-8.90625));
#304368=CARTESIAN_POINT('Ctrl Pts',(-1.58019549404244,4.86334165753294,
-8.81875));
#304369=CARTESIAN_POINT('Ctrl Pts',(-2.8586005031575,3.93452605039578,-8.73125));
#304370=CARTESIAN_POINT('Ctrl Pts',(-4.13700551227254,3.00571044325861,
-8.64375));
#304371=CARTESIAN_POINT('Ctrl Pts',(-4.62531277436637,1.5028552216293,-8.55625));
#304372=CARTESIAN_POINT('Ctrl Pts',(-5.1136200364602,3.30129738779633E-15,
-8.46875000000001));
#304373=CARTESIAN_POINT('Ctrl Pts',(-4.62531277436638,-1.5028552216293,
-8.38125));
#304374=CARTESIAN_POINT('Ctrl Pts',(-4.13700551227254,-3.0057104432586,
-8.29375000000001));
#304375=CARTESIAN_POINT('Ctrl Pts',(-2.8586005031575,-3.93452605039577,
-8.20625));
#304376=CARTESIAN_POINT('Ctrl Pts',(-2.45120890801561,-4.23051336981829,
-8.1783662195699));
#304377=CARTESIAN_POINT('Ctrl Pts',(-1.99181552565186,-4.4367514004807,
-8.14921769587173));
#304378=CARTESIAN_POINT('Origin',(-3.81730450148946E-15,-2.22044604925031E-15,
-37.015625));
#304379=CARTESIAN_POINT('',(-4.41289208089522E-15,-4.86334165753294,-11.75));
#304380=CARTESIAN_POINT('',(-4.41289208089522E-15,-4.86334165753294,-11.53125));
#304381=CARTESIAN_POINT('',(-8.23019658238468E-15,-4.86334165753294,-37.015625));
#304382=CARTESIAN_POINT('Ctrl Pts',(-5.9558757940577E-16,-4.86334165753294,
-11.75));
#304383=CARTESIAN_POINT('Ctrl Pts',(1.58019549404244,-4.86334165753293,
-11.6625));
#304384=CARTESIAN_POINT('Ctrl Pts',(2.85860050315749,-3.93452605039577,
-11.575));
#304385=CARTESIAN_POINT('Ctrl Pts',(4.13700551227254,-3.0057104432586,-11.4875));
#304386=CARTESIAN_POINT('Ctrl Pts',(4.62531277436637,-1.5028552216293,-11.4));
#304387=CARTESIAN_POINT('Ctrl Pts',(5.1136200364602,1.96001567781056E-15,
-11.3125));
#304388=CARTESIAN_POINT('Ctrl Pts',(4.62531277436638,1.5028552216293,-11.225));
#304389=CARTESIAN_POINT('Ctrl Pts',(4.13700551227254,3.00571044325861,-11.1375));
#304390=CARTESIAN_POINT('Ctrl Pts',(2.8586005031575,3.93452605039578,-11.05));
#304391=CARTESIAN_POINT('Ctrl Pts',(1.58019549404244,4.86334165753294,-10.9625));
#304392=CARTESIAN_POINT('Ctrl Pts',(0.,4.86334165753294,-10.875));
#304393=CARTESIAN_POINT('Ctrl Pts',(-1.58019549404244,4.86334165753294,
-10.7875));
#304394=CARTESIAN_POINT('Ctrl Pts',(-2.8586005031575,3.93452605039578,-10.7));
#304395=CARTESIAN_POINT('Ctrl Pts',(-4.13700551227254,3.00571044325861,
-10.6125));
#304396=CARTESIAN_POINT('Ctrl Pts',(-4.62531277436637,1.5028552216293,-10.525));
#304397=CARTESIAN_POINT('Ctrl Pts',(-5.1136200364602,3.23981629145788E-15,
-10.4375));
#304398=CARTESIAN_POINT('Ctrl Pts',(-4.62531277436638,-1.5028552216293,
-10.35));
#304399=CARTESIAN_POINT('Ctrl Pts',(-4.13700551227254,-3.0057104432586,
-10.2625));
#304400=CARTESIAN_POINT('Ctrl Pts',(-2.8586005031575,-3.93452605039577,
-10.175));
#304401=CARTESIAN_POINT('Ctrl Pts',(-1.58019549404244,-4.86334165753293,
-10.0875));
#304402=CARTESIAN_POINT('Ctrl Pts',(-5.9558757940577E-16,-4.86334165753294,
-10.));
#304403=CARTESIAN_POINT('Ctrl Pts',(-5.9558757940577E-16,-4.86334165753294,
-11.53125));
#304404=CARTESIAN_POINT('Ctrl Pts',(1.58019549404244,-4.86334165753293,
-11.44375));
#304405=CARTESIAN_POINT('Ctrl Pts',(2.85860050315749,-3.93452605039577,
-11.35625));
#304406=CARTESIAN_POINT('Ctrl Pts',(4.13700551227254,-3.0057104432586,-11.26875));
#304407=CARTESIAN_POINT('Ctrl Pts',(4.62531277436637,-1.5028552216293,-11.18125));
#304408=CARTESIAN_POINT('Ctrl Pts',(5.1136200364602,1.96684691073705E-15,
-11.09375));
#304409=CARTESIAN_POINT('Ctrl Pts',(4.62531277436638,1.5028552216293,-11.00625));
#304410=CARTESIAN_POINT('Ctrl Pts',(4.13700551227254,3.00571044325861,-10.91875));
#304411=CARTESIAN_POINT('Ctrl Pts',(2.8586005031575,3.93452605039578,-10.83125));
#304412=CARTESIAN_POINT('Ctrl Pts',(1.58019549404244,4.86334165753294,-10.74375));
#304413=CARTESIAN_POINT('Ctrl Pts',(0.,4.86334165753294,-10.65625));
#304414=CARTESIAN_POINT('Ctrl Pts',(-1.58019549404244,4.86334165753294,
-10.56875));
#304415=CARTESIAN_POINT('Ctrl Pts',(-2.8586005031575,3.93452605039578,-10.48125));
#304416=CARTESIAN_POINT('Ctrl Pts',(-4.13700551227254,3.00571044325861,
-10.39375));
#304417=CARTESIAN_POINT('Ctrl Pts',(-4.62531277436637,1.5028552216293,-10.30625));
#304418=CARTESIAN_POINT('Ctrl Pts',(-5.1136200364602,3.24664752438437E-15,
-10.21875));
#304419=CARTESIAN_POINT('Ctrl Pts',(-4.62531277436638,-1.5028552216293,
-10.13125));
#304420=CARTESIAN_POINT('Ctrl Pts',(-4.13700551227254,-3.0057104432586,
-10.04375));
#304421=CARTESIAN_POINT('Ctrl Pts',(-2.8586005031575,-3.93452605039577,
-9.95625));
#304422=CARTESIAN_POINT('Ctrl Pts',(-1.58019549404244,-4.86334165753293,
-9.86875));
#304423=CARTESIAN_POINT('Ctrl Pts',(-5.9558757940577E-16,-4.86334165753294,
-9.78125));
#304424=CARTESIAN_POINT('Origin',(-3.81730450148946E-15,-2.22044604925031E-15,
-37.015625));
#304425=CARTESIAN_POINT('',(-4.41289208089522E-15,-4.86334165753294,-13.5));
#304426=CARTESIAN_POINT('',(-4.41289208089522E-15,-4.86334165753294,-13.28125));
#304427=CARTESIAN_POINT('',(-8.23019658238468E-15,-4.86334165753294,-37.015625));
#304428=CARTESIAN_POINT('Ctrl Pts',(-5.9558757940577E-16,-4.86334165753294,
-13.5));
#304429=CARTESIAN_POINT('Ctrl Pts',(1.58019549404244,-4.86334165753293,
-13.4125));
#304430=CARTESIAN_POINT('Ctrl Pts',(2.85860050315749,-3.93452605039577,
-13.325));
#304431=CARTESIAN_POINT('Ctrl Pts',(4.13700551227254,-3.0057104432586,-13.2375));
#304432=CARTESIAN_POINT('Ctrl Pts',(4.62531277436637,-1.5028552216293,-13.15));
#304433=CARTESIAN_POINT('Ctrl Pts',(5.1136200364602,1.90536581439861E-15,
-13.0625));
#304434=CARTESIAN_POINT('Ctrl Pts',(4.62531277436638,1.5028552216293,-12.975));
#304435=CARTESIAN_POINT('Ctrl Pts',(4.13700551227254,3.00571044325861,-12.8875));
#304436=CARTESIAN_POINT('Ctrl Pts',(2.8586005031575,3.93452605039578,-12.8));
#304437=CARTESIAN_POINT('Ctrl Pts',(1.58019549404244,4.86334165753294,-12.7125));
#304438=CARTESIAN_POINT('Ctrl Pts',(0.,4.86334165753294,-12.625));
#304439=CARTESIAN_POINT('Ctrl Pts',(-1.58019549404244,4.86334165753294,
-12.5375));
#304440=CARTESIAN_POINT('Ctrl Pts',(-2.8586005031575,3.93452605039578,-12.45));
#304441=CARTESIAN_POINT('Ctrl Pts',(-4.13700551227254,3.00571044325861,
-12.3625));
#304442=CARTESIAN_POINT('Ctrl Pts',(-4.62531277436637,1.5028552216293,-12.275));
#304443=CARTESIAN_POINT('Ctrl Pts',(-5.1136200364602,3.18516642804593E-15,
-12.1875));
#304444=CARTESIAN_POINT('Ctrl Pts',(-4.62531277436638,-1.5028552216293,
-12.1));
#304445=CARTESIAN_POINT('Ctrl Pts',(-4.13700551227254,-3.0057104432586,
-12.0125));
#304446=CARTESIAN_POINT('Ctrl Pts',(-2.8586005031575,-3.93452605039577,
-11.925));
#304447=CARTESIAN_POINT('Ctrl Pts',(-1.58019549404244,-4.86334165753293,
-11.8375));
#304448=CARTESIAN_POINT('Ctrl Pts',(-5.9558757940577E-16,-4.86334165753294,
-11.75));
#304449=CARTESIAN_POINT('Ctrl Pts',(-5.9558757940577E-16,-4.86334165753294,
-13.28125));
#304450=CARTESIAN_POINT('Ctrl Pts',(1.58019549404244,-4.86334165753293,
-13.19375));
#304451=CARTESIAN_POINT('Ctrl Pts',(2.85860050315749,-3.93452605039577,
-13.10625));
#304452=CARTESIAN_POINT('Ctrl Pts',(4.13700551227254,-3.0057104432586,-13.01875));
#304453=CARTESIAN_POINT('Ctrl Pts',(4.62531277436637,-1.5028552216293,-12.93125));
#304454=CARTESIAN_POINT('Ctrl Pts',(5.1136200364602,1.9121970473251E-15,
-12.84375));
#304455=CARTESIAN_POINT('Ctrl Pts',(4.62531277436638,1.5028552216293,-12.75625));
#304456=CARTESIAN_POINT('Ctrl Pts',(4.13700551227254,3.00571044325861,-12.66875));
#304457=CARTESIAN_POINT('Ctrl Pts',(2.8586005031575,3.93452605039578,-12.58125));
#304458=CARTESIAN_POINT('Ctrl Pts',(1.58019549404244,4.86334165753294,-12.49375));
#304459=CARTESIAN_POINT('Ctrl Pts',(0.,4.86334165753294,-12.40625));
#304460=CARTESIAN_POINT('Ctrl Pts',(-1.58019549404244,4.86334165753294,
-12.31875));
#304461=CARTESIAN_POINT('Ctrl Pts',(-2.8586005031575,3.93452605039578,-12.23125));
#304462=CARTESIAN_POINT('Ctrl Pts',(-4.13700551227254,3.00571044325861,
-12.14375));
#304463=CARTESIAN_POINT('Ctrl Pts',(-4.62531277436637,1.5028552216293,-12.05625));
#304464=CARTESIAN_POINT('Ctrl Pts',(-5.1136200364602,3.19199766097243E-15,
-11.96875));
#304465=CARTESIAN_POINT('Ctrl Pts',(-4.62531277436638,-1.5028552216293,
-11.88125));
#304466=CARTESIAN_POINT('Ctrl Pts',(-4.13700551227254,-3.0057104432586,
-11.79375));
#304467=CARTESIAN_POINT('Ctrl Pts',(-2.8586005031575,-3.93452605039577,
-11.70625));
#304468=CARTESIAN_POINT('Ctrl Pts',(-1.58019549404244,-4.86334165753293,
-11.61875));
#304469=CARTESIAN_POINT('Ctrl Pts',(-5.9558757940577E-16,-4.86334165753294,
-11.53125));
#304470=CARTESIAN_POINT('Origin',(-3.81730450148946E-15,-2.22044604925031E-15,
-37.015625));
#304471=CARTESIAN_POINT('',(-4.41289208089522E-15,-4.86334165753294,-15.25));
#304472=CARTESIAN_POINT('',(-4.41289208089522E-15,-4.86334165753294,-15.03125));
#304473=CARTESIAN_POINT('',(-8.23019658238468E-15,-4.86334165753294,-37.015625));
#304474=CARTESIAN_POINT('Ctrl Pts',(-5.9558757940577E-16,-4.86334165753294,
-15.25));
#304475=CARTESIAN_POINT('Ctrl Pts',(1.58019549404244,-4.86334165753293,
-15.1625));
#304476=CARTESIAN_POINT('Ctrl Pts',(2.85860050315749,-3.93452605039577,
-15.075));
#304477=CARTESIAN_POINT('Ctrl Pts',(4.13700551227254,-3.0057104432586,-14.9875));
#304478=CARTESIAN_POINT('Ctrl Pts',(4.62531277436637,-1.5028552216293,-14.9));
#304479=CARTESIAN_POINT('Ctrl Pts',(5.1136200364602,1.85071595098665E-15,
-14.8125));
#304480=CARTESIAN_POINT('Ctrl Pts',(4.62531277436638,1.5028552216293,-14.725));
#304481=CARTESIAN_POINT('Ctrl Pts',(4.13700551227254,3.00571044325861,-14.6375));
#304482=CARTESIAN_POINT('Ctrl Pts',(2.8586005031575,3.93452605039578,-14.55));
#304483=CARTESIAN_POINT('Ctrl Pts',(1.58019549404244,4.86334165753294,-14.4625));
#304484=CARTESIAN_POINT('Ctrl Pts',(0.,4.86334165753294,-14.375));
#304485=CARTESIAN_POINT('Ctrl Pts',(-1.58019549404244,4.86334165753294,
-14.2875));
#304486=CARTESIAN_POINT('Ctrl Pts',(-2.8586005031575,3.93452605039578,-14.2));
#304487=CARTESIAN_POINT('Ctrl Pts',(-4.13700551227254,3.00571044325861,
-14.1125));
#304488=CARTESIAN_POINT('Ctrl Pts',(-4.62531277436637,1.5028552216293,-14.025));
#304489=CARTESIAN_POINT('Ctrl Pts',(-5.1136200364602,3.13051656463398E-15,
-13.9375));
#304490=CARTESIAN_POINT('Ctrl Pts',(-4.62531277436638,-1.5028552216293,
-13.85));
#304491=CARTESIAN_POINT('Ctrl Pts',(-4.13700551227254,-3.0057104432586,
-13.7625));
#304492=CARTESIAN_POINT('Ctrl Pts',(-2.8586005031575,-3.93452605039577,
-13.675));
#304493=CARTESIAN_POINT('Ctrl Pts',(-1.58019549404244,-4.86334165753293,
-13.5875));
#304494=CARTESIAN_POINT('Ctrl Pts',(-5.9558757940577E-16,-4.86334165753294,
-13.5));
#304495=CARTESIAN_POINT('Ctrl Pts',(-5.9558757940577E-16,-4.86334165753294,
-15.03125));
#304496=CARTESIAN_POINT('Ctrl Pts',(1.58019549404244,-4.86334165753293,
-14.94375));
#304497=CARTESIAN_POINT('Ctrl Pts',(2.85860050315749,-3.93452605039577,
-14.85625));
#304498=CARTESIAN_POINT('Ctrl Pts',(4.13700551227254,-3.0057104432586,-14.76875));
#304499=CARTESIAN_POINT('Ctrl Pts',(4.62531277436637,-1.5028552216293,-14.68125));
#304500=CARTESIAN_POINT('Ctrl Pts',(5.1136200364602,1.85754718391315E-15,
-14.59375));
#304501=CARTESIAN_POINT('Ctrl Pts',(4.62531277436638,1.5028552216293,-14.50625));
#304502=CARTESIAN_POINT('Ctrl Pts',(4.13700551227254,3.00571044325861,-14.41875));
#304503=CARTESIAN_POINT('Ctrl Pts',(2.8586005031575,3.93452605039578,-14.33125));
#304504=CARTESIAN_POINT('Ctrl Pts',(1.58019549404244,4.86334165753294,-14.24375));
#304505=CARTESIAN_POINT('Ctrl Pts',(0.,4.86334165753294,-14.15625));
#304506=CARTESIAN_POINT('Ctrl Pts',(-1.58019549404244,4.86334165753294,
-14.06875));
#304507=CARTESIAN_POINT('Ctrl Pts',(-2.8586005031575,3.93452605039578,-13.98125));
#304508=CARTESIAN_POINT('Ctrl Pts',(-4.13700551227254,3.00571044325861,
-13.89375));
#304509=CARTESIAN_POINT('Ctrl Pts',(-4.62531277436637,1.5028552216293,-13.80625));
#304510=CARTESIAN_POINT('Ctrl Pts',(-5.1136200364602,3.13734779756048E-15,
-13.71875));
#304511=CARTESIAN_POINT('Ctrl Pts',(-4.62531277436638,-1.5028552216293,
-13.63125));
#304512=CARTESIAN_POINT('Ctrl Pts',(-4.13700551227254,-3.0057104432586,
-13.54375));
#304513=CARTESIAN_POINT('Ctrl Pts',(-2.8586005031575,-3.93452605039577,
-13.45625));
#304514=CARTESIAN_POINT('Ctrl Pts',(-1.58019549404244,-4.86334165753293,
-13.36875));
#304515=CARTESIAN_POINT('Ctrl Pts',(-5.9558757940577E-16,-4.86334165753294,
-13.28125));
#304516=CARTESIAN_POINT('Origin',(-3.81730450148946E-15,-2.22044604925031E-15,
-37.015625));
#304517=CARTESIAN_POINT('',(-4.41289208089522E-15,-4.86334165753294,-17.));
#304518=CARTESIAN_POINT('',(-4.41289208089522E-15,-4.86334165753294,-16.78125));
#304519=CARTESIAN_POINT('',(-8.23019658238468E-15,-4.86334165753294,-37.015625));
#304520=CARTESIAN_POINT('Ctrl Pts',(-5.9558757940577E-16,-4.86334165753294,
-17.));
#304521=CARTESIAN_POINT('Ctrl Pts',(1.58019549404244,-4.86334165753293,
-16.9125));
#304522=CARTESIAN_POINT('Ctrl Pts',(2.85860050315749,-3.93452605039577,
-16.825));
#304523=CARTESIAN_POINT('Ctrl Pts',(4.13700551227254,-3.0057104432586,-16.7375));
#304524=CARTESIAN_POINT('Ctrl Pts',(4.62531277436637,-1.5028552216293,-16.65));
#304525=CARTESIAN_POINT('Ctrl Pts',(5.1136200364602,1.7960660875747E-15,
-16.5625));
#304526=CARTESIAN_POINT('Ctrl Pts',(4.62531277436638,1.5028552216293,-16.475));
#304527=CARTESIAN_POINT('Ctrl Pts',(4.13700551227254,3.00571044325861,-16.3875));
#304528=CARTESIAN_POINT('Ctrl Pts',(2.8586005031575,3.93452605039578,-16.3));
#304529=CARTESIAN_POINT('Ctrl Pts',(1.58019549404244,4.86334165753294,-16.2125));
#304530=CARTESIAN_POINT('Ctrl Pts',(0.,4.86334165753294,-16.125));
#304531=CARTESIAN_POINT('Ctrl Pts',(-1.58019549404244,4.86334165753294,
-16.0375));
#304532=CARTESIAN_POINT('Ctrl Pts',(-2.8586005031575,3.93452605039578,-15.95));
#304533=CARTESIAN_POINT('Ctrl Pts',(-4.13700551227254,3.00571044325861,
-15.8625));
#304534=CARTESIAN_POINT('Ctrl Pts',(-4.62531277436637,1.5028552216293,-15.775));
#304535=CARTESIAN_POINT('Ctrl Pts',(-5.1136200364602,3.07586670122203E-15,
-15.6875));
#304536=CARTESIAN_POINT('Ctrl Pts',(-4.62531277436638,-1.5028552216293,
-15.6));
#304537=CARTESIAN_POINT('Ctrl Pts',(-4.13700551227254,-3.0057104432586,
-15.5125));
#304538=CARTESIAN_POINT('Ctrl Pts',(-2.8586005031575,-3.93452605039577,
-15.425));
#304539=CARTESIAN_POINT('Ctrl Pts',(-1.58019549404244,-4.86334165753293,
-15.3375));
#304540=CARTESIAN_POINT('Ctrl Pts',(-5.9558757940577E-16,-4.86334165753294,
-15.25));
#304541=CARTESIAN_POINT('Ctrl Pts',(-5.9558757940577E-16,-4.86334165753294,
-16.78125));
#304542=CARTESIAN_POINT('Ctrl Pts',(1.58019549404244,-4.86334165753293,
-16.69375));
#304543=CARTESIAN_POINT('Ctrl Pts',(2.85860050315749,-3.93452605039577,
-16.60625));
#304544=CARTESIAN_POINT('Ctrl Pts',(4.13700551227254,-3.0057104432586,-16.51875));
#304545=CARTESIAN_POINT('Ctrl Pts',(4.62531277436637,-1.5028552216293,-16.43125));
#304546=CARTESIAN_POINT('Ctrl Pts',(5.1136200364602,1.8028973205012E-15,
-16.34375));
#304547=CARTESIAN_POINT('Ctrl Pts',(4.62531277436638,1.5028552216293,-16.25625));
#304548=CARTESIAN_POINT('Ctrl Pts',(4.13700551227254,3.00571044325861,-16.16875));
#304549=CARTESIAN_POINT('Ctrl Pts',(2.8586005031575,3.93452605039578,-16.08125));
#304550=CARTESIAN_POINT('Ctrl Pts',(1.58019549404244,4.86334165753294,-15.99375));
#304551=CARTESIAN_POINT('Ctrl Pts',(0.,4.86334165753294,-15.90625));
#304552=CARTESIAN_POINT('Ctrl Pts',(-1.58019549404244,4.86334165753294,
-15.81875));
#304553=CARTESIAN_POINT('Ctrl Pts',(-2.8586005031575,3.93452605039578,-15.73125));
#304554=CARTESIAN_POINT('Ctrl Pts',(-4.13700551227254,3.00571044325861,
-15.64375));
#304555=CARTESIAN_POINT('Ctrl Pts',(-4.62531277436637,1.5028552216293,-15.55625));
#304556=CARTESIAN_POINT('Ctrl Pts',(-5.1136200364602,3.08269793414853E-15,
-15.46875));
#304557=CARTESIAN_POINT('Ctrl Pts',(-4.62531277436638,-1.5028552216293,
-15.38125));
#304558=CARTESIAN_POINT('Ctrl Pts',(-4.13700551227254,-3.0057104432586,
-15.29375));
#304559=CARTESIAN_POINT('Ctrl Pts',(-2.8586005031575,-3.93452605039577,
-15.20625));
#304560=CARTESIAN_POINT('Ctrl Pts',(-1.58019549404244,-4.86334165753293,
-15.11875));
#304561=CARTESIAN_POINT('Ctrl Pts',(-5.9558757940577E-16,-4.86334165753294,
-15.03125));
#304562=CARTESIAN_POINT('Origin',(-3.81730450148946E-15,-2.22044604925031E-15,
-37.015625));
#304563=CARTESIAN_POINT('',(-4.41289208089522E-15,-4.86334165753294,-18.75));
#304564=CARTESIAN_POINT('',(-4.41289208089522E-15,-4.86334165753294,-18.53125));
#304565=CARTESIAN_POINT('',(-8.23019658238468E-15,-4.86334165753294,-37.015625));
#304566=CARTESIAN_POINT('Ctrl Pts',(-5.9558757940577E-16,-4.86334165753294,
-18.75));
#304567=CARTESIAN_POINT('Ctrl Pts',(1.58019549404244,-4.86334165753293,
-18.6625));
#304568=CARTESIAN_POINT('Ctrl Pts',(2.85860050315749,-3.93452605039577,
-18.575));
#304569=CARTESIAN_POINT('Ctrl Pts',(4.13700551227254,-3.0057104432586,-18.4875));
#304570=CARTESIAN_POINT('Ctrl Pts',(4.62531277436637,-1.5028552216293,-18.4));
#304571=CARTESIAN_POINT('Ctrl Pts',(5.1136200364602,1.74141622416275E-15,
-18.3125));
#304572=CARTESIAN_POINT('Ctrl Pts',(4.62531277436638,1.5028552216293,-18.225));
#304573=CARTESIAN_POINT('Ctrl Pts',(4.13700551227254,3.00571044325861,-18.1375));
#304574=CARTESIAN_POINT('Ctrl Pts',(2.8586005031575,3.93452605039578,-18.05));
#304575=CARTESIAN_POINT('Ctrl Pts',(1.58019549404244,4.86334165753294,-17.9625));
#304576=CARTESIAN_POINT('Ctrl Pts',(0.,4.86334165753294,-17.875));
#304577=CARTESIAN_POINT('Ctrl Pts',(-1.58019549404244,4.86334165753294,
-17.7875));
#304578=CARTESIAN_POINT('Ctrl Pts',(-2.8586005031575,3.93452605039578,-17.7));
#304579=CARTESIAN_POINT('Ctrl Pts',(-4.13700551227254,3.00571044325861,
-17.6125));
#304580=CARTESIAN_POINT('Ctrl Pts',(-4.62531277436637,1.5028552216293,-17.525));
#304581=CARTESIAN_POINT('Ctrl Pts',(-5.1136200364602,3.02121683781008E-15,
-17.4375));
#304582=CARTESIAN_POINT('Ctrl Pts',(-4.62531277436638,-1.5028552216293,
-17.35));
#304583=CARTESIAN_POINT('Ctrl Pts',(-4.13700551227254,-3.0057104432586,
-17.2625));
#304584=CARTESIAN_POINT('Ctrl Pts',(-2.8586005031575,-3.93452605039577,
-17.175));
#304585=CARTESIAN_POINT('Ctrl Pts',(-1.58019549404244,-4.86334165753293,
-17.0875));
#304586=CARTESIAN_POINT('Ctrl Pts',(-5.9558757940577E-16,-4.86334165753294,
-17.));
#304587=CARTESIAN_POINT('Ctrl Pts',(-5.9558757940577E-16,-4.86334165753294,
-18.53125));
#304588=CARTESIAN_POINT('Ctrl Pts',(1.58019549404244,-4.86334165753293,
-18.44375));
#304589=CARTESIAN_POINT('Ctrl Pts',(2.85860050315749,-3.93452605039577,
-18.35625));
#304590=CARTESIAN_POINT('Ctrl Pts',(4.13700551227254,-3.0057104432586,-18.26875));
#304591=CARTESIAN_POINT('Ctrl Pts',(4.62531277436637,-1.5028552216293,-18.18125));
#304592=CARTESIAN_POINT('Ctrl Pts',(5.1136200364602,1.74824745708925E-15,
-18.09375));
#304593=CARTESIAN_POINT('Ctrl Pts',(4.62531277436638,1.5028552216293,-18.00625));
#304594=CARTESIAN_POINT('Ctrl Pts',(4.13700551227254,3.00571044325861,-17.91875));
#304595=CARTESIAN_POINT('Ctrl Pts',(2.8586005031575,3.93452605039578,-17.83125));
#304596=CARTESIAN_POINT('Ctrl Pts',(1.58019549404244,4.86334165753294,-17.74375));
#304597=CARTESIAN_POINT('Ctrl Pts',(0.,4.86334165753294,-17.65625));
#304598=CARTESIAN_POINT('Ctrl Pts',(-1.58019549404244,4.86334165753294,
-17.56875));
#304599=CARTESIAN_POINT('Ctrl Pts',(-2.8586005031575,3.93452605039578,-17.48125));
#304600=CARTESIAN_POINT('Ctrl Pts',(-4.13700551227254,3.00571044325861,
-17.39375));
#304601=CARTESIAN_POINT('Ctrl Pts',(-4.62531277436637,1.5028552216293,-17.30625));
#304602=CARTESIAN_POINT('Ctrl Pts',(-5.1136200364602,3.02804807073658E-15,
-17.21875));
#304603=CARTESIAN_POINT('Ctrl Pts',(-4.62531277436638,-1.5028552216293,
-17.13125));
#304604=CARTESIAN_POINT('Ctrl Pts',(-4.13700551227254,-3.0057104432586,
-17.04375));
#304605=CARTESIAN_POINT('Ctrl Pts',(-2.8586005031575,-3.93452605039577,
-16.95625));
#304606=CARTESIAN_POINT('Ctrl Pts',(-1.58019549404244,-4.86334165753293,
-16.86875));
#304607=CARTESIAN_POINT('Ctrl Pts',(-5.9558757940577E-16,-4.86334165753294,
-16.78125));
#304608=CARTESIAN_POINT('Origin',(-3.81730450148946E-15,-2.22044604925031E-15,
-37.015625));
#304609=CARTESIAN_POINT('',(-4.41289208089522E-15,-4.86334165753294,-20.5));
#304610=CARTESIAN_POINT('',(-4.41289208089522E-15,-4.86334165753294,-20.28125));
#304611=CARTESIAN_POINT('',(-8.23019658238468E-15,-4.86334165753294,-37.015625));
#304612=CARTESIAN_POINT('Ctrl Pts',(-5.9558757940577E-16,-4.86334165753294,
-20.5));
#304613=CARTESIAN_POINT('Ctrl Pts',(1.58019549404244,-4.86334165753293,
-20.4125));
#304614=CARTESIAN_POINT('Ctrl Pts',(2.85860050315749,-3.93452605039577,
-20.325));
#304615=CARTESIAN_POINT('Ctrl Pts',(4.13700551227254,-3.0057104432586,-20.2375));
#304616=CARTESIAN_POINT('Ctrl Pts',(4.62531277436637,-1.5028552216293,-20.15));
#304617=CARTESIAN_POINT('Ctrl Pts',(5.1136200364602,1.6867663607508E-15,
-20.0625));
#304618=CARTESIAN_POINT('Ctrl Pts',(4.62531277436638,1.5028552216293,-19.975));
#304619=CARTESIAN_POINT('Ctrl Pts',(4.13700551227254,3.00571044325861,-19.8875));
#304620=CARTESIAN_POINT('Ctrl Pts',(2.8586005031575,3.93452605039578,-19.8));
#304621=CARTESIAN_POINT('Ctrl Pts',(1.58019549404244,4.86334165753294,-19.7125));
#304622=CARTESIAN_POINT('Ctrl Pts',(0.,4.86334165753294,-19.625));
#304623=CARTESIAN_POINT('Ctrl Pts',(-1.58019549404244,4.86334165753294,
-19.5375));
#304624=CARTESIAN_POINT('Ctrl Pts',(-2.8586005031575,3.93452605039578,-19.45));
#304625=CARTESIAN_POINT('Ctrl Pts',(-4.13700551227254,3.00571044325861,
-19.3625));
#304626=CARTESIAN_POINT('Ctrl Pts',(-4.62531277436637,1.5028552216293,-19.275));
#304627=CARTESIAN_POINT('Ctrl Pts',(-5.1136200364602,2.96656697439813E-15,
-19.1875));
#304628=CARTESIAN_POINT('Ctrl Pts',(-4.62531277436638,-1.5028552216293,
-19.1));
#304629=CARTESIAN_POINT('Ctrl Pts',(-4.13700551227254,-3.0057104432586,
-19.0125));
#304630=CARTESIAN_POINT('Ctrl Pts',(-2.8586005031575,-3.93452605039577,
-18.925));
#304631=CARTESIAN_POINT('Ctrl Pts',(-1.58019549404244,-4.86334165753293,
-18.8375));
#304632=CARTESIAN_POINT('Ctrl Pts',(-5.9558757940577E-16,-4.86334165753294,
-18.75));
#304633=CARTESIAN_POINT('Ctrl Pts',(-5.9558757940577E-16,-4.86334165753294,
-20.28125));
#304634=CARTESIAN_POINT('Ctrl Pts',(1.58019549404244,-4.86334165753293,
-20.19375));
#304635=CARTESIAN_POINT('Ctrl Pts',(2.85860050315749,-3.93452605039577,
-20.10625));
#304636=CARTESIAN_POINT('Ctrl Pts',(4.13700551227254,-3.0057104432586,-20.01875));
#304637=CARTESIAN_POINT('Ctrl Pts',(4.62531277436637,-1.5028552216293,-19.93125));
#304638=CARTESIAN_POINT('Ctrl Pts',(5.1136200364602,1.6935975936773E-15,
-19.84375));
#304639=CARTESIAN_POINT('Ctrl Pts',(4.62531277436638,1.5028552216293,-19.75625));
#304640=CARTESIAN_POINT('Ctrl Pts',(4.13700551227254,3.00571044325861,-19.66875));
#304641=CARTESIAN_POINT('Ctrl Pts',(2.8586005031575,3.93452605039578,-19.58125));
#304642=CARTESIAN_POINT('Ctrl Pts',(1.58019549404244,4.86334165753294,-19.49375));
#304643=CARTESIAN_POINT('Ctrl Pts',(0.,4.86334165753294,-19.40625));
#304644=CARTESIAN_POINT('Ctrl Pts',(-1.58019549404244,4.86334165753294,
-19.31875));
#304645=CARTESIAN_POINT('Ctrl Pts',(-2.8586005031575,3.93452605039578,-19.23125));
#304646=CARTESIAN_POINT('Ctrl Pts',(-4.13700551227254,3.00571044325861,
-19.14375));
#304647=CARTESIAN_POINT('Ctrl Pts',(-4.62531277436637,1.5028552216293,-19.05625));
#304648=CARTESIAN_POINT('Ctrl Pts',(-5.1136200364602,2.97339820732463E-15,
-18.96875));
#304649=CARTESIAN_POINT('Ctrl Pts',(-4.62531277436638,-1.5028552216293,
-18.88125));
#304650=CARTESIAN_POINT('Ctrl Pts',(-4.13700551227254,-3.0057104432586,
-18.79375));
#304651=CARTESIAN_POINT('Ctrl Pts',(-2.8586005031575,-3.93452605039577,
-18.70625));
#304652=CARTESIAN_POINT('Ctrl Pts',(-1.58019549404244,-4.86334165753293,
-18.61875));
#304653=CARTESIAN_POINT('Ctrl Pts',(-5.9558757940577E-16,-4.86334165753294,
-18.53125));
#304654=CARTESIAN_POINT('Origin',(-3.81730450148946E-15,-2.22044604925031E-15,
-37.015625));
#304655=CARTESIAN_POINT('',(-4.41289208089522E-15,-4.86334165753294,-22.25));
#304656=CARTESIAN_POINT('',(-4.41289208089522E-15,-4.86334165753294,-22.03125));
#304657=CARTESIAN_POINT('',(-8.23019658238468E-15,-4.86334165753294,-37.015625));
#304658=CARTESIAN_POINT('Ctrl Pts',(-5.9558757940577E-16,-4.86334165753294,
-22.25));
#304659=CARTESIAN_POINT('Ctrl Pts',(1.58019549404244,-4.86334165753293,
-22.1625));
#304660=CARTESIAN_POINT('Ctrl Pts',(2.85860050315749,-3.93452605039577,
-22.075));
#304661=CARTESIAN_POINT('Ctrl Pts',(4.13700551227254,-3.0057104432586,-21.9875));
#304662=CARTESIAN_POINT('Ctrl Pts',(4.62531277436637,-1.5028552216293,-21.9));
#304663=CARTESIAN_POINT('Ctrl Pts',(5.1136200364602,1.63211649733885E-15,
-21.8125));
#304664=CARTESIAN_POINT('Ctrl Pts',(4.62531277436638,1.5028552216293,-21.725));
#304665=CARTESIAN_POINT('Ctrl Pts',(4.13700551227254,3.00571044325861,-21.6375));
#304666=CARTESIAN_POINT('Ctrl Pts',(2.8586005031575,3.93452605039578,-21.55));
#304667=CARTESIAN_POINT('Ctrl Pts',(1.58019549404244,4.86334165753294,-21.4625));
#304668=CARTESIAN_POINT('Ctrl Pts',(0.,4.86334165753294,-21.375));
#304669=CARTESIAN_POINT('Ctrl Pts',(-1.58019549404244,4.86334165753294,
-21.2875));
#304670=CARTESIAN_POINT('Ctrl Pts',(-2.8586005031575,3.93452605039578,-21.2));
#304671=CARTESIAN_POINT('Ctrl Pts',(-4.13700551227254,3.00571044325861,
-21.1125));
#304672=CARTESIAN_POINT('Ctrl Pts',(-4.62531277436637,1.5028552216293,-21.025));
#304673=CARTESIAN_POINT('Ctrl Pts',(-5.1136200364602,2.91191711098618E-15,
-20.9375));
#304674=CARTESIAN_POINT('Ctrl Pts',(-4.62531277436638,-1.5028552216293,
-20.85));
#304675=CARTESIAN_POINT('Ctrl Pts',(-4.13700551227254,-3.0057104432586,
-20.7625));
#304676=CARTESIAN_POINT('Ctrl Pts',(-2.8586005031575,-3.93452605039577,
-20.675));
#304677=CARTESIAN_POINT('Ctrl Pts',(-1.58019549404244,-4.86334165753293,
-20.5875));
#304678=CARTESIAN_POINT('Ctrl Pts',(-5.9558757940577E-16,-4.86334165753294,
-20.5));
#304679=CARTESIAN_POINT('Ctrl Pts',(-5.9558757940577E-16,-4.86334165753294,
-22.03125));
#304680=CARTESIAN_POINT('Ctrl Pts',(1.58019549404244,-4.86334165753293,
-21.94375));
#304681=CARTESIAN_POINT('Ctrl Pts',(2.85860050315749,-3.93452605039577,
-21.85625));
#304682=CARTESIAN_POINT('Ctrl Pts',(4.13700551227254,-3.0057104432586,-21.76875));
#304683=CARTESIAN_POINT('Ctrl Pts',(4.62531277436637,-1.5028552216293,-21.68125));
#304684=CARTESIAN_POINT('Ctrl Pts',(5.1136200364602,1.63894773026535E-15,
-21.59375));
#304685=CARTESIAN_POINT('Ctrl Pts',(4.62531277436638,1.5028552216293,-21.50625));
#304686=CARTESIAN_POINT('Ctrl Pts',(4.13700551227254,3.00571044325861,-21.41875));
#304687=CARTESIAN_POINT('Ctrl Pts',(2.8586005031575,3.93452605039578,-21.33125));
#304688=CARTESIAN_POINT('Ctrl Pts',(1.58019549404244,4.86334165753294,-21.24375));
#304689=CARTESIAN_POINT('Ctrl Pts',(0.,4.86334165753294,-21.15625));
#304690=CARTESIAN_POINT('Ctrl Pts',(-1.58019549404244,4.86334165753294,
-21.06875));
#304691=CARTESIAN_POINT('Ctrl Pts',(-2.8586005031575,3.93452605039578,-20.98125));
#304692=CARTESIAN_POINT('Ctrl Pts',(-4.13700551227254,3.00571044325861,
-20.89375));
#304693=CARTESIAN_POINT('Ctrl Pts',(-4.62531277436637,1.5028552216293,-20.80625));
#304694=CARTESIAN_POINT('Ctrl Pts',(-5.1136200364602,2.91874834391268E-15,
-20.71875));
#304695=CARTESIAN_POINT('Ctrl Pts',(-4.62531277436638,-1.5028552216293,
-20.63125));
#304696=CARTESIAN_POINT('Ctrl Pts',(-4.13700551227254,-3.0057104432586,
-20.54375));
#304697=CARTESIAN_POINT('Ctrl Pts',(-2.8586005031575,-3.93452605039577,
-20.45625));
#304698=CARTESIAN_POINT('Ctrl Pts',(-1.58019549404244,-4.86334165753293,
-20.36875));
#304699=CARTESIAN_POINT('Ctrl Pts',(-5.9558757940577E-16,-4.86334165753294,
-20.28125));
#304700=CARTESIAN_POINT('Origin',(-3.81730450148946E-15,-2.22044604925031E-15,
-37.015625));
#304701=CARTESIAN_POINT('',(-4.41289208089522E-15,-4.86334165753294,-24.));
#304702=CARTESIAN_POINT('',(-4.41289208089522E-15,-4.86334165753294,-23.78125));
#304703=CARTESIAN_POINT('',(-8.23019658238468E-15,-4.86334165753294,-37.015625));
#304704=CARTESIAN_POINT('Ctrl Pts',(-5.9558757940577E-16,-4.86334165753294,
-24.));
#304705=CARTESIAN_POINT('Ctrl Pts',(1.58019549404244,-4.86334165753293,
-23.9125));
#304706=CARTESIAN_POINT('Ctrl Pts',(2.85860050315749,-3.93452605039577,
-23.825));
#304707=CARTESIAN_POINT('Ctrl Pts',(4.13700551227254,-3.0057104432586,-23.7375));
#304708=CARTESIAN_POINT('Ctrl Pts',(4.62531277436637,-1.5028552216293,-23.65));
#304709=CARTESIAN_POINT('Ctrl Pts',(5.1136200364602,1.5774666339269E-15,
-23.5625));
#304710=CARTESIAN_POINT('Ctrl Pts',(4.62531277436638,1.5028552216293,-23.475));
#304711=CARTESIAN_POINT('Ctrl Pts',(4.13700551227254,3.00571044325861,-23.3875));
#304712=CARTESIAN_POINT('Ctrl Pts',(2.8586005031575,3.93452605039578,-23.3));
#304713=CARTESIAN_POINT('Ctrl Pts',(1.58019549404244,4.86334165753294,-23.2125));
#304714=CARTESIAN_POINT('Ctrl Pts',(0.,4.86334165753294,-23.125));
#304715=CARTESIAN_POINT('Ctrl Pts',(-1.58019549404244,4.86334165753294,
-23.0375));
#304716=CARTESIAN_POINT('Ctrl Pts',(-2.8586005031575,3.93452605039578,-22.95));
#304717=CARTESIAN_POINT('Ctrl Pts',(-4.13700551227254,3.00571044325861,
-22.8625));
#304718=CARTESIAN_POINT('Ctrl Pts',(-4.62531277436637,1.5028552216293,-22.775));
#304719=CARTESIAN_POINT('Ctrl Pts',(-5.1136200364602,2.85726724757423E-15,
-22.6875));
#304720=CARTESIAN_POINT('Ctrl Pts',(-4.62531277436638,-1.5028552216293,
-22.6));
#304721=CARTESIAN_POINT('Ctrl Pts',(-4.13700551227254,-3.0057104432586,
-22.5125));
#304722=CARTESIAN_POINT('Ctrl Pts',(-2.8586005031575,-3.93452605039577,
-22.425));
#304723=CARTESIAN_POINT('Ctrl Pts',(-1.58019549404244,-4.86334165753293,
-22.3375));
#304724=CARTESIAN_POINT('Ctrl Pts',(-5.9558757940577E-16,-4.86334165753294,
-22.25));
#304725=CARTESIAN_POINT('Ctrl Pts',(-5.9558757940577E-16,-4.86334165753294,
-23.78125));
#304726=CARTESIAN_POINT('Ctrl Pts',(1.58019549404244,-4.86334165753293,
-23.69375));
#304727=CARTESIAN_POINT('Ctrl Pts',(2.85860050315749,-3.93452605039577,
-23.60625));
#304728=CARTESIAN_POINT('Ctrl Pts',(4.13700551227254,-3.0057104432586,-23.51875));
#304729=CARTESIAN_POINT('Ctrl Pts',(4.62531277436637,-1.5028552216293,-23.43125));
#304730=CARTESIAN_POINT('Ctrl Pts',(5.1136200364602,1.5842978668534E-15,
-23.34375));
#304731=CARTESIAN_POINT('Ctrl Pts',(4.62531277436638,1.5028552216293,-23.25625));
#304732=CARTESIAN_POINT('Ctrl Pts',(4.13700551227254,3.00571044325861,-23.16875));
#304733=CARTESIAN_POINT('Ctrl Pts',(2.8586005031575,3.93452605039578,-23.08125));
#304734=CARTESIAN_POINT('Ctrl Pts',(1.58019549404244,4.86334165753294,-22.99375));
#304735=CARTESIAN_POINT('Ctrl Pts',(0.,4.86334165753294,-22.90625));
#304736=CARTESIAN_POINT('Ctrl Pts',(-1.58019549404244,4.86334165753294,
-22.81875));
#304737=CARTESIAN_POINT('Ctrl Pts',(-2.8586005031575,3.93452605039578,-22.73125));
#304738=CARTESIAN_POINT('Ctrl Pts',(-4.13700551227254,3.00571044325861,
-22.64375));
#304739=CARTESIAN_POINT('Ctrl Pts',(-4.62531277436637,1.5028552216293,-22.55625));
#304740=CARTESIAN_POINT('Ctrl Pts',(-5.1136200364602,2.86409848050072E-15,
-22.46875));
#304741=CARTESIAN_POINT('Ctrl Pts',(-4.62531277436638,-1.5028552216293,
-22.38125));
#304742=CARTESIAN_POINT('Ctrl Pts',(-4.13700551227254,-3.0057104432586,
-22.29375));
#304743=CARTESIAN_POINT('Ctrl Pts',(-2.8586005031575,-3.93452605039577,
-22.20625));
#304744=CARTESIAN_POINT('Ctrl Pts',(-1.58019549404244,-4.86334165753293,
-22.11875));
#304745=CARTESIAN_POINT('Ctrl Pts',(-5.9558757940577E-16,-4.86334165753294,
-22.03125));
#304746=CARTESIAN_POINT('Origin',(-3.81730450148946E-15,-2.22044604925031E-15,
-37.015625));
#304747=CARTESIAN_POINT('',(-4.41289208089522E-15,-4.86334165753294,-25.75));
#304748=CARTESIAN_POINT('',(-4.41289208089522E-15,-4.86334165753294,-25.53125));
#304749=CARTESIAN_POINT('',(-8.23019658238468E-15,-4.86334165753294,-37.015625));
#304750=CARTESIAN_POINT('Ctrl Pts',(-5.9558757940577E-16,-4.86334165753294,
-25.75));
#304751=CARTESIAN_POINT('Ctrl Pts',(1.58019549404244,-4.86334165753293,
-25.6625));
#304752=CARTESIAN_POINT('Ctrl Pts',(2.85860050315749,-3.93452605039577,
-25.575));
#304753=CARTESIAN_POINT('Ctrl Pts',(4.13700551227254,-3.0057104432586,-25.4875));
#304754=CARTESIAN_POINT('Ctrl Pts',(4.62531277436637,-1.5028552216293,-25.4));
#304755=CARTESIAN_POINT('Ctrl Pts',(5.1136200364602,1.52281677051495E-15,
-25.3125));
#304756=CARTESIAN_POINT('Ctrl Pts',(4.62531277436638,1.5028552216293,-25.225));
#304757=CARTESIAN_POINT('Ctrl Pts',(4.13700551227254,3.00571044325861,-25.1375));
#304758=CARTESIAN_POINT('Ctrl Pts',(2.8586005031575,3.93452605039578,-25.05));
#304759=CARTESIAN_POINT('Ctrl Pts',(1.58019549404244,4.86334165753293,-24.9625));
#304760=CARTESIAN_POINT('Ctrl Pts',(0.,4.86334165753294,-24.875));
#304761=CARTESIAN_POINT('Ctrl Pts',(-1.58019549404244,4.86334165753293,
-24.7875));
#304762=CARTESIAN_POINT('Ctrl Pts',(-2.8586005031575,3.93452605039578,-24.7));
#304763=CARTESIAN_POINT('Ctrl Pts',(-4.13700551227254,3.00571044325861,
-24.6125));
#304764=CARTESIAN_POINT('Ctrl Pts',(-4.62531277436637,1.5028552216293,-24.525));
#304765=CARTESIAN_POINT('Ctrl Pts',(-5.1136200364602,2.80261738416228E-15,
-24.4375));
#304766=CARTESIAN_POINT('Ctrl Pts',(-4.62531277436638,-1.5028552216293,
-24.35));
#304767=CARTESIAN_POINT('Ctrl Pts',(-4.13700551227254,-3.0057104432586,
-24.2625));
#304768=CARTESIAN_POINT('Ctrl Pts',(-2.8586005031575,-3.93452605039577,
-24.175));
#304769=CARTESIAN_POINT('Ctrl Pts',(-1.58019549404244,-4.86334165753293,
-24.0875));
#304770=CARTESIAN_POINT('Ctrl Pts',(-5.9558757940577E-16,-4.86334165753294,
-24.));
#304771=CARTESIAN_POINT('Ctrl Pts',(-5.9558757940577E-16,-4.86334165753294,
-25.53125));
#304772=CARTESIAN_POINT('Ctrl Pts',(1.58019549404244,-4.86334165753293,
-25.44375));
#304773=CARTESIAN_POINT('Ctrl Pts',(2.85860050315749,-3.93452605039577,
-25.35625));
#304774=CARTESIAN_POINT('Ctrl Pts',(4.13700551227254,-3.0057104432586,-25.26875));
#304775=CARTESIAN_POINT('Ctrl Pts',(4.62531277436637,-1.5028552216293,-25.18125));
#304776=CARTESIAN_POINT('Ctrl Pts',(5.1136200364602,1.52964800344145E-15,
-25.09375));
#304777=CARTESIAN_POINT('Ctrl Pts',(4.62531277436638,1.5028552216293,-25.00625));
#304778=CARTESIAN_POINT('Ctrl Pts',(4.13700551227254,3.00571044325861,-24.91875));
#304779=CARTESIAN_POINT('Ctrl Pts',(2.8586005031575,3.93452605039578,-24.83125));
#304780=CARTESIAN_POINT('Ctrl Pts',(1.58019549404244,4.86334165753293,-24.74375));
#304781=CARTESIAN_POINT('Ctrl Pts',(0.,4.86334165753294,-24.65625));
#304782=CARTESIAN_POINT('Ctrl Pts',(-1.58019549404244,4.86334165753293,
-24.56875));
#304783=CARTESIAN_POINT('Ctrl Pts',(-2.8586005031575,3.93452605039578,-24.48125));
#304784=CARTESIAN_POINT('Ctrl Pts',(-4.13700551227254,3.00571044325861,
-24.39375));
#304785=CARTESIAN_POINT('Ctrl Pts',(-4.62531277436637,1.5028552216293,-24.30625));
#304786=CARTESIAN_POINT('Ctrl Pts',(-5.1136200364602,2.80944861708877E-15,
-24.21875));
#304787=CARTESIAN_POINT('Ctrl Pts',(-4.62531277436638,-1.5028552216293,
-24.13125));
#304788=CARTESIAN_POINT('Ctrl Pts',(-4.13700551227254,-3.0057104432586,
-24.04375));
#304789=CARTESIAN_POINT('Ctrl Pts',(-2.8586005031575,-3.93452605039577,
-23.95625));
#304790=CARTESIAN_POINT('Ctrl Pts',(-1.58019549404244,-4.86334165753293,
-23.86875));
#304791=CARTESIAN_POINT('Ctrl Pts',(-5.9558757940577E-16,-4.86334165753294,
-23.78125));
#304792=CARTESIAN_POINT('Origin',(-3.81730450148946E-15,-2.22044604925031E-15,
-37.015625));
#304793=CARTESIAN_POINT('',(-4.41289208089522E-15,-4.86334165753294,-27.5));
#304794=CARTESIAN_POINT('',(-4.41289208089522E-15,-4.86334165753294,-27.28125));
#304795=CARTESIAN_POINT('',(-8.23019658238468E-15,-4.86334165753294,-37.015625));
#304796=CARTESIAN_POINT('Ctrl Pts',(-5.9558757940577E-16,-4.86334165753294,
-27.5));
#304797=CARTESIAN_POINT('Ctrl Pts',(1.58019549404244,-4.86334165753293,
-27.4125));
#304798=CARTESIAN_POINT('Ctrl Pts',(2.85860050315749,-3.93452605039577,
-27.325));
#304799=CARTESIAN_POINT('Ctrl Pts',(4.13700551227254,-3.0057104432586,-27.2375));
#304800=CARTESIAN_POINT('Ctrl Pts',(4.62531277436637,-1.5028552216293,-27.15));
#304801=CARTESIAN_POINT('Ctrl Pts',(5.1136200364602,1.468166907103E-15,
-27.0625));
#304802=CARTESIAN_POINT('Ctrl Pts',(4.62531277436638,1.5028552216293,-26.975));
#304803=CARTESIAN_POINT('Ctrl Pts',(4.13700551227254,3.00571044325861,-26.8875));
#304804=CARTESIAN_POINT('Ctrl Pts',(2.8586005031575,3.93452605039578,-26.8));
#304805=CARTESIAN_POINT('Ctrl Pts',(1.58019549404244,4.86334165753293,-26.7125));
#304806=CARTESIAN_POINT('Ctrl Pts',(0.,4.86334165753294,-26.625));
#304807=CARTESIAN_POINT('Ctrl Pts',(-1.58019549404244,4.86334165753293,
-26.5375));
#304808=CARTESIAN_POINT('Ctrl Pts',(-2.8586005031575,3.93452605039578,-26.45));
#304809=CARTESIAN_POINT('Ctrl Pts',(-4.13700551227254,3.00571044325861,
-26.3625));
#304810=CARTESIAN_POINT('Ctrl Pts',(-4.62531277436637,1.5028552216293,-26.275));
#304811=CARTESIAN_POINT('Ctrl Pts',(-5.1136200364602,2.74796752075033E-15,
-26.1875));
#304812=CARTESIAN_POINT('Ctrl Pts',(-4.62531277436638,-1.5028552216293,
-26.1));
#304813=CARTESIAN_POINT('Ctrl Pts',(-4.13700551227254,-3.0057104432586,
-26.0125));
#304814=CARTESIAN_POINT('Ctrl Pts',(-2.8586005031575,-3.93452605039577,
-25.925));
#304815=CARTESIAN_POINT('Ctrl Pts',(-1.58019549404244,-4.86334165753293,
-25.8375));
#304816=CARTESIAN_POINT('Ctrl Pts',(-5.9558757940577E-16,-4.86334165753294,
-25.75));
#304817=CARTESIAN_POINT('Ctrl Pts',(-5.9558757940577E-16,-4.86334165753294,
-27.28125));
#304818=CARTESIAN_POINT('Ctrl Pts',(1.58019549404244,-4.86334165753293,
-27.19375));
#304819=CARTESIAN_POINT('Ctrl Pts',(2.85860050315749,-3.93452605039577,
-27.10625));
#304820=CARTESIAN_POINT('Ctrl Pts',(4.13700551227254,-3.0057104432586,-27.01875));
#304821=CARTESIAN_POINT('Ctrl Pts',(4.62531277436637,-1.5028552216293,-26.93125));
#304822=CARTESIAN_POINT('Ctrl Pts',(5.1136200364602,1.47499814002949E-15,
-26.84375));
#304823=CARTESIAN_POINT('Ctrl Pts',(4.62531277436638,1.5028552216293,-26.75625));
#304824=CARTESIAN_POINT('Ctrl Pts',(4.13700551227254,3.00571044325861,-26.66875));
#304825=CARTESIAN_POINT('Ctrl Pts',(2.8586005031575,3.93452605039578,-26.58125));
#304826=CARTESIAN_POINT('Ctrl Pts',(1.58019549404244,4.86334165753293,-26.49375));
#304827=CARTESIAN_POINT('Ctrl Pts',(0.,4.86334165753294,-26.40625));
#304828=CARTESIAN_POINT('Ctrl Pts',(-1.58019549404244,4.86334165753293,
-26.31875));
#304829=CARTESIAN_POINT('Ctrl Pts',(-2.8586005031575,3.93452605039578,-26.23125));
#304830=CARTESIAN_POINT('Ctrl Pts',(-4.13700551227254,3.00571044325861,
-26.14375));
#304831=CARTESIAN_POINT('Ctrl Pts',(-4.62531277436637,1.5028552216293,-26.05625));
#304832=CARTESIAN_POINT('Ctrl Pts',(-5.1136200364602,2.75479875367682E-15,
-25.96875));
#304833=CARTESIAN_POINT('Ctrl Pts',(-4.62531277436638,-1.5028552216293,
-25.88125));
#304834=CARTESIAN_POINT('Ctrl Pts',(-4.13700551227254,-3.0057104432586,
-25.79375));
#304835=CARTESIAN_POINT('Ctrl Pts',(-2.8586005031575,-3.93452605039577,
-25.70625));
#304836=CARTESIAN_POINT('Ctrl Pts',(-1.58019549404244,-4.86334165753293,
-25.61875));
#304837=CARTESIAN_POINT('Ctrl Pts',(-5.9558757940577E-16,-4.86334165753294,
-25.53125));
#304838=CARTESIAN_POINT('Origin',(-3.81730450148946E-15,-2.22044604925031E-15,
-37.015625));
#304839=CARTESIAN_POINT('',(-4.41289208089522E-15,-4.86334165753294,-29.25));
#304840=CARTESIAN_POINT('',(-4.41289208089522E-15,-4.86334165753294,-29.03125));
#304841=CARTESIAN_POINT('',(-8.23019658238468E-15,-4.86334165753294,-37.015625));
#304842=CARTESIAN_POINT('Ctrl Pts',(-5.9558757940577E-16,-4.86334165753294,
-29.25));
#304843=CARTESIAN_POINT('Ctrl Pts',(1.58019549404244,-4.86334165753293,
-29.1625));
#304844=CARTESIAN_POINT('Ctrl Pts',(2.85860050315749,-3.93452605039577,
-29.075));
#304845=CARTESIAN_POINT('Ctrl Pts',(4.13700551227254,-3.0057104432586,-28.9875));
#304846=CARTESIAN_POINT('Ctrl Pts',(4.62531277436637,-1.5028552216293,-28.9));
#304847=CARTESIAN_POINT('Ctrl Pts',(5.1136200364602,1.41351704369105E-15,
-28.8125));
#304848=CARTESIAN_POINT('Ctrl Pts',(4.62531277436638,1.5028552216293,-28.725));
#304849=CARTESIAN_POINT('Ctrl Pts',(4.13700551227254,3.00571044325861,-28.6375));
#304850=CARTESIAN_POINT('Ctrl Pts',(2.8586005031575,3.93452605039578,-28.55));
#304851=CARTESIAN_POINT('Ctrl Pts',(1.58019549404244,4.86334165753293,-28.4625));
#304852=CARTESIAN_POINT('Ctrl Pts',(0.,4.86334165753294,-28.375));
#304853=CARTESIAN_POINT('Ctrl Pts',(-1.58019549404244,4.86334165753293,
-28.2875));
#304854=CARTESIAN_POINT('Ctrl Pts',(-2.8586005031575,3.93452605039578,-28.2));
#304855=CARTESIAN_POINT('Ctrl Pts',(-4.13700551227254,3.00571044325861,
-28.1125));
#304856=CARTESIAN_POINT('Ctrl Pts',(-4.62531277436637,1.5028552216293,-28.025));
#304857=CARTESIAN_POINT('Ctrl Pts',(-5.1136200364602,2.69331765733838E-15,
-27.9375));
#304858=CARTESIAN_POINT('Ctrl Pts',(-4.62531277436638,-1.5028552216293,
-27.85));
#304859=CARTESIAN_POINT('Ctrl Pts',(-4.13700551227254,-3.0057104432586,
-27.7625));
#304860=CARTESIAN_POINT('Ctrl Pts',(-2.8586005031575,-3.93452605039577,
-27.675));
#304861=CARTESIAN_POINT('Ctrl Pts',(-1.58019549404244,-4.86334165753293,
-27.5875));
#304862=CARTESIAN_POINT('Ctrl Pts',(-5.9558757940577E-16,-4.86334165753294,
-27.5));
#304863=CARTESIAN_POINT('Ctrl Pts',(-5.9558757940577E-16,-4.86334165753294,
-29.03125));
#304864=CARTESIAN_POINT('Ctrl Pts',(1.58019549404244,-4.86334165753293,
-28.94375));
#304865=CARTESIAN_POINT('Ctrl Pts',(2.85860050315749,-3.93452605039577,
-28.85625));
#304866=CARTESIAN_POINT('Ctrl Pts',(4.13700551227254,-3.0057104432586,-28.76875));
#304867=CARTESIAN_POINT('Ctrl Pts',(4.62531277436637,-1.5028552216293,-28.68125));
#304868=CARTESIAN_POINT('Ctrl Pts',(5.1136200364602,1.42034827661754E-15,
-28.59375));
#304869=CARTESIAN_POINT('Ctrl Pts',(4.62531277436638,1.5028552216293,-28.50625));
#304870=CARTESIAN_POINT('Ctrl Pts',(4.13700551227254,3.00571044325861,-28.41875));
#304871=CARTESIAN_POINT('Ctrl Pts',(2.8586005031575,3.93452605039578,-28.33125));
#304872=CARTESIAN_POINT('Ctrl Pts',(1.58019549404244,4.86334165753293,-28.24375));
#304873=CARTESIAN_POINT('Ctrl Pts',(0.,4.86334165753294,-28.15625));
#304874=CARTESIAN_POINT('Ctrl Pts',(-1.58019549404244,4.86334165753293,
-28.06875));
#304875=CARTESIAN_POINT('Ctrl Pts',(-2.8586005031575,3.93452605039578,-27.98125));
#304876=CARTESIAN_POINT('Ctrl Pts',(-4.13700551227254,3.00571044325861,
-27.89375));
#304877=CARTESIAN_POINT('Ctrl Pts',(-4.62531277436637,1.5028552216293,-27.80625));
#304878=CARTESIAN_POINT('Ctrl Pts',(-5.1136200364602,2.70014889026487E-15,
-27.71875));
#304879=CARTESIAN_POINT('Ctrl Pts',(-4.62531277436638,-1.5028552216293,
-27.63125));
#304880=CARTESIAN_POINT('Ctrl Pts',(-4.13700551227254,-3.0057104432586,
-27.54375));
#304881=CARTESIAN_POINT('Ctrl Pts',(-2.8586005031575,-3.93452605039577,
-27.45625));
#304882=CARTESIAN_POINT('Ctrl Pts',(-1.58019549404244,-4.86334165753293,
-27.36875));
#304883=CARTESIAN_POINT('Ctrl Pts',(-5.9558757940577E-16,-4.86334165753294,
-27.28125));
#304884=CARTESIAN_POINT('Origin',(-3.81730450148946E-15,-2.22044604925031E-15,
-37.015625));
#304885=CARTESIAN_POINT('',(-4.41289208089522E-15,-4.86334165753294,-31.));
#304886=CARTESIAN_POINT('',(-4.41289208089522E-15,-4.86334165753294,-30.78125));
#304887=CARTESIAN_POINT('',(-8.23019658238468E-15,-4.86334165753294,-37.015625));
#304888=CARTESIAN_POINT('Ctrl Pts',(-5.9558757940577E-16,-4.86334165753294,
-31.));
#304889=CARTESIAN_POINT('Ctrl Pts',(1.58019549404244,-4.86334165753293,
-30.9125));
#304890=CARTESIAN_POINT('Ctrl Pts',(2.85860050315749,-3.93452605039577,
-30.825));
#304891=CARTESIAN_POINT('Ctrl Pts',(4.13700551227254,-3.0057104432586,-30.7375));
#304892=CARTESIAN_POINT('Ctrl Pts',(4.62531277436637,-1.5028552216293,-30.65));
#304893=CARTESIAN_POINT('Ctrl Pts',(5.1136200364602,1.3588671802791E-15,
-30.5625));
#304894=CARTESIAN_POINT('Ctrl Pts',(4.62531277436638,1.5028552216293,-30.475));
#304895=CARTESIAN_POINT('Ctrl Pts',(4.13700551227254,3.00571044325861,-30.3875));
#304896=CARTESIAN_POINT('Ctrl Pts',(2.8586005031575,3.93452605039578,-30.3));
#304897=CARTESIAN_POINT('Ctrl Pts',(1.58019549404244,4.86334165753293,-30.2125));
#304898=CARTESIAN_POINT('Ctrl Pts',(0.,4.86334165753294,-30.125));
#304899=CARTESIAN_POINT('Ctrl Pts',(-1.58019549404244,4.86334165753293,
-30.0375));
#304900=CARTESIAN_POINT('Ctrl Pts',(-2.8586005031575,3.93452605039578,-29.95));
#304901=CARTESIAN_POINT('Ctrl Pts',(-4.13700551227254,3.00571044325861,
-29.8625));
#304902=CARTESIAN_POINT('Ctrl Pts',(-4.62531277436637,1.5028552216293,-29.775));
#304903=CARTESIAN_POINT('Ctrl Pts',(-5.1136200364602,2.63866779392642E-15,
-29.6875));
#304904=CARTESIAN_POINT('Ctrl Pts',(-4.62531277436638,-1.5028552216293,
-29.6));
#304905=CARTESIAN_POINT('Ctrl Pts',(-4.13700551227254,-3.0057104432586,
-29.5125));
#304906=CARTESIAN_POINT('Ctrl Pts',(-2.8586005031575,-3.93452605039577,
-29.425));
#304907=CARTESIAN_POINT('Ctrl Pts',(-1.58019549404244,-4.86334165753293,
-29.3375));
#304908=CARTESIAN_POINT('Ctrl Pts',(-5.9558757940577E-16,-4.86334165753294,
-29.25));
#304909=CARTESIAN_POINT('Ctrl Pts',(-5.9558757940577E-16,-4.86334165753294,
-30.78125));
#304910=CARTESIAN_POINT('Ctrl Pts',(1.58019549404244,-4.86334165753293,
-30.69375));
#304911=CARTESIAN_POINT('Ctrl Pts',(2.85860050315749,-3.93452605039577,
-30.60625));
#304912=CARTESIAN_POINT('Ctrl Pts',(4.13700551227254,-3.0057104432586,-30.51875));
#304913=CARTESIAN_POINT('Ctrl Pts',(4.62531277436637,-1.5028552216293,-30.43125));
#304914=CARTESIAN_POINT('Ctrl Pts',(5.1136200364602,1.36569841320559E-15,
-30.34375));
#304915=CARTESIAN_POINT('Ctrl Pts',(4.62531277436638,1.5028552216293,-30.25625));
#304916=CARTESIAN_POINT('Ctrl Pts',(4.13700551227254,3.00571044325861,-30.16875));
#304917=CARTESIAN_POINT('Ctrl Pts',(2.8586005031575,3.93452605039578,-30.08125));
#304918=CARTESIAN_POINT('Ctrl Pts',(1.58019549404244,4.86334165753293,-29.99375));
#304919=CARTESIAN_POINT('Ctrl Pts',(0.,4.86334165753294,-29.90625));
#304920=CARTESIAN_POINT('Ctrl Pts',(-1.58019549404244,4.86334165753293,
-29.81875));
#304921=CARTESIAN_POINT('Ctrl Pts',(-2.8586005031575,3.93452605039578,-29.73125));
#304922=CARTESIAN_POINT('Ctrl Pts',(-4.13700551227254,3.00571044325861,
-29.64375));
#304923=CARTESIAN_POINT('Ctrl Pts',(-4.62531277436637,1.5028552216293,-29.55625));
#304924=CARTESIAN_POINT('Ctrl Pts',(-5.1136200364602,2.64549902685292E-15,
-29.46875));
#304925=CARTESIAN_POINT('Ctrl Pts',(-4.62531277436638,-1.5028552216293,
-29.38125));
#304926=CARTESIAN_POINT('Ctrl Pts',(-4.13700551227254,-3.0057104432586,
-29.29375));
#304927=CARTESIAN_POINT('Ctrl Pts',(-2.8586005031575,-3.93452605039577,
-29.20625));
#304928=CARTESIAN_POINT('Ctrl Pts',(-1.58019549404244,-4.86334165753293,
-29.11875));
#304929=CARTESIAN_POINT('Ctrl Pts',(-5.9558757940577E-16,-4.86334165753294,
-29.03125));
#304930=CARTESIAN_POINT('Origin',(-3.81730450148946E-15,-2.22044604925031E-15,
-37.015625));
#304931=CARTESIAN_POINT('',(-4.41289208089522E-15,-4.86334165753294,-32.75));
#304932=CARTESIAN_POINT('',(-4.41289208089522E-15,-4.86334165753294,-32.53125));
#304933=CARTESIAN_POINT('',(-8.23019658238468E-15,-4.86334165753294,-37.015625));
#304934=CARTESIAN_POINT('Ctrl Pts',(-5.9558757940577E-16,-4.86334165753294,
-32.75));
#304935=CARTESIAN_POINT('Ctrl Pts',(1.58019549404244,-4.86334165753293,
-32.6625));
#304936=CARTESIAN_POINT('Ctrl Pts',(2.85860050315749,-3.93452605039577,
-32.575));
#304937=CARTESIAN_POINT('Ctrl Pts',(4.13700551227254,-3.0057104432586,-32.4875));
#304938=CARTESIAN_POINT('Ctrl Pts',(4.62531277436637,-1.5028552216293,-32.4));
#304939=CARTESIAN_POINT('Ctrl Pts',(5.1136200364602,1.30421731686715E-15,
-32.3125));
#304940=CARTESIAN_POINT('Ctrl Pts',(4.62531277436638,1.5028552216293,-32.225));
#304941=CARTESIAN_POINT('Ctrl Pts',(4.13700551227254,3.00571044325861,-32.1375));
#304942=CARTESIAN_POINT('Ctrl Pts',(2.8586005031575,3.93452605039578,-32.05));
#304943=CARTESIAN_POINT('Ctrl Pts',(1.58019549404244,4.86334165753293,-31.9625));
#304944=CARTESIAN_POINT('Ctrl Pts',(0.,4.86334165753294,-31.875));
#304945=CARTESIAN_POINT('Ctrl Pts',(-1.58019549404244,4.86334165753293,
-31.7875));
#304946=CARTESIAN_POINT('Ctrl Pts',(-2.8586005031575,3.93452605039578,-31.7));
#304947=CARTESIAN_POINT('Ctrl Pts',(-4.13700551227254,3.00571044325861,
-31.6125));
#304948=CARTESIAN_POINT('Ctrl Pts',(-4.62531277436637,1.5028552216293,-31.525));
#304949=CARTESIAN_POINT('Ctrl Pts',(-5.1136200364602,2.58401793051447E-15,
-31.4375));
#304950=CARTESIAN_POINT('Ctrl Pts',(-4.62531277436638,-1.5028552216293,
-31.35));
#304951=CARTESIAN_POINT('Ctrl Pts',(-4.13700551227254,-3.0057104432586,
-31.2625));
#304952=CARTESIAN_POINT('Ctrl Pts',(-2.8586005031575,-3.93452605039577,
-31.175));
#304953=CARTESIAN_POINT('Ctrl Pts',(-1.58019549404244,-4.86334165753293,
-31.0875));
#304954=CARTESIAN_POINT('Ctrl Pts',(-5.9558757940577E-16,-4.86334165753294,
-31.));
#304955=CARTESIAN_POINT('Ctrl Pts',(-5.9558757940577E-16,-4.86334165753294,
-32.53125));
#304956=CARTESIAN_POINT('Ctrl Pts',(1.58019549404244,-4.86334165753293,
-32.44375));
#304957=CARTESIAN_POINT('Ctrl Pts',(2.85860050315749,-3.93452605039577,
-32.35625));
#304958=CARTESIAN_POINT('Ctrl Pts',(4.13700551227254,-3.0057104432586,-32.26875));
#304959=CARTESIAN_POINT('Ctrl Pts',(4.62531277436637,-1.5028552216293,-32.18125));
#304960=CARTESIAN_POINT('Ctrl Pts',(5.1136200364602,1.31104854979364E-15,
-32.09375));
#304961=CARTESIAN_POINT('Ctrl Pts',(4.62531277436638,1.5028552216293,-32.00625));
#304962=CARTESIAN_POINT('Ctrl Pts',(4.13700551227254,3.00571044325861,-31.91875));
#304963=CARTESIAN_POINT('Ctrl Pts',(2.8586005031575,3.93452605039578,-31.83125));
#304964=CARTESIAN_POINT('Ctrl Pts',(1.58019549404244,4.86334165753293,-31.74375));
#304965=CARTESIAN_POINT('Ctrl Pts',(0.,4.86334165753294,-31.65625));
#304966=CARTESIAN_POINT('Ctrl Pts',(-1.58019549404244,4.86334165753293,
-31.56875));
#304967=CARTESIAN_POINT('Ctrl Pts',(-2.8586005031575,3.93452605039578,-31.48125));
#304968=CARTESIAN_POINT('Ctrl Pts',(-4.13700551227254,3.00571044325861,
-31.39375));
#304969=CARTESIAN_POINT('Ctrl Pts',(-4.62531277436637,1.5028552216293,-31.30625));
#304970=CARTESIAN_POINT('Ctrl Pts',(-5.1136200364602,2.59084916344097E-15,
-31.21875));
#304971=CARTESIAN_POINT('Ctrl Pts',(-4.62531277436638,-1.5028552216293,
-31.13125));
#304972=CARTESIAN_POINT('Ctrl Pts',(-4.13700551227254,-3.0057104432586,
-31.04375));
#304973=CARTESIAN_POINT('Ctrl Pts',(-2.8586005031575,-3.93452605039577,
-30.95625));
#304974=CARTESIAN_POINT('Ctrl Pts',(-1.58019549404244,-4.86334165753293,
-30.86875));
#304975=CARTESIAN_POINT('Ctrl Pts',(-5.9558757940577E-16,-4.86334165753294,
-30.78125));
#304976=CARTESIAN_POINT('Origin',(-3.81730450148946E-15,-2.22044604925031E-15,
-37.015625));
#304977=CARTESIAN_POINT('',(-4.41289208089522E-15,-4.86334165753294,-34.5));
#304978=CARTESIAN_POINT('',(-4.41289208089522E-15,-4.86334165753294,-34.28125));
#304979=CARTESIAN_POINT('',(-8.23019658238468E-15,-4.86334165753294,-37.015625));
#304980=CARTESIAN_POINT('Ctrl Pts',(-5.9558757940577E-16,-4.86334165753294,
-34.5));
#304981=CARTESIAN_POINT('Ctrl Pts',(1.58019549404244,-4.86334165753293,
-34.4125));
#304982=CARTESIAN_POINT('Ctrl Pts',(2.85860050315749,-3.93452605039577,
-34.325));
#304983=CARTESIAN_POINT('Ctrl Pts',(4.13700551227254,-3.0057104432586,-34.2375));
#304984=CARTESIAN_POINT('Ctrl Pts',(4.62531277436637,-1.5028552216293,-34.15));
#304985=CARTESIAN_POINT('Ctrl Pts',(5.1136200364602,1.2495674534552E-15,
-34.0625));
#304986=CARTESIAN_POINT('Ctrl Pts',(4.62531277436638,1.5028552216293,-33.975));
#304987=CARTESIAN_POINT('Ctrl Pts',(4.13700551227254,3.00571044325861,-33.8875));
#304988=CARTESIAN_POINT('Ctrl Pts',(2.8586005031575,3.93452605039578,-33.8));
#304989=CARTESIAN_POINT('Ctrl Pts',(1.58019549404244,4.86334165753293,-33.7125));
#304990=CARTESIAN_POINT('Ctrl Pts',(0.,4.86334165753294,-33.625));
#304991=CARTESIAN_POINT('Ctrl Pts',(-1.58019549404244,4.86334165753293,
-33.5375));
#304992=CARTESIAN_POINT('Ctrl Pts',(-2.8586005031575,3.93452605039578,-33.45));
#304993=CARTESIAN_POINT('Ctrl Pts',(-4.13700551227254,3.00571044325861,
-33.3625));
#304994=CARTESIAN_POINT('Ctrl Pts',(-4.62531277436637,1.5028552216293,-33.275));
#304995=CARTESIAN_POINT('Ctrl Pts',(-5.1136200364602,2.52936806710252E-15,
-33.1875));
#304996=CARTESIAN_POINT('Ctrl Pts',(-4.62531277436638,-1.5028552216293,
-33.1));
#304997=CARTESIAN_POINT('Ctrl Pts',(-4.13700551227254,-3.0057104432586,
-33.0125));
#304998=CARTESIAN_POINT('Ctrl Pts',(-2.8586005031575,-3.93452605039577,
-32.925));
#304999=CARTESIAN_POINT('Ctrl Pts',(-1.58019549404244,-4.86334165753293,
-32.8375));
#305000=CARTESIAN_POINT('Ctrl Pts',(-5.9558757940577E-16,-4.86334165753294,
-32.75));
#305001=CARTESIAN_POINT('Ctrl Pts',(-5.9558757940577E-16,-4.86334165753294,
-34.28125));
#305002=CARTESIAN_POINT('Ctrl Pts',(1.58019549404244,-4.86334165753293,
-34.19375));
#305003=CARTESIAN_POINT('Ctrl Pts',(2.85860050315749,-3.93452605039577,
-34.10625));
#305004=CARTESIAN_POINT('Ctrl Pts',(4.13700551227254,-3.0057104432586,-34.01875));
#305005=CARTESIAN_POINT('Ctrl Pts',(4.62531277436637,-1.5028552216293,-33.93125));
#305006=CARTESIAN_POINT('Ctrl Pts',(5.1136200364602,1.25639868638169E-15,
-33.84375));
#305007=CARTESIAN_POINT('Ctrl Pts',(4.62531277436638,1.5028552216293,-33.75625));
#305008=CARTESIAN_POINT('Ctrl Pts',(4.13700551227254,3.00571044325861,-33.66875));
#305009=CARTESIAN_POINT('Ctrl Pts',(2.8586005031575,3.93452605039578,-33.58125));
#305010=CARTESIAN_POINT('Ctrl Pts',(1.58019549404244,4.86334165753293,-33.49375));
#305011=CARTESIAN_POINT('Ctrl Pts',(0.,4.86334165753294,-33.40625));
#305012=CARTESIAN_POINT('Ctrl Pts',(-1.58019549404244,4.86334165753293,
-33.31875));
#305013=CARTESIAN_POINT('Ctrl Pts',(-2.8586005031575,3.93452605039578,-33.23125));
#305014=CARTESIAN_POINT('Ctrl Pts',(-4.13700551227254,3.00571044325861,
-33.14375));
#305015=CARTESIAN_POINT('Ctrl Pts',(-4.62531277436637,1.5028552216293,-33.05625));
#305016=CARTESIAN_POINT('Ctrl Pts',(-5.1136200364602,2.53619930002902E-15,
-32.96875));
#305017=CARTESIAN_POINT('Ctrl Pts',(-4.62531277436638,-1.5028552216293,
-32.88125));
#305018=CARTESIAN_POINT('Ctrl Pts',(-4.13700551227254,-3.0057104432586,
-32.79375));
#305019=CARTESIAN_POINT('Ctrl Pts',(-2.8586005031575,-3.93452605039577,
-32.70625));
#305020=CARTESIAN_POINT('Ctrl Pts',(-1.58019549404244,-4.86334165753293,
-32.61875));
#305021=CARTESIAN_POINT('Ctrl Pts',(-5.9558757940577E-16,-4.86334165753294,
-32.53125));
#305022=CARTESIAN_POINT('Origin',(-3.81730450148946E-15,-2.22044604925031E-15,
-37.015625));
#305023=CARTESIAN_POINT('',(-8.23019658238468E-15,-4.86334165753294,-36.0741583424671));
#305024=CARTESIAN_POINT('',(-4.41289208089522E-15,-4.86334165753294,-36.03125));
#305025=CARTESIAN_POINT('',(-8.23019658238468E-15,-4.86334165753294,-37.015625));
#305026=CARTESIAN_POINT('',(2.87087722362434,-3.92557716072047,-36.0741583424671));
#305027=CARTESIAN_POINT('Origin',(-3.81730450148946E-15,-2.22044604925031E-15,
-36.0741583424671));
#305028=CARTESIAN_POINT('Ctrl Pts',(2.87087722362434,-3.92557716072047,
-36.074158342467));
#305029=CARTESIAN_POINT('Ctrl Pts',(4.13959932290703,-2.99772751497028,
-35.9870352138948));
#305030=CARTESIAN_POINT('Ctrl Pts',(4.62531277436637,-1.5028552216293,-35.9));
#305031=CARTESIAN_POINT('Ctrl Pts',(5.1136200364602,1.19491759004325E-15,
-35.8125));
#305032=CARTESIAN_POINT('Ctrl Pts',(4.62531277436638,1.5028552216293,-35.725));
#305033=CARTESIAN_POINT('Ctrl Pts',(4.13700551227254,3.00571044325861,-35.6375));
#305034=CARTESIAN_POINT('Ctrl Pts',(2.8586005031575,3.93452605039578,-35.55));
#305035=CARTESIAN_POINT('Ctrl Pts',(1.58019549404244,4.86334165753293,-35.4625));
#305036=CARTESIAN_POINT('Ctrl Pts',(0.,4.86334165753294,-35.375));
#305037=CARTESIAN_POINT('Ctrl Pts',(-1.58019549404244,4.86334165753293,
-35.2875));
#305038=CARTESIAN_POINT('Ctrl Pts',(-2.8586005031575,3.93452605039578,-35.2));
#305039=CARTESIAN_POINT('Ctrl Pts',(-4.13700551227254,3.00571044325861,
-35.1125));
#305040=CARTESIAN_POINT('Ctrl Pts',(-4.62531277436637,1.5028552216293,-35.025));
#305041=CARTESIAN_POINT('Ctrl Pts',(-5.1136200364602,2.47471820369058E-15,
-34.9375));
#305042=CARTESIAN_POINT('Ctrl Pts',(-4.62531277436638,-1.5028552216293,
-34.85));
#305043=CARTESIAN_POINT('Ctrl Pts',(-4.13700551227254,-3.0057104432586,
-34.7625));
#305044=CARTESIAN_POINT('Ctrl Pts',(-2.8586005031575,-3.93452605039577,
-34.675));
#305045=CARTESIAN_POINT('Ctrl Pts',(-1.58019549404244,-4.86334165753293,
-34.5875));
#305046=CARTESIAN_POINT('Ctrl Pts',(-5.9558757940577E-16,-4.86334165753294,
-34.5));
#305047=CARTESIAN_POINT('Ctrl Pts',(-5.9558757940577E-16,-4.86334165753294,
-36.03125));
#305048=CARTESIAN_POINT('Ctrl Pts',(1.58019549404244,-4.86334165753293,
-35.94375));
#305049=CARTESIAN_POINT('Ctrl Pts',(2.85860050315749,-3.93452605039577,
-35.85625));
#305050=CARTESIAN_POINT('Ctrl Pts',(4.13700551227254,-3.0057104432586,-35.76875));
#305051=CARTESIAN_POINT('Ctrl Pts',(4.62531277436637,-1.5028552216293,-35.68125));
#305052=CARTESIAN_POINT('Ctrl Pts',(5.1136200364602,1.20174882296974E-15,
-35.59375));
#305053=CARTESIAN_POINT('Ctrl Pts',(4.62531277436638,1.5028552216293,-35.50625));
#305054=CARTESIAN_POINT('Ctrl Pts',(4.13700551227254,3.00571044325861,-35.41875));
#305055=CARTESIAN_POINT('Ctrl Pts',(2.8586005031575,3.93452605039578,-35.33125));
#305056=CARTESIAN_POINT('Ctrl Pts',(1.58019549404244,4.86334165753293,-35.24375));
#305057=CARTESIAN_POINT('Ctrl Pts',(0.,4.86334165753294,-35.15625));
#305058=CARTESIAN_POINT('Ctrl Pts',(-1.58019549404244,4.86334165753293,
-35.06875));
#305059=CARTESIAN_POINT('Ctrl Pts',(-2.8586005031575,3.93452605039578,-34.98125));
#305060=CARTESIAN_POINT('Ctrl Pts',(-4.13700551227254,3.00571044325861,
-34.89375));
#305061=CARTESIAN_POINT('Ctrl Pts',(-4.62531277436637,1.5028552216293,-34.80625));
#305062=CARTESIAN_POINT('Ctrl Pts',(-5.1136200364602,2.48154943661707E-15,
-34.71875));
#305063=CARTESIAN_POINT('Ctrl Pts',(-4.62531277436638,-1.5028552216293,
-34.63125));
#305064=CARTESIAN_POINT('Ctrl Pts',(-4.13700551227254,-3.0057104432586,
-34.54375));
#305065=CARTESIAN_POINT('Ctrl Pts',(-2.8586005031575,-3.93452605039577,
-34.45625));
#305066=CARTESIAN_POINT('Ctrl Pts',(-1.58019549404244,-4.86334165753293,
-34.36875));
#305067=CARTESIAN_POINT('Ctrl Pts',(-5.9558757940577E-16,-4.86334165753294,
-34.28125));
#305068=CARTESIAN_POINT('Origin',(0.,1.54726425086094E-32,-36.25));
#305069=CARTESIAN_POINT('',(-5.74053187100322E-16,4.6875,-36.25));
#305070=CARTESIAN_POINT('Origin',(0.,0.,-36.25));
#305071=CARTESIAN_POINT('Origin',(0.,0.,-36.25));
#305072=CARTESIAN_POINT('',(-0.75570415697393,-4.80426927898796,-36.0741583424671));
#305073=CARTESIAN_POINT('Origin',(-3.81730450148946E-15,-2.22044604925031E-15,
-36.0741583424671));
#305074=CARTESIAN_POINT('Ctrl Pts',(-0.755704156980561,-4.80426927898596,
-36.074158342468));
#305075=CARTESIAN_POINT('Ctrl Pts',(-0.20401214347208,-4.96963876412555,
-35.9965237414583));
#305076=CARTESIAN_POINT('Ctrl Pts',(0.311551649488213,-5.01323384168292,
-35.9327029210741));
#305077=CARTESIAN_POINT('Ctrl Pts',(1.25407404975781,-4.99702713055866,
-35.8106779496758));
#305078=CARTESIAN_POINT('Ctrl Pts',(1.76270719049683,-4.91132116278564,
-35.7443314791183));
#305079=CARTESIAN_POINT('Ctrl Pts',(3.0561085366865,-4.48758075325132,-35.5736761112956));
#305080=CARTESIAN_POINT('Ctrl Pts',(3.66622286879486,-4.06718946684808,
-35.4903729948851));
#305081=CARTESIAN_POINT('Ctrl Pts',(4.61382316280902,-3.24347284732762,
-35.3397991561213));
#305082=CARTESIAN_POINT('Ctrl Pts',(5.04706534954943,-2.69479623139893,
-35.2577302368079));
#305083=CARTESIAN_POINT('Ctrl Pts',(5.53804224961896,-1.75560587935618,
-35.1392571522409));
#305084=CARTESIAN_POINT('Ctrl Pts',(5.67664426551943,-1.41114454880524,
-35.0991515136516));
#305085=CARTESIAN_POINT('Ctrl Pts',(5.88654445210013,-0.717259107080557,
-35.0184068473996));
#305086=CARTESIAN_POINT('Ctrl Pts',(5.95970573886025,-0.360868816120939,
-34.9777942611398));
#305087=CARTESIAN_POINT('Ctrl Pts',(6.00000000000006,1.3086753902769E-13,
-34.9375));
#305088=CARTESIAN_POINT('',(5.66027585496539E-13,5.3065902853892,-35.6309097146108));
#305089=CARTESIAN_POINT('Ctrl Pts',(4.25090439081148,-4.23436085615996,
-34.9375));
#305090=CARTESIAN_POINT('Ctrl Pts',(3.94586432209468,-4.52301011578173,
-34.9499085068966));
#305091=CARTESIAN_POINT('Ctrl Pts',(3.60994414662963,-4.78043202406146,
-34.9619227444854));
#305092=CARTESIAN_POINT('Ctrl Pts',(2.89993674271926,-5.21329695011778,
-34.986087803612));
#305093=CARTESIAN_POINT('Ctrl Pts',(2.52765946231677,-5.39008399969571,
-34.9983670497719));
#305094=CARTESIAN_POINT('Ctrl Pts',(1.33396338181343,-5.81126867800779,
-35.0366314074234));
#305095=CARTESIAN_POINT('Ctrl Pts',(0.582212176146963,-5.88009959498879,
-35.0592032216902));
#305096=CARTESIAN_POINT('Ctrl Pts',(-0.78543039238956,-5.83604565467705,
-35.0990862861668));
#305097=CARTESIAN_POINT('Ctrl Pts',(-1.54046399409007,-5.65922745007568,
-35.1227986339086));
#305098=CARTESIAN_POINT('Ctrl Pts',(-2.87943510559081,-5.04856276714971,
-35.1682398652137));
#305099=CARTESIAN_POINT('Ctrl Pts',(-3.5125870879507,-4.61978096154844,
-35.1902411990604));
#305100=CARTESIAN_POINT('Ctrl Pts',(-4.31607850491965,-3.7579555268088,
-35.2267553883466));
#305101=CARTESIAN_POINT('Ctrl Pts',(-4.54240102332553,-3.46176213771459,
-35.2384602619037));
#305102=CARTESIAN_POINT('Ctrl Pts',(-5.12359255224559,-2.52341861708909,
-35.2732506014562));
#305103=CARTESIAN_POINT('Ctrl Pts',(-5.38789728595103,-1.82861905627414,
-35.2952726496514));
#305104=CARTESIAN_POINT('Ctrl Pts',(-5.62948928770176,-0.391419802924234,
-35.340899264706));
#305105=CARTESIAN_POINT('Ctrl Pts',(-5.60963733778489,0.338237306065926,
-35.3643460096725));
#305106=CARTESIAN_POINT('Ctrl Pts',(-5.29068241366305,1.7582581177162,-35.4105557797717));
#305107=CARTESIAN_POINT('Ctrl Pts',(-4.99092361989608,2.43522600496335,
-35.4329662937982));
#305108=CARTESIAN_POINT('Ctrl Pts',(-4.12356683987079,3.65185184338728,
-35.4818385718741));
#305109=CARTESIAN_POINT('Ctrl Pts',(-3.60214275753461,4.11179926418803,
-35.5041628936101));
#305110=CARTESIAN_POINT('Ctrl Pts',(-2.50569072638291,4.82632890339624,
-35.5456578831318));
#305111=CARTESIAN_POINT('Ctrl Pts',(-1.84237918164405,5.09141668561591,
-35.569351301463));
#305112=CARTESIAN_POINT('Ctrl Pts',(-0.787765501183242,5.286414527606,-35.6051819697655));
#305113=CARTESIAN_POINT('Ctrl Pts',(-0.402304728178604,5.31953353865749,
-35.6179664613425));
#305114=CARTESIAN_POINT('Ctrl Pts',(1.1326703464043E-12,5.3065902853892,
-35.6309097146108));
#305115=CARTESIAN_POINT('',(-5.74053187100322E-16,4.6875,-36.25));
#305116=CARTESIAN_POINT('Ctrl Pts',(1.13305198556901E-12,5.3065902853892,
-35.6309097146108));
#305117=CARTESIAN_POINT('Ctrl Pts',(0.301858928469087,5.29687865067854,
-35.6406213493215));
#305118=CARTESIAN_POINT('Ctrl Pts',(0.613170200032512,5.26082782642507,
-35.6509592015469));
#305119=CARTESIAN_POINT('Ctrl Pts',(1.59305535335563,5.05107298329413,-35.6847185175551));
#305120=CARTESIAN_POINT('Ctrl Pts',(2.22246370547848,4.78190033023382,-35.7081169756363));
#305121=CARTESIAN_POINT('Ctrl Pts',(3.06451237669578,4.20907822167898,-35.7421202323282));
#305122=CARTESIAN_POINT('Ctrl Pts',(3.32719700442894,3.99037699520634,-35.7532357491875));
#305123=CARTESIAN_POINT('Ctrl Pts',(4.02745140797445,3.27661400272233,-35.7873464474319));
#305124=CARTESIAN_POINT('Ctrl Pts',(4.39375114628118,2.72273009067369,-35.8105276921273));
#305125=CARTESIAN_POINT('Ctrl Pts',(4.90047483751086,1.49956602513327,-35.8561248424504));
#305126=CARTESIAN_POINT('Ctrl Pts',(5.0333291364154,0.84052286403436,-35.878337573202));
#305127=CARTESIAN_POINT('Ctrl Pts',(5.03197635517925,-0.154058292819836,
-35.9137516628987));
#305128=CARTESIAN_POINT('Ctrl Pts',(4.99971688172876,-0.479745816608457,
-35.9254296301762));
#305129=CARTESIAN_POINT('Ctrl Pts',(4.81851961074914,-1.3918952367453,-35.9583641196365));
#305130=CARTESIAN_POINT('Ctrl Pts',(4.5840718021508,-2.01546334153228,-35.9805560596166));
#305131=CARTESIAN_POINT('Ctrl Pts',(3.83654650082638,-3.12507114135312,
-36.0291042366888));
#305132=CARTESIAN_POINT('Ctrl Pts',(3.38981590912108,-3.57335138044469,
-36.0521323813635));
#305133=CARTESIAN_POINT('Ctrl Pts',(2.87087722362394,-3.92557716072074,
-36.0741583424671));
#305134=CARTESIAN_POINT('Ctrl Pts',(0.,6.09472152853892,-36.1953125));
#305135=CARTESIAN_POINT('Ctrl Pts',(-1.98029506767702,6.09472152853892,
-36.1078125));
#305136=CARTESIAN_POINT('Ctrl Pts',(-3.58238743130462,4.93073329257085,
-36.0203125));
#305137=CARTESIAN_POINT('Ctrl Pts',(-5.18447979493222,3.76674505660277,
-35.9328125));
#305138=CARTESIAN_POINT('Ctrl Pts',(-5.7964246247213,1.88337252830138,-35.8453125));
#305139=CARTESIAN_POINT('Ctrl Pts',(-6.40836945451038,2.52838161674187E-15,
-35.7578125));
#305140=CARTESIAN_POINT('Ctrl Pts',(-5.7964246247213,-1.88337252830138,
-35.6703125));
#305141=CARTESIAN_POINT('Ctrl Pts',(-5.18447979493222,-3.76674505660276,
-35.5828125));
#305142=CARTESIAN_POINT('Ctrl Pts',(-3.58238743130462,-4.93073329257084,
-35.4953125));
#305143=CARTESIAN_POINT('Ctrl Pts',(-1.98029506767702,-6.09472152853892,
-35.4078125));
#305144=CARTESIAN_POINT('Ctrl Pts',(-7.46388121161966E-16,-6.09472152853892,
-35.3203125));
#305145=CARTESIAN_POINT('Ctrl Pts',(1.98029506767702,-6.09472152853892,
-35.2328125));
#305146=CARTESIAN_POINT('Ctrl Pts',(3.58238743130462,-4.93073329257084,
-35.1453125));
#305147=CARTESIAN_POINT('Ctrl Pts',(5.18447979493222,-3.76674505660277,
-35.0578125));
#305148=CARTESIAN_POINT('Ctrl Pts',(5.7964246247213,-1.88337252830138,-34.9703125));
#305149=CARTESIAN_POINT('Ctrl Pts',(6.40836945451038,9.86108720403888E-16,
-34.8828125));
#305150=CARTESIAN_POINT('Ctrl Pts',(5.7964246247213,1.88337252830138,-34.7953125));
#305151=CARTESIAN_POINT('Ctrl Pts',(5.18447979493222,3.76674505660277,-34.7078125));
#305152=CARTESIAN_POINT('Ctrl Pts',(3.58238743130462,4.93073329257085,-34.6203125));
#305153=CARTESIAN_POINT('Ctrl Pts',(1.98029506767702,6.09472152853892,-34.5328125));
#305154=CARTESIAN_POINT('Ctrl Pts',(0.,6.09472152853892,-34.4453125));
#305155=CARTESIAN_POINT('Ctrl Pts',(-1.98029506767702,6.09472152853892,
-34.3578125));
#305156=CARTESIAN_POINT('Ctrl Pts',(-3.58238743130462,4.93073329257085,
-34.2703125));
#305157=CARTESIAN_POINT('Ctrl Pts',(-5.18447979493222,3.76674505660277,
-34.1828125));
#305158=CARTESIAN_POINT('Ctrl Pts',(-5.7964246247213,1.88337252830138,-34.0953125));
#305159=CARTESIAN_POINT('Ctrl Pts',(-6.40836945451038,2.58303148015383E-15,
-34.0078125));
#305160=CARTESIAN_POINT('Ctrl Pts',(-5.7964246247213,-1.88337252830138,
-33.9203125));
#305161=CARTESIAN_POINT('Ctrl Pts',(-5.18447979493222,-3.76674505660276,
-33.8328125));
#305162=CARTESIAN_POINT('Ctrl Pts',(-3.58238743130462,-4.93073329257084,
-33.7453125));
#305163=CARTESIAN_POINT('Ctrl Pts',(-1.98029506767702,-6.09472152853892,
-33.6578125));
#305164=CARTESIAN_POINT('Ctrl Pts',(-7.46388121161966E-16,-6.09472152853892,
-33.5703125));
#305165=CARTESIAN_POINT('Ctrl Pts',(1.98029506767702,-6.09472152853892,
-33.4828125));
#305166=CARTESIAN_POINT('Ctrl Pts',(3.58238743130462,-4.93073329257084,
-33.3953125));
#305167=CARTESIAN_POINT('Ctrl Pts',(5.18447979493222,-3.76674505660277,
-33.3078125));
#305168=CARTESIAN_POINT('Ctrl Pts',(5.7964246247213,-1.88337252830138,-33.2203125));
#305169=CARTESIAN_POINT('Ctrl Pts',(6.40836945451038,1.04075858381584E-15,
-33.1328125));
#305170=CARTESIAN_POINT('Ctrl Pts',(5.7964246247213,1.88337252830138,-33.0453125));
#305171=CARTESIAN_POINT('Ctrl Pts',(5.18447979493222,3.76674505660277,-32.9578125));
#305172=CARTESIAN_POINT('Ctrl Pts',(3.58238743130462,4.93073329257085,-32.8703125));
#305173=CARTESIAN_POINT('Ctrl Pts',(1.98029506767702,6.09472152853892,-32.7828125));
#305174=CARTESIAN_POINT('Ctrl Pts',(0.,6.09472152853892,-32.6953125));
#305175=CARTESIAN_POINT('Ctrl Pts',(-1.98029506767702,6.09472152853892,
-32.6078125));
#305176=CARTESIAN_POINT('Ctrl Pts',(-3.58238743130462,4.93073329257085,
-32.5203125));
#305177=CARTESIAN_POINT('Ctrl Pts',(-5.18447979493222,3.76674505660277,
-32.4328125));
#305178=CARTESIAN_POINT('Ctrl Pts',(-5.7964246247213,1.88337252830138,-32.3453125));
#305179=CARTESIAN_POINT('Ctrl Pts',(-6.40836945451038,2.63768134356578E-15,
-32.2578125));
#305180=CARTESIAN_POINT('Ctrl Pts',(-5.7964246247213,-1.88337252830138,
-32.1703125));
#305181=CARTESIAN_POINT('Ctrl Pts',(-5.18447979493222,-3.76674505660276,
-32.0828125));
#305182=CARTESIAN_POINT('Ctrl Pts',(-3.58238743130462,-4.93073329257084,
-31.9953125));
#305183=CARTESIAN_POINT('Ctrl Pts',(-1.98029506767702,-6.09472152853892,
-31.9078125));
#305184=CARTESIAN_POINT('Ctrl Pts',(-7.46388121161966E-16,-6.09472152853892,
-31.8203125));
#305185=CARTESIAN_POINT('Ctrl Pts',(1.98029506767702,-6.09472152853892,
-31.7328125));
#305186=CARTESIAN_POINT('Ctrl Pts',(3.58238743130462,-4.93073329257084,
-31.6453125));
#305187=CARTESIAN_POINT('Ctrl Pts',(5.18447979493222,-3.76674505660277,
-31.5578125));
#305188=CARTESIAN_POINT('Ctrl Pts',(5.7964246247213,-1.88337252830138,-31.4703125));
#305189=CARTESIAN_POINT('Ctrl Pts',(6.40836945451038,1.09540844722779E-15,
-31.3828125));
#305190=CARTESIAN_POINT('Ctrl Pts',(5.7964246247213,1.88337252830138,-31.2953125));
#305191=CARTESIAN_POINT('Ctrl Pts',(5.18447979493222,3.76674505660277,-31.2078125));
#305192=CARTESIAN_POINT('Ctrl Pts',(3.58238743130462,4.93073329257085,-31.1203125));
#305193=CARTESIAN_POINT('Ctrl Pts',(1.98029506767702,6.09472152853892,-31.0328125));
#305194=CARTESIAN_POINT('Ctrl Pts',(0.,6.09472152853892,-30.9453125));
#305195=CARTESIAN_POINT('Ctrl Pts',(-1.98029506767702,6.09472152853892,
-30.8578125));
#305196=CARTESIAN_POINT('Ctrl Pts',(-3.58238743130462,4.93073329257085,
-30.7703125));
#305197=CARTESIAN_POINT('Ctrl Pts',(-5.18447979493222,3.76674505660277,
-30.6828125));
#305198=CARTESIAN_POINT('Ctrl Pts',(-5.7964246247213,1.88337252830138,-30.5953125));
#305199=CARTESIAN_POINT('Ctrl Pts',(-6.40836945451038,2.69233120697773E-15,
-30.5078125));
#305200=CARTESIAN_POINT('Ctrl Pts',(-5.7964246247213,-1.88337252830138,
-30.4203125));
#305201=CARTESIAN_POINT('Ctrl Pts',(-5.18447979493222,-3.76674505660276,
-30.3328125));
#305202=CARTESIAN_POINT('Ctrl Pts',(-3.58238743130462,-4.93073329257084,
-30.2453125));
#305203=CARTESIAN_POINT('Ctrl Pts',(-1.98029506767702,-6.09472152853892,
-30.1578125));
#305204=CARTESIAN_POINT('Ctrl Pts',(-7.46388121161966E-16,-6.09472152853892,
-30.0703125));
#305205=CARTESIAN_POINT('Ctrl Pts',(1.98029506767702,-6.09472152853892,
-29.9828125));
#305206=CARTESIAN_POINT('Ctrl Pts',(3.58238743130462,-4.93073329257084,
-29.8953125));
#305207=CARTESIAN_POINT('Ctrl Pts',(5.18447979493222,-3.76674505660277,
-29.8078125));
#305208=CARTESIAN_POINT('Ctrl Pts',(5.7964246247213,-1.88337252830138,-29.7203125));
#305209=CARTESIAN_POINT('Ctrl Pts',(6.40836945451038,1.15005831063974E-15,
-29.6328125));
#305210=CARTESIAN_POINT('Ctrl Pts',(5.7964246247213,1.88337252830138,-29.5453125));
#305211=CARTESIAN_POINT('Ctrl Pts',(5.18447979493222,3.76674505660277,-29.4578125));
#305212=CARTESIAN_POINT('Ctrl Pts',(3.58238743130462,4.93073329257085,-29.3703125));
#305213=CARTESIAN_POINT('Ctrl Pts',(1.98029506767702,6.09472152853892,-29.2828125));
#305214=CARTESIAN_POINT('Ctrl Pts',(0.,6.09472152853892,-29.1953125));
#305215=CARTESIAN_POINT('Ctrl Pts',(-1.98029506767702,6.09472152853892,
-29.1078125));
#305216=CARTESIAN_POINT('Ctrl Pts',(-3.58238743130462,4.93073329257085,
-29.0203125));
#305217=CARTESIAN_POINT('Ctrl Pts',(-5.18447979493222,3.76674505660277,
-28.9328125));
#305218=CARTESIAN_POINT('Ctrl Pts',(-5.7964246247213,1.88337252830138,-28.8453125));
#305219=CARTESIAN_POINT('Ctrl Pts',(-6.40836945451038,2.74698107038968E-15,
-28.7578125));
#305220=CARTESIAN_POINT('Ctrl Pts',(-5.7964246247213,-1.88337252830138,
-28.6703125));
#305221=CARTESIAN_POINT('Ctrl Pts',(-5.18447979493222,-3.76674505660276,
-28.5828125));
#305222=CARTESIAN_POINT('Ctrl Pts',(-3.58238743130462,-4.93073329257084,
-28.4953125));
#305223=CARTESIAN_POINT('Ctrl Pts',(-1.98029506767702,-6.09472152853892,
-28.4078125));
#305224=CARTESIAN_POINT('Ctrl Pts',(-7.46388121161966E-16,-6.09472152853892,
-28.3203125));
#305225=CARTESIAN_POINT('Ctrl Pts',(1.98029506767702,-6.09472152853892,
-28.2328125));
#305226=CARTESIAN_POINT('Ctrl Pts',(3.58238743130462,-4.93073329257084,
-28.1453125));
#305227=CARTESIAN_POINT('Ctrl Pts',(5.18447979493222,-3.76674505660277,
-28.0578125));
#305228=CARTESIAN_POINT('Ctrl Pts',(5.7964246247213,-1.88337252830138,-27.9703125));
#305229=CARTESIAN_POINT('Ctrl Pts',(6.40836945451038,1.20470817405169E-15,
-27.8828125));
#305230=CARTESIAN_POINT('Ctrl Pts',(5.7964246247213,1.88337252830138,-27.7953125));
#305231=CARTESIAN_POINT('Ctrl Pts',(5.18447979493222,3.76674505660277,-27.7078125));
#305232=CARTESIAN_POINT('Ctrl Pts',(3.58238743130462,4.93073329257085,-27.6203125));
#305233=CARTESIAN_POINT('Ctrl Pts',(1.98029506767702,6.09472152853892,-27.5328125));
#305234=CARTESIAN_POINT('Ctrl Pts',(0.,6.09472152853892,-27.4453125));
#305235=CARTESIAN_POINT('Ctrl Pts',(-1.98029506767702,6.09472152853892,
-27.3578125));
#305236=CARTESIAN_POINT('Ctrl Pts',(-3.58238743130462,4.93073329257085,
-27.2703125));
#305237=CARTESIAN_POINT('Ctrl Pts',(-5.18447979493222,3.76674505660277,
-27.1828125));
#305238=CARTESIAN_POINT('Ctrl Pts',(-5.7964246247213,1.88337252830138,-27.0953125));
#305239=CARTESIAN_POINT('Ctrl Pts',(-6.40836945451038,2.80163093380163E-15,
-27.0078125));
#305240=CARTESIAN_POINT('Ctrl Pts',(-5.7964246247213,-1.88337252830138,
-26.9203125));
#305241=CARTESIAN_POINT('Ctrl Pts',(-5.18447979493222,-3.76674505660276,
-26.8328125));
#305242=CARTESIAN_POINT('Ctrl Pts',(-3.58238743130462,-4.93073329257084,
-26.7453125));
#305243=CARTESIAN_POINT('Ctrl Pts',(-1.98029506767702,-6.09472152853892,
-26.6578125));
#305244=CARTESIAN_POINT('Ctrl Pts',(-7.46388121161966E-16,-6.09472152853892,
-26.5703125));
#305245=CARTESIAN_POINT('Ctrl Pts',(1.98029506767702,-6.09472152853892,
-26.4828125));
#305246=CARTESIAN_POINT('Ctrl Pts',(3.58238743130462,-4.93073329257084,
-26.3953125));
#305247=CARTESIAN_POINT('Ctrl Pts',(5.18447979493222,-3.76674505660277,
-26.3078125));
#305248=CARTESIAN_POINT('Ctrl Pts',(5.7964246247213,-1.88337252830138,-26.2203125));
#305249=CARTESIAN_POINT('Ctrl Pts',(6.40836945451038,1.25935803746364E-15,
-26.1328125));
#305250=CARTESIAN_POINT('Ctrl Pts',(5.7964246247213,1.88337252830138,-26.0453125));
#305251=CARTESIAN_POINT('Ctrl Pts',(5.18447979493222,3.76674505660277,-25.9578125));
#305252=CARTESIAN_POINT('Ctrl Pts',(3.58238743130462,4.93073329257085,-25.8703125));
#305253=CARTESIAN_POINT('Ctrl Pts',(1.98029506767702,6.09472152853892,-25.7828125));
#305254=CARTESIAN_POINT('Ctrl Pts',(0.,6.09472152853892,-25.6953125));
#305255=CARTESIAN_POINT('Ctrl Pts',(-1.98029506767702,6.09472152853892,
-25.6078125));
#305256=CARTESIAN_POINT('Ctrl Pts',(-3.58238743130462,4.93073329257085,
-25.5203125));
#305257=CARTESIAN_POINT('Ctrl Pts',(-5.18447979493222,3.76674505660277,
-25.4328125));
#305258=CARTESIAN_POINT('Ctrl Pts',(-5.7964246247213,1.88337252830138,-25.3453125));
#305259=CARTESIAN_POINT('Ctrl Pts',(-6.40836945451038,2.85628079721358E-15,
-25.2578125));
#305260=CARTESIAN_POINT('Ctrl Pts',(-5.7964246247213,-1.88337252830138,
-25.1703125));
#305261=CARTESIAN_POINT('Ctrl Pts',(-5.18447979493222,-3.76674505660276,
-25.0828125));
#305262=CARTESIAN_POINT('Ctrl Pts',(-3.58238743130462,-4.93073329257084,
-24.9953125));
#305263=CARTESIAN_POINT('Ctrl Pts',(-1.98029506767702,-6.09472152853892,
-24.9078125));
#305264=CARTESIAN_POINT('Ctrl Pts',(-7.46388121161966E-16,-6.09472152853892,
-24.8203125));
#305265=CARTESIAN_POINT('Ctrl Pts',(1.98029506767702,-6.09472152853892,
-24.7328125));
#305266=CARTESIAN_POINT('Ctrl Pts',(3.58238743130462,-4.93073329257084,
-24.6453125));
#305267=CARTESIAN_POINT('Ctrl Pts',(5.18447979493222,-3.76674505660277,
-24.5578125));
#305268=CARTESIAN_POINT('Ctrl Pts',(5.7964246247213,-1.88337252830138,-24.4703125));
#305269=CARTESIAN_POINT('Ctrl Pts',(6.40836945451038,1.31400790087559E-15,
-24.3828125));
#305270=CARTESIAN_POINT('Ctrl Pts',(5.7964246247213,1.88337252830138,-24.2953125));
#305271=CARTESIAN_POINT('Ctrl Pts',(5.18447979493222,3.76674505660277,-24.2078125));
#305272=CARTESIAN_POINT('Ctrl Pts',(3.58238743130462,4.93073329257085,-24.1203125));
#305273=CARTESIAN_POINT('Ctrl Pts',(1.98029506767702,6.09472152853892,-24.0328125));
#305274=CARTESIAN_POINT('Ctrl Pts',(0.,6.09472152853892,-23.9453125));
#305275=CARTESIAN_POINT('Ctrl Pts',(-1.98029506767702,6.09472152853892,
-23.8578125));
#305276=CARTESIAN_POINT('Ctrl Pts',(-3.58238743130462,4.93073329257085,
-23.7703125));
#305277=CARTESIAN_POINT('Ctrl Pts',(-5.18447979493222,3.76674505660277,
-23.6828125));
#305278=CARTESIAN_POINT('Ctrl Pts',(-5.7964246247213,1.88337252830138,-23.5953125));
#305279=CARTESIAN_POINT('Ctrl Pts',(-6.40836945451038,2.91093066062553E-15,
-23.5078125));
#305280=CARTESIAN_POINT('Ctrl Pts',(-5.7964246247213,-1.88337252830138,
-23.4203125));
#305281=CARTESIAN_POINT('Ctrl Pts',(-5.18447979493222,-3.76674505660276,
-23.3328125));
#305282=CARTESIAN_POINT('Ctrl Pts',(-3.58238743130462,-4.93073329257084,
-23.2453125));
#305283=CARTESIAN_POINT('Ctrl Pts',(-1.98029506767702,-6.09472152853892,
-23.1578125));
#305284=CARTESIAN_POINT('Ctrl Pts',(-7.46388121161966E-16,-6.09472152853892,
-23.0703125));
#305285=CARTESIAN_POINT('Ctrl Pts',(1.98029506767702,-6.09472152853892,
-22.9828125));
#305286=CARTESIAN_POINT('Ctrl Pts',(3.58238743130462,-4.93073329257084,
-22.8953125));
#305287=CARTESIAN_POINT('Ctrl Pts',(5.18447979493222,-3.76674505660277,
-22.8078125));
#305288=CARTESIAN_POINT('Ctrl Pts',(5.7964246247213,-1.88337252830138,-22.7203125));
#305289=CARTESIAN_POINT('Ctrl Pts',(6.40836945451038,1.36865776428754E-15,
-22.6328125));
#305290=CARTESIAN_POINT('Ctrl Pts',(5.7964246247213,1.88337252830138,-22.5453125));
#305291=CARTESIAN_POINT('Ctrl Pts',(5.18447979493222,3.76674505660277,-22.4578125));
#305292=CARTESIAN_POINT('Ctrl Pts',(3.58238743130462,4.93073329257085,-22.3703125));
#305293=CARTESIAN_POINT('Ctrl Pts',(1.98029506767702,6.09472152853892,-22.2828125));
#305294=CARTESIAN_POINT('Ctrl Pts',(0.,6.09472152853893,-22.1953125));
#305295=CARTESIAN_POINT('Ctrl Pts',(-1.98029506767702,6.09472152853892,
-22.1078125));
#305296=CARTESIAN_POINT('Ctrl Pts',(-3.58238743130462,4.93073329257085,
-22.0203125));
#305297=CARTESIAN_POINT('Ctrl Pts',(-5.18447979493222,3.76674505660277,
-21.9328125));
#305298=CARTESIAN_POINT('Ctrl Pts',(-5.7964246247213,1.88337252830138,-21.8453125));
#305299=CARTESIAN_POINT('Ctrl Pts',(-6.40836945451038,2.96558052403748E-15,
-21.7578125));
#305300=CARTESIAN_POINT('Ctrl Pts',(-5.7964246247213,-1.88337252830138,
-21.6703125));
#305301=CARTESIAN_POINT('Ctrl Pts',(-5.18447979493222,-3.76674505660276,
-21.5828125));
#305302=CARTESIAN_POINT('Ctrl Pts',(-3.58238743130462,-4.93073329257084,
-21.4953125));
#305303=CARTESIAN_POINT('Ctrl Pts',(-1.98029506767702,-6.09472152853892,
-21.4078125));
#305304=CARTESIAN_POINT('Ctrl Pts',(-7.46388121161966E-16,-6.09472152853892,
-21.3203125));
#305305=CARTESIAN_POINT('Ctrl Pts',(1.98029506767702,-6.09472152853892,
-21.2328125));
#305306=CARTESIAN_POINT('Ctrl Pts',(3.58238743130462,-4.93073329257084,
-21.1453125));
#305307=CARTESIAN_POINT('Ctrl Pts',(5.18447979493222,-3.76674505660277,
-21.0578125));
#305308=CARTESIAN_POINT('Ctrl Pts',(5.7964246247213,-1.88337252830138,-20.9703125));
#305309=CARTESIAN_POINT('Ctrl Pts',(6.40836945451038,1.42330762769949E-15,
-20.8828125));
#305310=CARTESIAN_POINT('Ctrl Pts',(5.7964246247213,1.88337252830138,-20.7953125));
#305311=CARTESIAN_POINT('Ctrl Pts',(5.18447979493222,3.76674505660277,-20.7078125));
#305312=CARTESIAN_POINT('Ctrl Pts',(3.58238743130462,4.93073329257085,-20.6203125));
#305313=CARTESIAN_POINT('Ctrl Pts',(1.98029506767702,6.09472152853892,-20.5328125));
#305314=CARTESIAN_POINT('Ctrl Pts',(0.,6.09472152853893,-20.4453125));
#305315=CARTESIAN_POINT('Ctrl Pts',(-1.98029506767702,6.09472152853892,
-20.3578125));
#305316=CARTESIAN_POINT('Ctrl Pts',(-3.58238743130462,4.93073329257085,
-20.2703125));
#305317=CARTESIAN_POINT('Ctrl Pts',(-5.18447979493222,3.76674505660277,
-20.1828125));
#305318=CARTESIAN_POINT('Ctrl Pts',(-5.7964246247213,1.88337252830138,-20.0953125));
#305319=CARTESIAN_POINT('Ctrl Pts',(-6.40836945451038,3.02023038744943E-15,
-20.0078125));
#305320=CARTESIAN_POINT('Ctrl Pts',(-5.7964246247213,-1.88337252830138,
-19.9203125));
#305321=CARTESIAN_POINT('Ctrl Pts',(-5.18447979493222,-3.76674505660276,
-19.8328125));
#305322=CARTESIAN_POINT('Ctrl Pts',(-3.58238743130462,-4.93073329257084,
-19.7453125));
#305323=CARTESIAN_POINT('Ctrl Pts',(-1.98029506767702,-6.09472152853892,
-19.6578125));
#305324=CARTESIAN_POINT('Ctrl Pts',(-7.46388121161966E-16,-6.09472152853892,
-19.5703125));
#305325=CARTESIAN_POINT('Ctrl Pts',(1.98029506767702,-6.09472152853892,
-19.4828125));
#305326=CARTESIAN_POINT('Ctrl Pts',(3.58238743130462,-4.93073329257084,
-19.3953125));
#305327=CARTESIAN_POINT('Ctrl Pts',(5.18447979493222,-3.76674505660277,
-19.3078125));
#305328=CARTESIAN_POINT('Ctrl Pts',(5.7964246247213,-1.88337252830138,-19.2203125));
#305329=CARTESIAN_POINT('Ctrl Pts',(6.40836945451038,1.47795749111144E-15,
-19.1328125));
#305330=CARTESIAN_POINT('Ctrl Pts',(5.7964246247213,1.88337252830138,-19.0453125));
#305331=CARTESIAN_POINT('Ctrl Pts',(5.18447979493222,3.76674505660277,-18.9578125));
#305332=CARTESIAN_POINT('Ctrl Pts',(3.58238743130462,4.93073329257085,-18.8703125));
#305333=CARTESIAN_POINT('Ctrl Pts',(1.98029506767702,6.09472152853892,-18.7828125));
#305334=CARTESIAN_POINT('Ctrl Pts',(0.,6.09472152853893,-18.6953125));
#305335=CARTESIAN_POINT('Ctrl Pts',(-1.98029506767702,6.09472152853892,
-18.6078125));
#305336=CARTESIAN_POINT('Ctrl Pts',(-3.58238743130462,4.93073329257085,
-18.5203125));
#305337=CARTESIAN_POINT('Ctrl Pts',(-5.18447979493222,3.76674505660277,
-18.4328125));
#305338=CARTESIAN_POINT('Ctrl Pts',(-5.7964246247213,1.88337252830138,-18.3453125));
#305339=CARTESIAN_POINT('Ctrl Pts',(-6.40836945451038,3.07488025086138E-15,
-18.2578125));
#305340=CARTESIAN_POINT('Ctrl Pts',(-5.7964246247213,-1.88337252830138,
-18.1703125));
#305341=CARTESIAN_POINT('Ctrl Pts',(-5.18447979493222,-3.76674505660276,
-18.0828125));
#305342=CARTESIAN_POINT('Ctrl Pts',(-3.58238743130462,-4.93073329257084,
-17.9953125));
#305343=CARTESIAN_POINT('Ctrl Pts',(-1.98029506767702,-6.09472152853892,
-17.9078125));
#305344=CARTESIAN_POINT('Ctrl Pts',(-7.46388121161966E-16,-6.09472152853892,
-17.8203125));
#305345=CARTESIAN_POINT('Ctrl Pts',(1.98029506767702,-6.09472152853892,
-17.7328125));
#305346=CARTESIAN_POINT('Ctrl Pts',(3.58238743130462,-4.93073329257084,
-17.6453125));
#305347=CARTESIAN_POINT('Ctrl Pts',(5.18447979493222,-3.76674505660277,
-17.5578125));
#305348=CARTESIAN_POINT('Ctrl Pts',(5.7964246247213,-1.88337252830138,-17.4703125));
#305349=CARTESIAN_POINT('Ctrl Pts',(6.40836945451038,1.5326073545234E-15,
-17.3828125));
#305350=CARTESIAN_POINT('Ctrl Pts',(5.7964246247213,1.88337252830138,-17.2953125));
#305351=CARTESIAN_POINT('Ctrl Pts',(5.18447979493222,3.76674505660277,-17.2078125));
#305352=CARTESIAN_POINT('Ctrl Pts',(3.58238743130462,4.93073329257085,-17.1203125));
#305353=CARTESIAN_POINT('Ctrl Pts',(1.98029506767702,6.09472152853892,-17.0328125));
#305354=CARTESIAN_POINT('Ctrl Pts',(0.,6.09472152853893,-16.9453125));
#305355=CARTESIAN_POINT('Ctrl Pts',(-1.98029506767702,6.09472152853892,
-16.8578125));
#305356=CARTESIAN_POINT('Ctrl Pts',(-3.58238743130462,4.93073329257085,
-16.7703125));
#305357=CARTESIAN_POINT('Ctrl Pts',(-5.18447979493222,3.76674505660277,
-16.6828125));
#305358=CARTESIAN_POINT('Ctrl Pts',(-5.7964246247213,1.88337252830138,-16.5953125));
#305359=CARTESIAN_POINT('Ctrl Pts',(-6.40836945451038,3.12953011427333E-15,
-16.5078125));
#305360=CARTESIAN_POINT('Ctrl Pts',(-5.7964246247213,-1.88337252830138,
-16.4203125));
#305361=CARTESIAN_POINT('Ctrl Pts',(-5.18447979493222,-3.76674505660276,
-16.3328125));
#305362=CARTESIAN_POINT('Ctrl Pts',(-3.58238743130462,-4.93073329257084,
-16.2453125));
#305363=CARTESIAN_POINT('Ctrl Pts',(-1.98029506767702,-6.09472152853892,
-16.1578125));
#305364=CARTESIAN_POINT('Ctrl Pts',(-7.46388121161966E-16,-6.09472152853892,
-16.0703125));
#305365=CARTESIAN_POINT('Ctrl Pts',(1.98029506767702,-6.09472152853892,
-15.9828125));
#305366=CARTESIAN_POINT('Ctrl Pts',(3.58238743130462,-4.93073329257084,
-15.8953125));
#305367=CARTESIAN_POINT('Ctrl Pts',(5.18447979493222,-3.76674505660277,
-15.8078125));
#305368=CARTESIAN_POINT('Ctrl Pts',(5.7964246247213,-1.88337252830138,-15.7203125));
#305369=CARTESIAN_POINT('Ctrl Pts',(6.40836945451038,1.58725721793535E-15,
-15.6328125));
#305370=CARTESIAN_POINT('Ctrl Pts',(5.7964246247213,1.88337252830138,-15.5453125));
#305371=CARTESIAN_POINT('Ctrl Pts',(5.18447979493222,3.76674505660277,-15.4578125));
#305372=CARTESIAN_POINT('Ctrl Pts',(3.58238743130462,4.93073329257085,-15.3703125));
#305373=CARTESIAN_POINT('Ctrl Pts',(1.98029506767702,6.09472152853892,-15.2828125));
#305374=CARTESIAN_POINT('Ctrl Pts',(0.,6.09472152853893,-15.1953125));
#305375=CARTESIAN_POINT('Ctrl Pts',(-1.98029506767702,6.09472152853892,
-15.1078125));
#305376=CARTESIAN_POINT('Ctrl Pts',(-3.58238743130462,4.93073329257085,
-15.0203125));
#305377=CARTESIAN_POINT('Ctrl Pts',(-5.18447979493222,3.76674505660277,
-14.9328125));
#305378=CARTESIAN_POINT('Ctrl Pts',(-5.7964246247213,1.88337252830138,-14.8453125));
#305379=CARTESIAN_POINT('Ctrl Pts',(-6.40836945451038,3.18417997768528E-15,
-14.7578125));
#305380=CARTESIAN_POINT('Ctrl Pts',(-5.7964246247213,-1.88337252830138,
-14.6703125));
#305381=CARTESIAN_POINT('Ctrl Pts',(-5.18447979493222,-3.76674505660276,
-14.5828125));
#305382=CARTESIAN_POINT('Ctrl Pts',(-3.58238743130462,-4.93073329257084,
-14.4953125));
#305383=CARTESIAN_POINT('Ctrl Pts',(-1.98029506767702,-6.09472152853892,
-14.4078125));
#305384=CARTESIAN_POINT('Ctrl Pts',(-7.46388121161966E-16,-6.09472152853892,
-14.3203125));
#305385=CARTESIAN_POINT('Ctrl Pts',(1.98029506767702,-6.09472152853892,
-14.2328125));
#305386=CARTESIAN_POINT('Ctrl Pts',(3.58238743130462,-4.93073329257084,
-14.1453125));
#305387=CARTESIAN_POINT('Ctrl Pts',(5.18447979493222,-3.76674505660277,
-14.0578125));
#305388=CARTESIAN_POINT('Ctrl Pts',(5.7964246247213,-1.88337252830138,-13.9703125));
#305389=CARTESIAN_POINT('Ctrl Pts',(6.40836945451038,1.6419070813473E-15,
-13.8828125));
#305390=CARTESIAN_POINT('Ctrl Pts',(5.7964246247213,1.88337252830138,-13.7953125));
#305391=CARTESIAN_POINT('Ctrl Pts',(5.18447979493222,3.76674505660277,-13.7078125));
#305392=CARTESIAN_POINT('Ctrl Pts',(3.58238743130462,4.93073329257085,-13.6203125));
#305393=CARTESIAN_POINT('Ctrl Pts',(1.98029506767702,6.09472152853892,-13.5328125));
#305394=CARTESIAN_POINT('Ctrl Pts',(0.,6.09472152853893,-13.4453125));
#305395=CARTESIAN_POINT('Ctrl Pts',(-1.98029506767702,6.09472152853892,
-13.3578125));
#305396=CARTESIAN_POINT('Ctrl Pts',(-3.58238743130462,4.93073329257085,
-13.2703125));
#305397=CARTESIAN_POINT('Ctrl Pts',(-5.18447979493222,3.76674505660277,
-13.1828125));
#305398=CARTESIAN_POINT('Ctrl Pts',(-5.7964246247213,1.88337252830138,-13.0953125));
#305399=CARTESIAN_POINT('Ctrl Pts',(-6.40836945451038,3.23882984109724E-15,
-13.0078125));
#305400=CARTESIAN_POINT('Ctrl Pts',(-5.7964246247213,-1.88337252830138,
-12.9203125));
#305401=CARTESIAN_POINT('Ctrl Pts',(-5.18447979493222,-3.76674505660276,
-12.8328125));
#305402=CARTESIAN_POINT('Ctrl Pts',(-3.58238743130462,-4.93073329257084,
-12.7453125));
#305403=CARTESIAN_POINT('Ctrl Pts',(-1.98029506767702,-6.09472152853892,
-12.6578125));
#305404=CARTESIAN_POINT('Ctrl Pts',(-7.46388121161966E-16,-6.09472152853892,
-12.5703125));
#305405=CARTESIAN_POINT('Ctrl Pts',(1.98029506767702,-6.09472152853892,
-12.4828125));
#305406=CARTESIAN_POINT('Ctrl Pts',(3.58238743130462,-4.93073329257084,
-12.3953125));
#305407=CARTESIAN_POINT('Ctrl Pts',(5.18447979493222,-3.76674505660277,
-12.3078125));
#305408=CARTESIAN_POINT('Ctrl Pts',(5.7964246247213,-1.88337252830138,-12.2203125));
#305409=CARTESIAN_POINT('Ctrl Pts',(6.40836945451038,1.69655694475925E-15,
-12.1328125));
#305410=CARTESIAN_POINT('Ctrl Pts',(5.7964246247213,1.88337252830138,-12.0453125));
#305411=CARTESIAN_POINT('Ctrl Pts',(5.18447979493222,3.76674505660277,-11.9578125));
#305412=CARTESIAN_POINT('Ctrl Pts',(3.58238743130462,4.93073329257085,-11.8703125));
#305413=CARTESIAN_POINT('Ctrl Pts',(1.98029506767702,6.09472152853892,-11.7828125));
#305414=CARTESIAN_POINT('Ctrl Pts',(0.,6.09472152853893,-11.6953125));
#305415=CARTESIAN_POINT('Ctrl Pts',(-1.98029506767702,6.09472152853892,
-11.6078125));
#305416=CARTESIAN_POINT('Ctrl Pts',(-3.58238743130462,4.93073329257085,
-11.5203125));
#305417=CARTESIAN_POINT('Ctrl Pts',(-5.18447979493222,3.76674505660277,
-11.4328125));
#305418=CARTESIAN_POINT('Ctrl Pts',(-5.7964246247213,1.88337252830138,-11.3453125));
#305419=CARTESIAN_POINT('Ctrl Pts',(-6.40836945451038,3.29347970450919E-15,
-11.2578125));
#305420=CARTESIAN_POINT('Ctrl Pts',(-5.7964246247213,-1.88337252830138,
-11.1703125));
#305421=CARTESIAN_POINT('Ctrl Pts',(-5.18447979493222,-3.76674505660276,
-11.0828125));
#305422=CARTESIAN_POINT('Ctrl Pts',(-3.58238743130462,-4.93073329257084,
-10.9953125));
#305423=CARTESIAN_POINT('Ctrl Pts',(-1.98029506767702,-6.09472152853892,
-10.9078125));
#305424=CARTESIAN_POINT('Ctrl Pts',(-7.46388121161966E-16,-6.09472152853892,
-10.8203125));
#305425=CARTESIAN_POINT('Ctrl Pts',(1.98029506767702,-6.09472152853892,
-10.7328125));
#305426=CARTESIAN_POINT('Ctrl Pts',(3.58238743130462,-4.93073329257084,
-10.6453125));
#305427=CARTESIAN_POINT('Ctrl Pts',(5.18447979493222,-3.76674505660277,
-10.5578125));
#305428=CARTESIAN_POINT('Ctrl Pts',(5.7964246247213,-1.88337252830138,-10.4703125));
#305429=CARTESIAN_POINT('Ctrl Pts',(6.40836945451038,1.7512068081712E-15,
-10.3828125));
#305430=CARTESIAN_POINT('Ctrl Pts',(5.7964246247213,1.88337252830138,-10.2953125));
#305431=CARTESIAN_POINT('Ctrl Pts',(5.18447979493222,3.76674505660277,-10.2078125));
#305432=CARTESIAN_POINT('Ctrl Pts',(3.58238743130462,4.93073329257085,-10.1203125));
#305433=CARTESIAN_POINT('Ctrl Pts',(1.98029506767702,6.09472152853892,-10.0328125));
#305434=CARTESIAN_POINT('Ctrl Pts',(0.,6.09472152853893,-9.94531250000001));
#305435=CARTESIAN_POINT('Ctrl Pts',(-1.98029506767702,6.09472152853892,
-9.85781250000001));
#305436=CARTESIAN_POINT('Ctrl Pts',(-3.58238743130462,4.93073329257085,
-9.77031250000001));
#305437=CARTESIAN_POINT('Ctrl Pts',(-5.18447979493222,3.76674505660277,
-9.6828125));
#305438=CARTESIAN_POINT('Ctrl Pts',(-5.7964246247213,1.88337252830138,-9.59531250000001));
#305439=CARTESIAN_POINT('Ctrl Pts',(-6.40836945451038,3.34812956792114E-15,
-9.50781250000001));
#305440=CARTESIAN_POINT('Ctrl Pts',(-5.7964246247213,-1.88337252830138,
-9.42031250000001));
#305441=CARTESIAN_POINT('Ctrl Pts',(-5.18447979493222,-3.76674505660276,
-9.3328125));
#305442=CARTESIAN_POINT('Ctrl Pts',(-3.58238743130462,-4.93073329257084,
-9.24531250000001));
#305443=CARTESIAN_POINT('Ctrl Pts',(-1.98029506767702,-6.09472152853892,
-9.15781250000001));
#305444=CARTESIAN_POINT('Ctrl Pts',(-7.46388121161966E-16,-6.09472152853892,
-9.07031250000001));
#305445=CARTESIAN_POINT('Ctrl Pts',(1.98029506767702,-6.09472152853892,
-8.9828125));
#305446=CARTESIAN_POINT('Ctrl Pts',(3.58238743130462,-4.93073329257084,
-8.89531250000001));
#305447=CARTESIAN_POINT('Ctrl Pts',(5.18447979493222,-3.76674505660277,
-8.8078125));
#305448=CARTESIAN_POINT('Ctrl Pts',(5.7964246247213,-1.88337252830138,-8.72031250000001));
#305449=CARTESIAN_POINT('Ctrl Pts',(6.40836945451038,1.80585667158315E-15,
-8.6328125));
#305450=CARTESIAN_POINT('Ctrl Pts',(5.7964246247213,1.88337252830138,-8.54531250000001));
#305451=CARTESIAN_POINT('Ctrl Pts',(5.18447979493222,3.76674505660277,-8.4578125));
#305452=CARTESIAN_POINT('Ctrl Pts',(3.58238743130462,4.93073329257085,-8.37031250000001));
#305453=CARTESIAN_POINT('Ctrl Pts',(1.98029506767702,6.09472152853892,-8.28281250000001));
#305454=CARTESIAN_POINT('Ctrl Pts',(0.,6.09472152853893,-8.19531250000001));
#305455=CARTESIAN_POINT('Ctrl Pts',(-1.98029506767702,6.09472152853892,
-8.10781249999999));
#305456=CARTESIAN_POINT('Ctrl Pts',(-3.58238743130462,4.93073329257085,
-8.02031250000001));
#305457=CARTESIAN_POINT('Ctrl Pts',(-5.18447979493222,3.76674505660277,
-7.9328125));
#305458=CARTESIAN_POINT('Ctrl Pts',(-5.7964246247213,1.88337252830138,-7.84531250000001));
#305459=CARTESIAN_POINT('Ctrl Pts',(-6.40836945451038,3.40277943133309E-15,
-7.7578125));
#305460=CARTESIAN_POINT('Ctrl Pts',(-5.7964246247213,-1.88337252830138,
-7.67031250000001));
#305461=CARTESIAN_POINT('Ctrl Pts',(-5.18447979493222,-3.76674505660276,
-7.5828125));
#305462=CARTESIAN_POINT('Ctrl Pts',(-3.58238743130462,-4.93073329257084,
-7.49531250000001));
#305463=CARTESIAN_POINT('Ctrl Pts',(-1.98029506767702,-6.09472152853892,
-7.4078125));
#305464=CARTESIAN_POINT('Ctrl Pts',(-7.46388121161966E-16,-6.09472152853892,
-7.32031250000001));
#305465=CARTESIAN_POINT('Ctrl Pts',(1.98029506767702,-6.09472152853892,
-7.23281250000001));
#305466=CARTESIAN_POINT('Ctrl Pts',(3.58238743130462,-4.93073329257084,
-7.14531250000001));
#305467=CARTESIAN_POINT('Ctrl Pts',(5.18447979493222,-3.76674505660277,
-7.05781250000001));
#305468=CARTESIAN_POINT('Ctrl Pts',(5.7964246247213,-1.88337252830138,-6.97031250000001));
#305469=CARTESIAN_POINT('Ctrl Pts',(6.40836945451038,1.8605065349951E-15,
-6.8828125));
#305470=CARTESIAN_POINT('Ctrl Pts',(5.7964246247213,1.88337252830138,-6.79531250000001));
#305471=CARTESIAN_POINT('Ctrl Pts',(5.18447979493222,3.76674505660277,-6.7078125));
#305472=CARTESIAN_POINT('Ctrl Pts',(3.58238743130462,4.93073329257085,-6.62031250000001));
#305473=CARTESIAN_POINT('Ctrl Pts',(1.98029506767702,6.09472152853892,-6.5328125));
#305474=CARTESIAN_POINT('Ctrl Pts',(0.,6.09472152853893,-6.44531250000001));
#305475=CARTESIAN_POINT('Ctrl Pts',(-1.98029506767702,6.09472152853892,
-6.35781250000001));
#305476=CARTESIAN_POINT('Ctrl Pts',(-3.58238743130462,4.93073329257085,
-6.27031250000001));
#305477=CARTESIAN_POINT('Ctrl Pts',(-5.18447979493222,3.76674505660277,
-6.18281250000001));
#305478=CARTESIAN_POINT('Ctrl Pts',(-5.7964246247213,1.88337252830138,-6.09531250000001));
#305479=CARTESIAN_POINT('Ctrl Pts',(-6.40836945451038,3.45742929474504E-15,
-6.00781250000001));
#305480=CARTESIAN_POINT('Ctrl Pts',(-5.7964246247213,-1.88337252830138,
-5.92031250000001));
#305481=CARTESIAN_POINT('Ctrl Pts',(-5.18447979493222,-3.76674505660276,
-5.8328125));
#305482=CARTESIAN_POINT('Ctrl Pts',(-3.58238743130462,-4.93073329257084,
-5.74531250000001));
#305483=CARTESIAN_POINT('Ctrl Pts',(-1.98029506767702,-6.09472152853892,
-5.6578125));
#305484=CARTESIAN_POINT('Ctrl Pts',(-7.46388121161966E-16,-6.09472152853892,
-5.57031250000001));
#305485=CARTESIAN_POINT('Ctrl Pts',(1.98029506767702,-6.09472152853892,
-5.48281250000001));
#305486=CARTESIAN_POINT('Ctrl Pts',(3.58238743130462,-4.93073329257084,
-5.39531250000001));
#305487=CARTESIAN_POINT('Ctrl Pts',(5.18447979493222,-3.76674505660277,
-5.30781250000001));
#305488=CARTESIAN_POINT('Ctrl Pts',(5.7964246247213,-1.88337252830138,-5.22031250000001));
#305489=CARTESIAN_POINT('Ctrl Pts',(6.40836945451038,1.91515639840705E-15,
-5.13281250000001));
#305490=CARTESIAN_POINT('Ctrl Pts',(5.7964246247213,1.88337252830138,-5.04531250000001));
#305491=CARTESIAN_POINT('Ctrl Pts',(5.18447979493222,3.76674505660277,-4.9578125));
#305492=CARTESIAN_POINT('Ctrl Pts',(3.58238743130462,4.93073329257085,-4.87031250000001));
#305493=CARTESIAN_POINT('Ctrl Pts',(1.98029506767702,6.09472152853892,-4.7828125));
#305494=CARTESIAN_POINT('Ctrl Pts',(0.,6.09472152853893,-4.69531250000001));
#305495=CARTESIAN_POINT('Ctrl Pts',(-1.98029506767702,6.09472152853892,
-4.60781250000001));
#305496=CARTESIAN_POINT('Ctrl Pts',(-3.58238743130462,4.93073329257085,
-4.52031250000001));
#305497=CARTESIAN_POINT('Ctrl Pts',(-4.25030452462165,4.44546311909431,
-4.48383348855718));
#305498=CARTESIAN_POINT('Ctrl Pts',(-4.76505105107542,3.79998934091675,
-4.44551580562765));
#305499=CARTESIAN_POINT('Ctrl Pts',(0.,4.86332528902566,-36.9062594503621));
#305500=CARTESIAN_POINT('Ctrl Pts',(-1.58019017559203,4.86332528902566,
-36.8187594503621));
#305501=CARTESIAN_POINT('Ctrl Pts',(-2.85859088199032,3.93451280799522,
-36.7312594503621));
#305502=CARTESIAN_POINT('Ctrl Pts',(-4.1369915883886,3.00570032696477,-36.6437594503621));
#305503=CARTESIAN_POINT('Ctrl Pts',(-4.62529720699086,1.50285016348238,
-36.5562594503621));
#305504=CARTESIAN_POINT('Ctrl Pts',(-5.11360282559314,2.42689822422288E-15,
-36.4687594503621));
#305505=CARTESIAN_POINT('Ctrl Pts',(-4.62529720699087,-1.50285016348238,
-36.3812594503621));
#305506=CARTESIAN_POINT('Ctrl Pts',(-4.1369915883886,-3.00570032696476,
-36.2937594503621));
#305507=CARTESIAN_POINT('Ctrl Pts',(-2.85859088199032,-3.93451280799521,
-36.2062594503621));
#305508=CARTESIAN_POINT('Ctrl Pts',(-1.58019017559203,-4.86332528902566,
-36.118759450362));
#305509=CARTESIAN_POINT('Ctrl Pts',(-5.95585574841766E-16,-4.86332528902566,
-36.0312594503621));
#305510=CARTESIAN_POINT('Ctrl Pts',(1.58019017559203,-4.86332528902566,
-35.9437594503621));
#305511=CARTESIAN_POINT('Ctrl Pts',(2.85859088199031,-3.93451280799521,
-35.8562594503621));
#305512=CARTESIAN_POINT('Ctrl Pts',(4.13699158838859,-3.00570032696476,
-35.768759450362));
#305513=CARTESIAN_POINT('Ctrl Pts',(4.62529720699086,-1.50285016348238,
-35.6812594503621));
#305514=CARTESIAN_POINT('Ctrl Pts',(5.11360282559314,1.20175168943416E-15,
-35.5937594503621));
#305515=CARTESIAN_POINT('Ctrl Pts',(4.62529720699087,1.50285016348238,-35.5062594503621));
#305516=CARTESIAN_POINT('Ctrl Pts',(4.1369915883886,3.00570032696477,-35.418759450362));
#305517=CARTESIAN_POINT('Ctrl Pts',(2.85859088199032,3.93451280799522,-35.3312594503621));
#305518=CARTESIAN_POINT('Ctrl Pts',(1.58019017559203,4.86332528902566,-35.2437594503621));
#305519=CARTESIAN_POINT('Ctrl Pts',(0.,4.86332528902566,-35.1562594503621));
#305520=CARTESIAN_POINT('Ctrl Pts',(-1.58019017559203,4.86332528902566,
-35.0687594503621));
#305521=CARTESIAN_POINT('Ctrl Pts',(-2.85859088199032,3.93451280799522,
-34.9812594503621));
#305522=CARTESIAN_POINT('Ctrl Pts',(-4.1369915883886,3.00570032696477,-34.893759450362));
#305523=CARTESIAN_POINT('Ctrl Pts',(-4.62529720699086,1.50285016348238,
-34.8062594503621));
#305524=CARTESIAN_POINT('Ctrl Pts',(-5.11360282559314,2.48154808763483E-15,
-34.7187594503621));
#305525=CARTESIAN_POINT('Ctrl Pts',(-4.62529720699087,-1.50285016348238,
-34.6312594503621));
#305526=CARTESIAN_POINT('Ctrl Pts',(-4.1369915883886,-3.00570032696476,
-34.5437594503621));
#305527=CARTESIAN_POINT('Ctrl Pts',(-2.85859088199032,-3.93451280799521,
-34.4562594503621));
#305528=CARTESIAN_POINT('Ctrl Pts',(-1.58019017559203,-4.86332528902566,
-34.3687594503621));
#305529=CARTESIAN_POINT('Ctrl Pts',(-5.95585574841766E-16,-4.86332528902566,
-34.2812594503621));
#305530=CARTESIAN_POINT('Ctrl Pts',(1.58019017559203,-4.86332528902566,
-34.1937594503621));
#305531=CARTESIAN_POINT('Ctrl Pts',(2.85859088199031,-3.93451280799521,
-34.1062594503621));
#305532=CARTESIAN_POINT('Ctrl Pts',(4.13699158838859,-3.00570032696476,
-34.0187594503621));
#305533=CARTESIAN_POINT('Ctrl Pts',(4.62529720699086,-1.50285016348238,
-33.9312594503621));
#305534=CARTESIAN_POINT('Ctrl Pts',(5.11360282559314,1.25640155284611E-15,
-33.8437594503621));
#305535=CARTESIAN_POINT('Ctrl Pts',(4.62529720699087,1.50285016348238,-33.7562594503621));
#305536=CARTESIAN_POINT('Ctrl Pts',(4.1369915883886,3.00570032696477,-33.6687594503621));
#305537=CARTESIAN_POINT('Ctrl Pts',(2.85859088199032,3.93451280799522,-33.5812594503621));
#305538=CARTESIAN_POINT('Ctrl Pts',(1.58019017559203,4.86332528902566,-33.4937594503621));
#305539=CARTESIAN_POINT('Ctrl Pts',(0.,4.86332528902566,-33.4062594503621));
#305540=CARTESIAN_POINT('Ctrl Pts',(-1.58019017559203,4.86332528902566,
-33.3187594503621));
#305541=CARTESIAN_POINT('Ctrl Pts',(-2.85859088199032,3.93451280799522,
-33.2312594503621));
#305542=CARTESIAN_POINT('Ctrl Pts',(-4.1369915883886,3.00570032696477,-33.1437594503621));
#305543=CARTESIAN_POINT('Ctrl Pts',(-4.62529720699086,1.50285016348238,
-33.0562594503621));
#305544=CARTESIAN_POINT('Ctrl Pts',(-5.11360282559314,2.53619795104679E-15,
-32.9687594503621));
#305545=CARTESIAN_POINT('Ctrl Pts',(-4.62529720699087,-1.50285016348238,
-32.8812594503621));
#305546=CARTESIAN_POINT('Ctrl Pts',(-4.1369915883886,-3.00570032696476,
-32.7937594503621));
#305547=CARTESIAN_POINT('Ctrl Pts',(-2.85859088199032,-3.93451280799521,
-32.7062594503621));
#305548=CARTESIAN_POINT('Ctrl Pts',(-1.58019017559203,-4.86332528902566,
-32.6187594503621));
#305549=CARTESIAN_POINT('Ctrl Pts',(-5.95585574841766E-16,-4.86332528902566,
-32.5312594503621));
#305550=CARTESIAN_POINT('Ctrl Pts',(1.58019017559203,-4.86332528902566,
-32.4437594503621));
#305551=CARTESIAN_POINT('Ctrl Pts',(2.85859088199031,-3.93451280799521,
-32.3562594503621));
#305552=CARTESIAN_POINT('Ctrl Pts',(4.13699158838859,-3.00570032696476,
-32.2687594503621));
#305553=CARTESIAN_POINT('Ctrl Pts',(4.62529720699086,-1.50285016348238,
-32.1812594503621));
#305554=CARTESIAN_POINT('Ctrl Pts',(5.11360282559314,1.31105141625806E-15,
-32.0937594503621));
#305555=CARTESIAN_POINT('Ctrl Pts',(4.62529720699087,1.50285016348238,-32.0062594503621));
#305556=CARTESIAN_POINT('Ctrl Pts',(4.1369915883886,3.00570032696477,-31.9187594503621));
#305557=CARTESIAN_POINT('Ctrl Pts',(2.85859088199032,3.93451280799522,-31.8312594503621));
#305558=CARTESIAN_POINT('Ctrl Pts',(1.58019017559203,4.86332528902566,-31.7437594503621));
#305559=CARTESIAN_POINT('Ctrl Pts',(0.,4.86332528902566,-31.6562594503621));
#305560=CARTESIAN_POINT('Ctrl Pts',(-1.58019017559203,4.86332528902566,
-31.5687594503621));
#305561=CARTESIAN_POINT('Ctrl Pts',(-2.85859088199032,3.93451280799522,
-31.4812594503621));
#305562=CARTESIAN_POINT('Ctrl Pts',(-4.1369915883886,3.00570032696477,-31.3937594503621));
#305563=CARTESIAN_POINT('Ctrl Pts',(-4.62529720699086,1.50285016348238,
-31.3062594503621));
#305564=CARTESIAN_POINT('Ctrl Pts',(-5.11360282559314,2.59084781445874E-15,
-31.2187594503621));
#305565=CARTESIAN_POINT('Ctrl Pts',(-4.62529720699087,-1.50285016348238,
-31.1312594503621));
#305566=CARTESIAN_POINT('Ctrl Pts',(-4.1369915883886,-3.00570032696476,
-31.0437594503621));
#305567=CARTESIAN_POINT('Ctrl Pts',(-2.85859088199032,-3.93451280799521,
-30.9562594503621));
#305568=CARTESIAN_POINT('Ctrl Pts',(-1.58019017559203,-4.86332528902566,
-30.8687594503621));
#305569=CARTESIAN_POINT('Ctrl Pts',(-5.95585574841766E-16,-4.86332528902566,
-30.7812594503621));
#305570=CARTESIAN_POINT('Ctrl Pts',(1.58019017559203,-4.86332528902566,
-30.6937594503621));
#305571=CARTESIAN_POINT('Ctrl Pts',(2.85859088199031,-3.93451280799521,
-30.6062594503621));
#305572=CARTESIAN_POINT('Ctrl Pts',(4.13699158838859,-3.00570032696476,
-30.5187594503621));
#305573=CARTESIAN_POINT('Ctrl Pts',(4.62529720699086,-1.50285016348238,
-30.4312594503621));
#305574=CARTESIAN_POINT('Ctrl Pts',(5.11360282559314,1.36570127967001E-15,
-30.3437594503621));
#305575=CARTESIAN_POINT('Ctrl Pts',(4.62529720699087,1.50285016348238,-30.2562594503621));
#305576=CARTESIAN_POINT('Ctrl Pts',(4.1369915883886,3.00570032696477,-30.1687594503621));
#305577=CARTESIAN_POINT('Ctrl Pts',(2.85859088199032,3.93451280799522,-30.0812594503621));
#305578=CARTESIAN_POINT('Ctrl Pts',(1.58019017559203,4.86332528902566,-29.9937594503621));
#305579=CARTESIAN_POINT('Ctrl Pts',(0.,4.86332528902566,-29.9062594503621));
#305580=CARTESIAN_POINT('Ctrl Pts',(-1.58019017559203,4.86332528902566,
-29.8187594503621));
#305581=CARTESIAN_POINT('Ctrl Pts',(-2.85859088199032,3.93451280799522,
-29.7312594503621));
#305582=CARTESIAN_POINT('Ctrl Pts',(-4.1369915883886,3.00570032696477,-29.6437594503621));
#305583=CARTESIAN_POINT('Ctrl Pts',(-4.62529720699086,1.50285016348238,
-29.5562594503621));
#305584=CARTESIAN_POINT('Ctrl Pts',(-5.11360282559314,2.64549767787069E-15,
-29.4687594503621));
#305585=CARTESIAN_POINT('Ctrl Pts',(-4.62529720699087,-1.50285016348238,
-29.3812594503621));
#305586=CARTESIAN_POINT('Ctrl Pts',(-4.1369915883886,-3.00570032696476,
-29.2937594503621));
#305587=CARTESIAN_POINT('Ctrl Pts',(-2.85859088199032,-3.93451280799521,
-29.2062594503621));
#305588=CARTESIAN_POINT('Ctrl Pts',(-1.58019017559203,-4.86332528902566,
-29.1187594503621));
#305589=CARTESIAN_POINT('Ctrl Pts',(-5.95585574841766E-16,-4.86332528902566,
-29.0312594503621));
#305590=CARTESIAN_POINT('Ctrl Pts',(1.58019017559203,-4.86332528902566,
-28.9437594503621));
#305591=CARTESIAN_POINT('Ctrl Pts',(2.85859088199031,-3.93451280799521,
-28.8562594503621));
#305592=CARTESIAN_POINT('Ctrl Pts',(4.13699158838859,-3.00570032696476,
-28.7687594503621));
#305593=CARTESIAN_POINT('Ctrl Pts',(4.62529720699086,-1.50285016348238,
-28.6812594503621));
#305594=CARTESIAN_POINT('Ctrl Pts',(5.11360282559314,1.42035114308196E-15,
-28.5937594503621));
#305595=CARTESIAN_POINT('Ctrl Pts',(4.62529720699087,1.50285016348238,-28.5062594503621));
#305596=CARTESIAN_POINT('Ctrl Pts',(4.1369915883886,3.00570032696477,-28.4187594503621));
#305597=CARTESIAN_POINT('Ctrl Pts',(2.85859088199032,3.93451280799522,-28.3312594503621));
#305598=CARTESIAN_POINT('Ctrl Pts',(1.58019017559203,4.86332528902566,-28.2437594503621));
#305599=CARTESIAN_POINT('Ctrl Pts',(0.,4.86332528902566,-28.1562594503621));
#305600=CARTESIAN_POINT('Ctrl Pts',(-1.58019017559203,4.86332528902566,
-28.0687594503621));
#305601=CARTESIAN_POINT('Ctrl Pts',(-2.85859088199032,3.93451280799522,
-27.9812594503621));
#305602=CARTESIAN_POINT('Ctrl Pts',(-4.1369915883886,3.00570032696477,-27.8937594503621));
#305603=CARTESIAN_POINT('Ctrl Pts',(-4.62529720699086,1.50285016348238,
-27.8062594503621));
#305604=CARTESIAN_POINT('Ctrl Pts',(-5.11360282559314,2.70014754128264E-15,
-27.7187594503621));
#305605=CARTESIAN_POINT('Ctrl Pts',(-4.62529720699087,-1.50285016348238,
-27.6312594503621));
#305606=CARTESIAN_POINT('Ctrl Pts',(-4.1369915883886,-3.00570032696476,
-27.5437594503621));
#305607=CARTESIAN_POINT('Ctrl Pts',(-2.85859088199032,-3.93451280799521,
-27.4562594503621));
#305608=CARTESIAN_POINT('Ctrl Pts',(-1.58019017559203,-4.86332528902566,
-27.3687594503621));
#305609=CARTESIAN_POINT('Ctrl Pts',(-5.95585574841766E-16,-4.86332528902566,
-27.2812594503621));
#305610=CARTESIAN_POINT('Ctrl Pts',(1.58019017559203,-4.86332528902566,
-27.1937594503621));
#305611=CARTESIAN_POINT('Ctrl Pts',(2.85859088199031,-3.93451280799521,
-27.1062594503621));
#305612=CARTESIAN_POINT('Ctrl Pts',(4.13699158838859,-3.00570032696476,
-27.0187594503621));
#305613=CARTESIAN_POINT('Ctrl Pts',(4.62529720699086,-1.50285016348238,
-26.9312594503621));
#305614=CARTESIAN_POINT('Ctrl Pts',(5.11360282559314,1.47500100649391E-15,
-26.8437594503621));
#305615=CARTESIAN_POINT('Ctrl Pts',(4.62529720699087,1.50285016348238,-26.7562594503621));
#305616=CARTESIAN_POINT('Ctrl Pts',(4.1369915883886,3.00570032696477,-26.6687594503621));
#305617=CARTESIAN_POINT('Ctrl Pts',(2.85859088199032,3.93451280799522,-26.5812594503621));
#305618=CARTESIAN_POINT('Ctrl Pts',(1.58019017559203,4.86332528902566,-26.4937594503621));
#305619=CARTESIAN_POINT('Ctrl Pts',(0.,4.86332528902566,-26.4062594503621));
#305620=CARTESIAN_POINT('Ctrl Pts',(-1.58019017559203,4.86332528902566,
-26.3187594503621));
#305621=CARTESIAN_POINT('Ctrl Pts',(-2.85859088199032,3.93451280799522,
-26.2312594503621));
#305622=CARTESIAN_POINT('Ctrl Pts',(-4.1369915883886,3.00570032696477,-26.1437594503621));
#305623=CARTESIAN_POINT('Ctrl Pts',(-4.62529720699086,1.50285016348238,
-26.0562594503621));
#305624=CARTESIAN_POINT('Ctrl Pts',(-5.11360282559314,2.75479740469459E-15,
-25.9687594503621));
#305625=CARTESIAN_POINT('Ctrl Pts',(-4.62529720699087,-1.50285016348238,
-25.8812594503621));
#305626=CARTESIAN_POINT('Ctrl Pts',(-4.1369915883886,-3.00570032696476,
-25.7937594503621));
#305627=CARTESIAN_POINT('Ctrl Pts',(-2.85859088199032,-3.93451280799521,
-25.7062594503621));
#305628=CARTESIAN_POINT('Ctrl Pts',(-1.58019017559203,-4.86332528902566,
-25.6187594503621));
#305629=CARTESIAN_POINT('Ctrl Pts',(-5.95585574841766E-16,-4.86332528902566,
-25.5312594503621));
#305630=CARTESIAN_POINT('Ctrl Pts',(1.58019017559203,-4.86332528902566,
-25.4437594503621));
#305631=CARTESIAN_POINT('Ctrl Pts',(2.85859088199031,-3.93451280799521,
-25.3562594503621));
#305632=CARTESIAN_POINT('Ctrl Pts',(4.13699158838859,-3.00570032696476,
-25.2687594503621));
#305633=CARTESIAN_POINT('Ctrl Pts',(4.62529720699086,-1.50285016348238,
-25.1812594503621));
#305634=CARTESIAN_POINT('Ctrl Pts',(5.11360282559314,1.52965086990587E-15,
-25.0937594503621));
#305635=CARTESIAN_POINT('Ctrl Pts',(4.62529720699087,1.50285016348238,-25.0062594503621));
#305636=CARTESIAN_POINT('Ctrl Pts',(4.1369915883886,3.00570032696477,-24.9187594503621));
#305637=CARTESIAN_POINT('Ctrl Pts',(2.85859088199032,3.93451280799522,-24.8312594503621));
#305638=CARTESIAN_POINT('Ctrl Pts',(1.58019017559203,4.86332528902566,-24.7437594503621));
#305639=CARTESIAN_POINT('Ctrl Pts',(0.,4.86332528902566,-24.6562594503621));
#305640=CARTESIAN_POINT('Ctrl Pts',(-1.58019017559203,4.86332528902566,
-24.5687594503621));
#305641=CARTESIAN_POINT('Ctrl Pts',(-2.85859088199032,3.93451280799522,
-24.4812594503621));
#305642=CARTESIAN_POINT('Ctrl Pts',(-4.1369915883886,3.00570032696477,-24.3937594503621));
#305643=CARTESIAN_POINT('Ctrl Pts',(-4.62529720699086,1.50285016348238,
-24.3062594503621));
#305644=CARTESIAN_POINT('Ctrl Pts',(-5.11360282559314,2.80944726810654E-15,
-24.2187594503621));
#305645=CARTESIAN_POINT('Ctrl Pts',(-4.62529720699087,-1.50285016348238,
-24.1312594503621));
#305646=CARTESIAN_POINT('Ctrl Pts',(-4.1369915883886,-3.00570032696476,
-24.0437594503621));
#305647=CARTESIAN_POINT('Ctrl Pts',(-2.85859088199032,-3.93451280799521,
-23.9562594503621));
#305648=CARTESIAN_POINT('Ctrl Pts',(-1.58019017559203,-4.86332528902566,
-23.8687594503621));
#305649=CARTESIAN_POINT('Ctrl Pts',(-5.95585574841766E-16,-4.86332528902566,
-23.7812594503621));
#305650=CARTESIAN_POINT('Ctrl Pts',(1.58019017559203,-4.86332528902566,
-23.6937594503621));
#305651=CARTESIAN_POINT('Ctrl Pts',(2.85859088199031,-3.93451280799521,
-23.6062594503621));
#305652=CARTESIAN_POINT('Ctrl Pts',(4.13699158838859,-3.00570032696476,
-23.5187594503621));
#305653=CARTESIAN_POINT('Ctrl Pts',(4.62529720699086,-1.50285016348238,
-23.4312594503621));
#305654=CARTESIAN_POINT('Ctrl Pts',(5.11360282559314,1.58430073331782E-15,
-23.3437594503621));
#305655=CARTESIAN_POINT('Ctrl Pts',(4.62529720699087,1.50285016348238,-23.2562594503621));
#305656=CARTESIAN_POINT('Ctrl Pts',(4.1369915883886,3.00570032696477,-23.1687594503621));
#305657=CARTESIAN_POINT('Ctrl Pts',(2.85859088199032,3.93451280799522,-23.0812594503621));
#305658=CARTESIAN_POINT('Ctrl Pts',(1.58019017559203,4.86332528902566,-22.9937594503621));
#305659=CARTESIAN_POINT('Ctrl Pts',(0.,4.86332528902566,-22.9062594503621));
#305660=CARTESIAN_POINT('Ctrl Pts',(-1.58019017559203,4.86332528902566,
-22.8187594503621));
#305661=CARTESIAN_POINT('Ctrl Pts',(-2.85859088199032,3.93451280799522,
-22.7312594503621));
#305662=CARTESIAN_POINT('Ctrl Pts',(-4.1369915883886,3.00570032696477,-22.6437594503621));
#305663=CARTESIAN_POINT('Ctrl Pts',(-4.62529720699086,1.50285016348238,
-22.5562594503621));
#305664=CARTESIAN_POINT('Ctrl Pts',(-5.11360282559314,2.86409713151849E-15,
-22.4687594503621));
#305665=CARTESIAN_POINT('Ctrl Pts',(-4.62529720699087,-1.50285016348238,
-22.3812594503621));
#305666=CARTESIAN_POINT('Ctrl Pts',(-4.1369915883886,-3.00570032696476,
-22.2937594503621));
#305667=CARTESIAN_POINT('Ctrl Pts',(-2.85859088199032,-3.93451280799521,
-22.2062594503621));
#305668=CARTESIAN_POINT('Ctrl Pts',(-1.58019017559203,-4.86332528902566,
-22.1187594503621));
#305669=CARTESIAN_POINT('Ctrl Pts',(-5.95585574841766E-16,-4.86332528902566,
-22.0312594503621));
#305670=CARTESIAN_POINT('Ctrl Pts',(1.58019017559203,-4.86332528902566,
-21.9437594503621));
#305671=CARTESIAN_POINT('Ctrl Pts',(2.85859088199031,-3.93451280799521,
-21.8562594503621));
#305672=CARTESIAN_POINT('Ctrl Pts',(4.13699158838859,-3.00570032696476,
-21.7687594503621));
#305673=CARTESIAN_POINT('Ctrl Pts',(4.62529720699086,-1.50285016348238,
-21.6812594503621));
#305674=CARTESIAN_POINT('Ctrl Pts',(5.11360282559314,1.63895059672977E-15,
-21.5937594503621));
#305675=CARTESIAN_POINT('Ctrl Pts',(4.62529720699087,1.50285016348238,-21.5062594503621));
#305676=CARTESIAN_POINT('Ctrl Pts',(4.1369915883886,3.00570032696477,-21.4187594503621));
#305677=CARTESIAN_POINT('Ctrl Pts',(2.85859088199032,3.93451280799522,-21.3312594503621));
#305678=CARTESIAN_POINT('Ctrl Pts',(1.58019017559203,4.86332528902566,-21.2437594503621));
#305679=CARTESIAN_POINT('Ctrl Pts',(0.,4.86332528902566,-21.1562594503621));
#305680=CARTESIAN_POINT('Ctrl Pts',(-1.58019017559203,4.86332528902566,
-21.0687594503621));
#305681=CARTESIAN_POINT('Ctrl Pts',(-2.85859088199032,3.93451280799522,
-20.9812594503621));
#305682=CARTESIAN_POINT('Ctrl Pts',(-4.1369915883886,3.00570032696477,-20.8937594503621));
#305683=CARTESIAN_POINT('Ctrl Pts',(-4.62529720699086,1.50285016348238,
-20.8062594503621));
#305684=CARTESIAN_POINT('Ctrl Pts',(-5.11360282559314,2.91874699493044E-15,
-20.7187594503621));
#305685=CARTESIAN_POINT('Ctrl Pts',(-4.62529720699087,-1.50285016348238,
-20.6312594503621));
#305686=CARTESIAN_POINT('Ctrl Pts',(-4.1369915883886,-3.00570032696476,
-20.5437594503621));
#305687=CARTESIAN_POINT('Ctrl Pts',(-2.85859088199032,-3.93451280799521,
-20.4562594503621));
#305688=CARTESIAN_POINT('Ctrl Pts',(-1.58019017559203,-4.86332528902566,
-20.3687594503621));
#305689=CARTESIAN_POINT('Ctrl Pts',(-5.95585574841766E-16,-4.86332528902566,
-20.2812594503621));
#305690=CARTESIAN_POINT('Ctrl Pts',(1.58019017559203,-4.86332528902566,
-20.1937594503621));
#305691=CARTESIAN_POINT('Ctrl Pts',(2.85859088199031,-3.93451280799521,
-20.1062594503621));
#305692=CARTESIAN_POINT('Ctrl Pts',(4.13699158838859,-3.00570032696476,
-20.0187594503621));
#305693=CARTESIAN_POINT('Ctrl Pts',(4.62529720699086,-1.50285016348238,
-19.9312594503621));
#305694=CARTESIAN_POINT('Ctrl Pts',(5.11360282559314,1.69360046014172E-15,
-19.8437594503621));
#305695=CARTESIAN_POINT('Ctrl Pts',(4.62529720699087,1.50285016348238,-19.7562594503621));
#305696=CARTESIAN_POINT('Ctrl Pts',(4.1369915883886,3.00570032696477,-19.6687594503621));
#305697=CARTESIAN_POINT('Ctrl Pts',(2.85859088199032,3.93451280799522,-19.5812594503621));
#305698=CARTESIAN_POINT('Ctrl Pts',(1.58019017559203,4.86332528902566,-19.4937594503621));
#305699=CARTESIAN_POINT('Ctrl Pts',(0.,4.86332528902566,-19.4062594503621));
#305700=CARTESIAN_POINT('Ctrl Pts',(-1.58019017559203,4.86332528902566,
-19.3187594503621));
#305701=CARTESIAN_POINT('Ctrl Pts',(-2.85859088199032,3.93451280799522,
-19.2312594503621));
#305702=CARTESIAN_POINT('Ctrl Pts',(-4.1369915883886,3.00570032696477,-19.1437594503621));
#305703=CARTESIAN_POINT('Ctrl Pts',(-4.62529720699086,1.50285016348238,
-19.0562594503621));
#305704=CARTESIAN_POINT('Ctrl Pts',(-5.11360282559314,2.97339685834239E-15,
-18.9687594503621));
#305705=CARTESIAN_POINT('Ctrl Pts',(-4.62529720699087,-1.50285016348238,
-18.8812594503621));
#305706=CARTESIAN_POINT('Ctrl Pts',(-4.1369915883886,-3.00570032696476,
-18.7937594503621));
#305707=CARTESIAN_POINT('Ctrl Pts',(-2.85859088199032,-3.93451280799521,
-18.7062594503621));
#305708=CARTESIAN_POINT('Ctrl Pts',(-1.58019017559203,-4.86332528902566,
-18.6187594503621));
#305709=CARTESIAN_POINT('Ctrl Pts',(-5.95585574841766E-16,-4.86332528902566,
-18.5312594503621));
#305710=CARTESIAN_POINT('Ctrl Pts',(1.58019017559203,-4.86332528902566,
-18.4437594503621));
#305711=CARTESIAN_POINT('Ctrl Pts',(2.85859088199031,-3.93451280799521,
-18.3562594503621));
#305712=CARTESIAN_POINT('Ctrl Pts',(4.13699158838859,-3.00570032696476,
-18.2687594503621));
#305713=CARTESIAN_POINT('Ctrl Pts',(4.62529720699086,-1.50285016348238,
-18.1812594503621));
#305714=CARTESIAN_POINT('Ctrl Pts',(5.11360282559314,1.74825032355367E-15,
-18.0937594503621));
#305715=CARTESIAN_POINT('Ctrl Pts',(4.62529720699087,1.50285016348238,-18.0062594503621));
#305716=CARTESIAN_POINT('Ctrl Pts',(4.1369915883886,3.00570032696477,-17.9187594503621));
#305717=CARTESIAN_POINT('Ctrl Pts',(2.85859088199032,3.93451280799522,-17.8312594503621));
#305718=CARTESIAN_POINT('Ctrl Pts',(1.58019017559203,4.86332528902566,-17.7437594503621));
#305719=CARTESIAN_POINT('Ctrl Pts',(0.,4.86332528902566,-17.6562594503621));
#305720=CARTESIAN_POINT('Ctrl Pts',(-1.58019017559203,4.86332528902566,
-17.5687594503621));
#305721=CARTESIAN_POINT('Ctrl Pts',(-2.85859088199032,3.93451280799522,
-17.4812594503621));
#305722=CARTESIAN_POINT('Ctrl Pts',(-4.1369915883886,3.00570032696477,-17.3937594503621));
#305723=CARTESIAN_POINT('Ctrl Pts',(-4.62529720699086,1.50285016348238,
-17.3062594503621));
#305724=CARTESIAN_POINT('Ctrl Pts',(-5.11360282559314,3.02804672175434E-15,
-17.2187594503621));
#305725=CARTESIAN_POINT('Ctrl Pts',(-4.62529720699087,-1.50285016348238,
-17.1312594503621));
#305726=CARTESIAN_POINT('Ctrl Pts',(-4.1369915883886,-3.00570032696476,
-17.0437594503621));
#305727=CARTESIAN_POINT('Ctrl Pts',(-2.85859088199032,-3.93451280799521,
-16.9562594503621));
#305728=CARTESIAN_POINT('Ctrl Pts',(-1.58019017559203,-4.86332528902566,
-16.8687594503621));
#305729=CARTESIAN_POINT('Ctrl Pts',(-5.95585574841766E-16,-4.86332528902566,
-16.7812594503621));
#305730=CARTESIAN_POINT('Ctrl Pts',(1.58019017559203,-4.86332528902566,
-16.6937594503621));
#305731=CARTESIAN_POINT('Ctrl Pts',(2.85859088199031,-3.93451280799521,
-16.6062594503621));
#305732=CARTESIAN_POINT('Ctrl Pts',(4.13699158838859,-3.00570032696476,
-16.5187594503621));
#305733=CARTESIAN_POINT('Ctrl Pts',(4.62529720699086,-1.50285016348238,
-16.4312594503621));
#305734=CARTESIAN_POINT('Ctrl Pts',(5.11360282559314,1.80290018696562E-15,
-16.3437594503621));
#305735=CARTESIAN_POINT('Ctrl Pts',(4.62529720699087,1.50285016348238,-16.2562594503621));
#305736=CARTESIAN_POINT('Ctrl Pts',(4.1369915883886,3.00570032696477,-16.1687594503621));
#305737=CARTESIAN_POINT('Ctrl Pts',(2.85859088199032,3.93451280799522,-16.0812594503621));
#305738=CARTESIAN_POINT('Ctrl Pts',(1.58019017559203,4.86332528902566,-15.9937594503621));
#305739=CARTESIAN_POINT('Ctrl Pts',(0.,4.86332528902566,-15.9062594503621));
#305740=CARTESIAN_POINT('Ctrl Pts',(-1.58019017559203,4.86332528902566,
-15.8187594503621));
#305741=CARTESIAN_POINT('Ctrl Pts',(-2.85859088199032,3.93451280799522,
-15.7312594503621));
#305742=CARTESIAN_POINT('Ctrl Pts',(-4.1369915883886,3.00570032696477,-15.6437594503621));
#305743=CARTESIAN_POINT('Ctrl Pts',(-4.62529720699086,1.50285016348238,
-15.5562594503621));
#305744=CARTESIAN_POINT('Ctrl Pts',(-5.11360282559314,3.08269658516629E-15,
-15.4687594503621));
#305745=CARTESIAN_POINT('Ctrl Pts',(-4.62529720699087,-1.50285016348238,
-15.3812594503621));
#305746=CARTESIAN_POINT('Ctrl Pts',(-4.1369915883886,-3.00570032696476,
-15.2937594503621));
#305747=CARTESIAN_POINT('Ctrl Pts',(-2.85859088199032,-3.93451280799521,
-15.2062594503621));
#305748=CARTESIAN_POINT('Ctrl Pts',(-1.58019017559203,-4.86332528902566,
-15.1187594503621));
#305749=CARTESIAN_POINT('Ctrl Pts',(-5.95585574841766E-16,-4.86332528902566,
-15.0312594503621));
#305750=CARTESIAN_POINT('Ctrl Pts',(1.58019017559203,-4.86332528902566,
-14.9437594503621));
#305751=CARTESIAN_POINT('Ctrl Pts',(2.85859088199031,-3.93451280799521,
-14.8562594503621));
#305752=CARTESIAN_POINT('Ctrl Pts',(4.13699158838859,-3.00570032696476,
-14.7687594503621));
#305753=CARTESIAN_POINT('Ctrl Pts',(4.62529720699086,-1.50285016348238,
-14.6812594503621));
#305754=CARTESIAN_POINT('Ctrl Pts',(5.11360282559314,1.85755005037757E-15,
-14.5937594503621));
#305755=CARTESIAN_POINT('Ctrl Pts',(4.62529720699087,1.50285016348238,-14.5062594503621));
#305756=CARTESIAN_POINT('Ctrl Pts',(4.1369915883886,3.00570032696477,-14.4187594503621));
#305757=CARTESIAN_POINT('Ctrl Pts',(2.85859088199032,3.93451280799522,-14.3312594503621));
#305758=CARTESIAN_POINT('Ctrl Pts',(1.58019017559203,4.86332528902566,-14.2437594503621));
#305759=CARTESIAN_POINT('Ctrl Pts',(0.,4.86332528902566,-14.1562594503621));
#305760=CARTESIAN_POINT('Ctrl Pts',(-1.58019017559203,4.86332528902566,
-14.0687594503621));
#305761=CARTESIAN_POINT('Ctrl Pts',(-2.85859088199032,3.93451280799522,
-13.9812594503621));
#305762=CARTESIAN_POINT('Ctrl Pts',(-4.1369915883886,3.00570032696477,-13.8937594503621));
#305763=CARTESIAN_POINT('Ctrl Pts',(-4.62529720699086,1.50285016348238,
-13.8062594503621));
#305764=CARTESIAN_POINT('Ctrl Pts',(-5.11360282559314,3.13734644857824E-15,
-13.7187594503621));
#305765=CARTESIAN_POINT('Ctrl Pts',(-4.62529720699087,-1.50285016348238,
-13.6312594503621));
#305766=CARTESIAN_POINT('Ctrl Pts',(-4.1369915883886,-3.00570032696476,
-13.5437594503621));
#305767=CARTESIAN_POINT('Ctrl Pts',(-2.85859088199032,-3.93451280799521,
-13.4562594503621));
#305768=CARTESIAN_POINT('Ctrl Pts',(-1.58019017559203,-4.86332528902566,
-13.3687594503621));
#305769=CARTESIAN_POINT('Ctrl Pts',(-5.95585574841766E-16,-4.86332528902566,
-13.2812594503621));
#305770=CARTESIAN_POINT('Ctrl Pts',(1.58019017559203,-4.86332528902566,
-13.1937594503621));
#305771=CARTESIAN_POINT('Ctrl Pts',(2.85859088199031,-3.93451280799521,
-13.1062594503621));
#305772=CARTESIAN_POINT('Ctrl Pts',(4.13699158838859,-3.00570032696476,
-13.0187594503621));
#305773=CARTESIAN_POINT('Ctrl Pts',(4.62529720699086,-1.50285016348238,
-12.9312594503621));
#305774=CARTESIAN_POINT('Ctrl Pts',(5.11360282559314,1.91219991378952E-15,
-12.8437594503621));
#305775=CARTESIAN_POINT('Ctrl Pts',(4.62529720699087,1.50285016348238,-12.7562594503621));
#305776=CARTESIAN_POINT('Ctrl Pts',(4.1369915883886,3.00570032696477,-12.6687594503621));
#305777=CARTESIAN_POINT('Ctrl Pts',(2.85859088199032,3.93451280799522,-12.5812594503621));
#305778=CARTESIAN_POINT('Ctrl Pts',(1.58019017559203,4.86332528902566,-12.4937594503621));
#305779=CARTESIAN_POINT('Ctrl Pts',(0.,4.86332528902566,-12.4062594503621));
#305780=CARTESIAN_POINT('Ctrl Pts',(-1.58019017559203,4.86332528902566,
-12.3187594503621));
#305781=CARTESIAN_POINT('Ctrl Pts',(-2.85859088199032,3.93451280799522,
-12.2312594503621));
#305782=CARTESIAN_POINT('Ctrl Pts',(-4.1369915883886,3.00570032696477,-12.1437594503621));
#305783=CARTESIAN_POINT('Ctrl Pts',(-4.62529720699086,1.50285016348238,
-12.0562594503621));
#305784=CARTESIAN_POINT('Ctrl Pts',(-5.11360282559314,3.1919963119902E-15,
-11.9687594503621));
#305785=CARTESIAN_POINT('Ctrl Pts',(-4.62529720699087,-1.50285016348238,
-11.8812594503621));
#305786=CARTESIAN_POINT('Ctrl Pts',(-4.1369915883886,-3.00570032696476,
-11.7937594503621));
#305787=CARTESIAN_POINT('Ctrl Pts',(-2.85859088199032,-3.93451280799521,
-11.7062594503621));
#305788=CARTESIAN_POINT('Ctrl Pts',(-1.58019017559203,-4.86332528902566,
-11.6187594503621));
#305789=CARTESIAN_POINT('Ctrl Pts',(-5.95585574841766E-16,-4.86332528902566,
-11.5312594503621));
#305790=CARTESIAN_POINT('Ctrl Pts',(1.58019017559203,-4.86332528902566,
-11.4437594503621));
#305791=CARTESIAN_POINT('Ctrl Pts',(2.85859088199031,-3.93451280799521,
-11.3562594503621));
#305792=CARTESIAN_POINT('Ctrl Pts',(4.13699158838859,-3.00570032696476,
-11.2687594503621));
#305793=CARTESIAN_POINT('Ctrl Pts',(4.62529720699086,-1.50285016348238,
-11.1812594503621));
#305794=CARTESIAN_POINT('Ctrl Pts',(5.11360282559314,1.96684977720147E-15,
-11.0937594503621));
#305795=CARTESIAN_POINT('Ctrl Pts',(4.62529720699087,1.50285016348238,-11.0062594503621));
#305796=CARTESIAN_POINT('Ctrl Pts',(4.1369915883886,3.00570032696477,-10.9187594503621));
#305797=CARTESIAN_POINT('Ctrl Pts',(2.85859088199032,3.93451280799522,-10.8312594503621));
#305798=CARTESIAN_POINT('Ctrl Pts',(1.58019017559203,4.86332528902566,-10.7437594503621));
#305799=CARTESIAN_POINT('Ctrl Pts',(0.,4.86332528902566,-10.6562594503621));
#305800=CARTESIAN_POINT('Ctrl Pts',(-1.58019017559203,4.86332528902566,
-10.5687594503621));
#305801=CARTESIAN_POINT('Ctrl Pts',(-2.85859088199032,3.93451280799522,
-10.4812594503621));
#305802=CARTESIAN_POINT('Ctrl Pts',(-4.1369915883886,3.00570032696477,-10.3937594503621));
#305803=CARTESIAN_POINT('Ctrl Pts',(-4.62529720699086,1.50285016348238,
-10.3062594503621));
#305804=CARTESIAN_POINT('Ctrl Pts',(-5.11360282559314,3.24664617540214E-15,
-10.2187594503621));
#305805=CARTESIAN_POINT('Ctrl Pts',(-4.62529720699087,-1.50285016348238,
-10.1312594503621));
#305806=CARTESIAN_POINT('Ctrl Pts',(-4.1369915883886,-3.00570032696476,
-10.0437594503621));
#305807=CARTESIAN_POINT('Ctrl Pts',(-2.85859088199032,-3.93451280799521,
-9.95625945036208));
#305808=CARTESIAN_POINT('Ctrl Pts',(-1.58019017559203,-4.86332528902566,
-9.86875945036208));
#305809=CARTESIAN_POINT('Ctrl Pts',(-5.95585574841766E-16,-4.86332528902566,
-9.78125945036208));
#305810=CARTESIAN_POINT('Ctrl Pts',(1.58019017559203,-4.86332528902566,
-9.69375945036209));
#305811=CARTESIAN_POINT('Ctrl Pts',(2.85859088199031,-3.93451280799521,
-9.60625945036209));
#305812=CARTESIAN_POINT('Ctrl Pts',(4.13699158838859,-3.00570032696476,
-9.51875945036208));
#305813=CARTESIAN_POINT('Ctrl Pts',(4.62529720699086,-1.50285016348238,
-9.43125945036208));
#305814=CARTESIAN_POINT('Ctrl Pts',(5.11360282559314,2.02149964061342E-15,
-9.34375945036209));
#305815=CARTESIAN_POINT('Ctrl Pts',(4.62529720699087,1.50285016348238,-9.25625945036208));
#305816=CARTESIAN_POINT('Ctrl Pts',(4.1369915883886,3.00570032696477,-9.16875945036209));
#305817=CARTESIAN_POINT('Ctrl Pts',(2.85859088199032,3.93451280799522,-9.08125945036208));
#305818=CARTESIAN_POINT('Ctrl Pts',(1.58019017559203,4.86332528902566,-8.99375945036209));
#305819=CARTESIAN_POINT('Ctrl Pts',(0.,4.86332528902566,-8.90625945036208));
#305820=CARTESIAN_POINT('Ctrl Pts',(-1.58019017559203,4.86332528902566,
-8.81875945036208));
#305821=CARTESIAN_POINT('Ctrl Pts',(-2.85859088199032,3.93451280799522,
-8.73125945036208));
#305822=CARTESIAN_POINT('Ctrl Pts',(-4.1369915883886,3.00570032696477,-8.64375945036208));
#305823=CARTESIAN_POINT('Ctrl Pts',(-4.62529720699086,1.50285016348238,
-8.55625945036208));
#305824=CARTESIAN_POINT('Ctrl Pts',(-5.11360282559314,3.3012960388141E-15,
-8.46875945036209));
#305825=CARTESIAN_POINT('Ctrl Pts',(-4.62529720699087,-1.50285016348238,
-8.38125945036208));
#305826=CARTESIAN_POINT('Ctrl Pts',(-4.1369915883886,-3.00570032696476,
-8.29375945036209));
#305827=CARTESIAN_POINT('Ctrl Pts',(-2.85859088199032,-3.93451280799521,
-8.20625945036208));
#305828=CARTESIAN_POINT('Ctrl Pts',(-1.58019017559203,-4.86332528902566,
-8.11875945036208));
#305829=CARTESIAN_POINT('Ctrl Pts',(-5.95585574841766E-16,-4.86332528902566,
-8.03125945036208));
#305830=CARTESIAN_POINT('Ctrl Pts',(1.58019017559203,-4.86332528902566,
-7.94375945036208));
#305831=CARTESIAN_POINT('Ctrl Pts',(2.85859088199031,-3.93451280799521,
-7.85625945036208));
#305832=CARTESIAN_POINT('Ctrl Pts',(4.13699158838859,-3.00570032696476,
-7.76875945036209));
#305833=CARTESIAN_POINT('Ctrl Pts',(4.62529720699086,-1.50285016348238,
-7.68125945036208));
#305834=CARTESIAN_POINT('Ctrl Pts',(5.11360282559314,2.07614950402537E-15,
-7.59375945036209));
#305835=CARTESIAN_POINT('Ctrl Pts',(4.62529720699087,1.50285016348238,-7.50625945036208));
#305836=CARTESIAN_POINT('Ctrl Pts',(4.1369915883886,3.00570032696477,-7.41875945036209));
#305837=CARTESIAN_POINT('Ctrl Pts',(2.85859088199032,3.93451280799522,-7.33125945036208));
#305838=CARTESIAN_POINT('Ctrl Pts',(1.58019017559203,4.86332528902566,-7.24375945036208));
#305839=CARTESIAN_POINT('Ctrl Pts',(0.,4.86332528902566,-7.15625945036208));
#305840=CARTESIAN_POINT('Ctrl Pts',(-1.58019017559203,4.86332528902566,
-7.06875945036209));
#305841=CARTESIAN_POINT('Ctrl Pts',(-2.85859088199032,3.93451280799522,
-6.98125945036208));
#305842=CARTESIAN_POINT('Ctrl Pts',(-4.1369915883886,3.00570032696477,-6.89375945036209));
#305843=CARTESIAN_POINT('Ctrl Pts',(-4.62529720699086,1.50285016348238,
-6.80625945036208));
#305844=CARTESIAN_POINT('Ctrl Pts',(-5.11360282559314,3.35594590222605E-15,
-6.71875945036209));
#305845=CARTESIAN_POINT('Ctrl Pts',(-4.62529720699087,-1.50285016348238,
-6.63125945036208));
#305846=CARTESIAN_POINT('Ctrl Pts',(-4.1369915883886,-3.00570032696476,
-6.54375945036209));
#305847=CARTESIAN_POINT('Ctrl Pts',(-2.85859088199032,-3.93451280799521,
-6.45625945036208));
#305848=CARTESIAN_POINT('Ctrl Pts',(-1.58019017559203,-4.86332528902566,
-6.36875945036209));
#305849=CARTESIAN_POINT('Ctrl Pts',(-5.95585574841766E-16,-4.86332528902566,
-6.28125945036208));
#305850=CARTESIAN_POINT('Ctrl Pts',(1.58019017559203,-4.86332528902566,
-6.19375945036209));
#305851=CARTESIAN_POINT('Ctrl Pts',(2.85859088199031,-3.93451280799521,
-6.10625945036208));
#305852=CARTESIAN_POINT('Ctrl Pts',(4.13699158838859,-3.00570032696476,
-6.0187594503621));
#305853=CARTESIAN_POINT('Ctrl Pts',(4.62529720699086,-1.50285016348238,
-5.93125945036208));
#305854=CARTESIAN_POINT('Ctrl Pts',(5.11360282559314,2.13079936743733E-15,
-5.84375945036209));
#305855=CARTESIAN_POINT('Ctrl Pts',(4.62529720699087,1.50285016348238,-5.75625945036208));
#305856=CARTESIAN_POINT('Ctrl Pts',(4.1369915883886,3.00570032696477,-5.66875945036209));
#305857=CARTESIAN_POINT('Ctrl Pts',(2.85859088199032,3.93451280799522,-5.58125945036208));
#305858=CARTESIAN_POINT('Ctrl Pts',(1.58019017559203,4.86332528902566,-5.49375945036209));
#305859=CARTESIAN_POINT('Ctrl Pts',(0.,4.86332528902566,-5.40625945036208));
#305860=CARTESIAN_POINT('Ctrl Pts',(-1.58019017559203,4.86332528902566,
-5.31875945036209));
#305861=CARTESIAN_POINT('Ctrl Pts',(-2.85859088199032,3.93451280799522,
-5.23125945036208));
#305862=CARTESIAN_POINT('Ctrl Pts',(-3.3915599562443,3.54728810943805,-5.19478043891927));
#305863=CARTESIAN_POINT('Ctrl Pts',(-3.80230551497385,3.03222783406459,
-5.15646275598973));
#305864=CARTESIAN_POINT('Ctrl Pts',(-7.36910532594948E-14,6.00000000000001,
-6.50000000000001));
#305865=CARTESIAN_POINT('Ctrl Pts',(0.695536090209394,6.00000000000002,
-6.53121766629259));
#305866=CARTESIAN_POINT('Ctrl Pts',(1.38641832502867,5.87905710063626,-6.563990204745));
#305867=CARTESIAN_POINT('Ctrl Pts',(2.77639380398129,5.37608234738622,-6.63371136268937));
#305868=CARTESIAN_POINT('Ctrl Pts',(3.45221402618498,4.96919013454356,-6.66853947573316));
#305869=CARTESIAN_POINT('Ctrl Pts',(4.61350745859033,3.91586257612663,-6.74096845709073));
#305870=CARTESIAN_POINT('Ctrl Pts',(5.08648051138953,3.27813009530638,-6.77843673756609));
#305871=CARTESIAN_POINT('Ctrl Pts',(5.75390094257317,1.86835407146478,-6.85077518450608));
#305872=CARTESIAN_POINT('Ctrl Pts',(5.94657177527691,1.11193156507019,-6.88502499392445));
#305873=CARTESIAN_POINT('Ctrl Pts',(6.03524834172125,-0.45136365758525,
-6.95880105072841));
#305874=CARTESIAN_POINT('Ctrl Pts',(5.9229448545129,-1.24358642710857,-6.99568226363595));
#305875=CARTESIAN_POINT('Ctrl Pts',(5.40125880336164,-2.72662372932836,
-7.06677525385319));
#305876=CARTESIAN_POINT('Ctrl Pts',(5.00156711282546,-3.40474766259226,
-7.10375290376194));
#305877=CARTESIAN_POINT('Ctrl Pts',(3.96750118999664,-4.56744311065716,
-7.17682833144899));
#305878=CARTESIAN_POINT('Ctrl Pts',(3.34393241019509,-5.04189722999588,
-7.21094233439999));
#305879=CARTESIAN_POINT('Ctrl Pts',(1.93705624242696,-5.73360223580846,
-7.28417436019869));
#305880=CARTESIAN_POINT('Ctrl Pts',(1.16467505775192,-5.93885250963874,
-7.32183428918265));
#305881=CARTESIAN_POINT('Ctrl Pts',(-0.398071677820406,-6.03664804127998,
-7.39340105590642));
#305882=CARTESIAN_POINT('Ctrl Pts',(-1.17301020650276,-5.93495392183099,
-7.42859667074508));
#305883=CARTESIAN_POINT('Ctrl Pts',(-2.65044753997004,-5.43963450410889,
-7.50213172873049));
#305884=CARTESIAN_POINT('Ctrl Pts',(-3.33769715417903,-5.04720323133648,
-7.53738436153389));
#305885=CARTESIAN_POINT('Ctrl Pts',(-4.5229067872758,-4.01981977607675,
-7.60948622083326));
#305886=CARTESIAN_POINT('Ctrl Pts',(-5.00925311469169,-3.39455260229493,
-7.64684954334406));
#305887=CARTESIAN_POINT('Ctrl Pts',(-5.708787772007,-2.00208695227552,-7.71941790734077));
#305888=CARTESIAN_POINT('Ctrl Pts',(-5.91911839235579,-1.25005304156578,
-7.75350667432105));
#305889=CARTESIAN_POINT('Ctrl Pts',(-6.0443882583849,0.31463515188788,-7.82734846911949));
#305890=CARTESIAN_POINT('Ctrl Pts',(-5.94937536630207,1.11278518743067,
-7.86495515658336));
#305891=CARTESIAN_POINT('Ctrl Pts',(-5.45907891653994,2.6084356620542,-7.93565899265305));
#305892=CARTESIAN_POINT('Ctrl Pts',(-5.07516282202342,3.29364355428696,
-7.97246950412426));
#305893=CARTESIAN_POINT('Ctrl Pts',(-4.06741694281494,4.47895159391096,
-8.04567817732591));
#305894=CARTESIAN_POINT('Ctrl Pts',(-3.45321844823359,4.96791566333691,
-8.07995836388455));
#305895=CARTESIAN_POINT('Ctrl Pts',(-2.06182138758084,5.68968624537131,
-8.15293409901987));
#305896=CARTESIAN_POINT('Ctrl Pts',(-1.29586495890513,5.91137919559933,
-8.19054545545049));
#305897=CARTESIAN_POINT('Ctrl Pts',(-0.339438395925482,5.99280698755147,
-8.23466012744105));
#305898=CARTESIAN_POINT('Ctrl Pts',(-0.169625758311113,6.,-8.24238670661075));
#305899=CARTESIAN_POINT('Ctrl Pts',(-2.33459085396959E-13,6.00000000000001,
-8.25));
#305900=CARTESIAN_POINT('Ctrl Pts',(-0.75570415697393,-4.80426927898796,
-36.0741583424671));
#305901=CARTESIAN_POINT('Ctrl Pts',(-0.380160882715947,-4.86334165753294,
-36.0523006088412));
#305902=CARTESIAN_POINT('Ctrl Pts',(-5.9558757940577E-16,-4.86334165753294,
-36.03125));
#305903=CARTESIAN_POINT('Ctrl Pts',(0.,4.86333050978515,-37.1249935638448));
#305904=CARTESIAN_POINT('Ctrl Pts',(-1.58019187191962,4.86333050978515,
-37.0374935638448));
#305905=CARTESIAN_POINT('Ctrl Pts',(-2.85859395067575,3.93451703167837,
-36.9499935638448));
#305906=CARTESIAN_POINT('Ctrl Pts',(-4.13699602943188,3.00570355357158,
-36.8624935638448));
#305907=CARTESIAN_POINT('Ctrl Pts',(-4.6253021722282,1.50285177678579,-36.7749935638448));
#305908=CARTESIAN_POINT('Ctrl Pts',(-5.11360831502452,2.42006782353912E-15,
-36.6874935638448));
#305909=CARTESIAN_POINT('Ctrl Pts',(-4.6253021722282,-1.50285177678579,
-36.5999935638448));
#305910=CARTESIAN_POINT('Ctrl Pts',(-4.13699602943188,-3.00570355357157,
-36.5124935638448));
#305911=CARTESIAN_POINT('Ctrl Pts',(-2.85859395067575,-3.93451703167836,
-36.4249935638448));
#305912=CARTESIAN_POINT('Ctrl Pts',(-1.58019187191962,-4.86333050978515,
-36.3374935638448));
#305913=CARTESIAN_POINT('Ctrl Pts',(-5.95586214200406E-16,-4.86333050978515,
-36.2499935638448));
#305914=CARTESIAN_POINT('Ctrl Pts',(1.58019187191962,-4.86333050978515,
-36.1624935638448));
#305915=CARTESIAN_POINT('Ctrl Pts',(2.85859395067575,-3.93451703167836,
-36.0749935638448));
#305916=CARTESIAN_POINT('Ctrl Pts',(4.13699602943187,-3.00570355357157,
-35.9874935638448));
#305917=CARTESIAN_POINT('Ctrl Pts',(4.6253021722282,-1.50285177678579,-35.8999935638448));
#305918=CARTESIAN_POINT('Ctrl Pts',(5.11360831502452,1.19491994422748E-15,
-35.8124935638448));
#305919=CARTESIAN_POINT('Ctrl Pts',(4.6253021722282,1.50285177678579,-35.7249935638448));
#305920=CARTESIAN_POINT('Ctrl Pts',(4.13699602943188,3.00570355357158,-35.6374935638448));
#305921=CARTESIAN_POINT('Ctrl Pts',(2.85859395067575,3.93451703167837,-35.5499935638448));
#305922=CARTESIAN_POINT('Ctrl Pts',(1.58019187191962,4.86333050978515,-35.4624935638448));
#305923=CARTESIAN_POINT('Ctrl Pts',(0.,4.86333050978515,-35.3749935638448));
#305924=CARTESIAN_POINT('Ctrl Pts',(-1.58019187191962,4.86333050978515,
-35.2874935638448));
#305925=CARTESIAN_POINT('Ctrl Pts',(-2.85859395067575,3.93451703167837,
-35.1999935638448));
#305926=CARTESIAN_POINT('Ctrl Pts',(-4.13699602943188,3.00570355357158,
-35.1124935638448));
#305927=CARTESIAN_POINT('Ctrl Pts',(-4.6253021722282,1.50285177678579,-35.0249935638448));
#305928=CARTESIAN_POINT('Ctrl Pts',(-5.11360831502452,2.47471768695107E-15,
-34.9374935638448));
#305929=CARTESIAN_POINT('Ctrl Pts',(-4.6253021722282,-1.50285177678579,
-34.8499935638448));
#305930=CARTESIAN_POINT('Ctrl Pts',(-4.13699602943188,-3.00570355357157,
-34.7624935638448));
#305931=CARTESIAN_POINT('Ctrl Pts',(-2.85859395067575,-3.93451703167836,
-34.6749935638448));
#305932=CARTESIAN_POINT('Ctrl Pts',(-1.58019187191962,-4.86333050978515,
-34.5874935638448));
#305933=CARTESIAN_POINT('Ctrl Pts',(-5.95586214200406E-16,-4.86333050978515,
-34.4999935638448));
#305934=CARTESIAN_POINT('Ctrl Pts',(1.58019187191962,-4.86333050978515,
-34.4124935638448));
#305935=CARTESIAN_POINT('Ctrl Pts',(2.85859395067575,-3.93451703167836,
-34.3249935638448));
#305936=CARTESIAN_POINT('Ctrl Pts',(4.13699602943187,-3.00570355357157,
-34.2374935638448));
#305937=CARTESIAN_POINT('Ctrl Pts',(4.6253021722282,-1.50285177678579,-34.1499935638448));
#305938=CARTESIAN_POINT('Ctrl Pts',(5.11360831502452,1.24956980763943E-15,
-34.0624935638448));
#305939=CARTESIAN_POINT('Ctrl Pts',(4.6253021722282,1.50285177678579,-33.9749935638448));
#305940=CARTESIAN_POINT('Ctrl Pts',(4.13699602943188,3.00570355357158,-33.8874935638448));
#305941=CARTESIAN_POINT('Ctrl Pts',(2.85859395067575,3.93451703167837,-33.7999935638448));
#305942=CARTESIAN_POINT('Ctrl Pts',(1.58019187191962,4.86333050978515,-33.7124935638448));
#305943=CARTESIAN_POINT('Ctrl Pts',(0.,4.86333050978515,-33.6249935638448));
#305944=CARTESIAN_POINT('Ctrl Pts',(-1.58019187191962,4.86333050978515,
-33.5374935638448));
#305945=CARTESIAN_POINT('Ctrl Pts',(-2.85859395067575,3.93451703167837,
-33.4499935638448));
#305946=CARTESIAN_POINT('Ctrl Pts',(-4.13699602943188,3.00570355357158,
-33.3624935638448));
#305947=CARTESIAN_POINT('Ctrl Pts',(-4.6253021722282,1.50285177678579,-33.2749935638448));
#305948=CARTESIAN_POINT('Ctrl Pts',(-5.11360831502452,2.52936755036302E-15,
-33.1874935638448));
#305949=CARTESIAN_POINT('Ctrl Pts',(-4.6253021722282,-1.50285177678579,
-33.0999935638448));
#305950=CARTESIAN_POINT('Ctrl Pts',(-4.13699602943188,-3.00570355357157,
-33.0124935638448));
#305951=CARTESIAN_POINT('Ctrl Pts',(-2.85859395067575,-3.93451703167836,
-32.9249935638448));
#305952=CARTESIAN_POINT('Ctrl Pts',(-1.58019187191962,-4.86333050978515,
-32.8374935638448));
#305953=CARTESIAN_POINT('Ctrl Pts',(-5.95586214200406E-16,-4.86333050978515,
-32.7499935638448));
#305954=CARTESIAN_POINT('Ctrl Pts',(1.58019187191962,-4.86333050978515,
-32.6624935638448));
#305955=CARTESIAN_POINT('Ctrl Pts',(2.85859395067575,-3.93451703167836,
-32.5749935638448));
#305956=CARTESIAN_POINT('Ctrl Pts',(4.13699602943187,-3.00570355357157,
-32.4874935638448));
#305957=CARTESIAN_POINT('Ctrl Pts',(4.6253021722282,-1.50285177678579,-32.3999935638448));
#305958=CARTESIAN_POINT('Ctrl Pts',(5.11360831502452,1.30421967105138E-15,
-32.3124935638448));
#305959=CARTESIAN_POINT('Ctrl Pts',(4.6253021722282,1.50285177678579,-32.2249935638448));
#305960=CARTESIAN_POINT('Ctrl Pts',(4.13699602943188,3.00570355357158,-32.1374935638448));
#305961=CARTESIAN_POINT('Ctrl Pts',(2.85859395067575,3.93451703167837,-32.0499935638448));
#305962=CARTESIAN_POINT('Ctrl Pts',(1.58019187191962,4.86333050978515,-31.9624935638448));
#305963=CARTESIAN_POINT('Ctrl Pts',(0.,4.86333050978515,-31.8749935638448));
#305964=CARTESIAN_POINT('Ctrl Pts',(-1.58019187191962,4.86333050978515,
-31.7874935638448));
#305965=CARTESIAN_POINT('Ctrl Pts',(-2.85859395067575,3.93451703167837,
-31.6999935638448));
#305966=CARTESIAN_POINT('Ctrl Pts',(-4.13699602943188,3.00570355357158,
-31.6124935638448));
#305967=CARTESIAN_POINT('Ctrl Pts',(-4.6253021722282,1.50285177678579,-31.5249935638448));
#305968=CARTESIAN_POINT('Ctrl Pts',(-5.11360831502452,2.58401741377497E-15,
-31.4374935638448));
#305969=CARTESIAN_POINT('Ctrl Pts',(-4.6253021722282,-1.50285177678579,
-31.3499935638448));
#305970=CARTESIAN_POINT('Ctrl Pts',(-4.13699602943188,-3.00570355357157,
-31.2624935638448));
#305971=CARTESIAN_POINT('Ctrl Pts',(-2.85859395067575,-3.93451703167836,
-31.1749935638448));
#305972=CARTESIAN_POINT('Ctrl Pts',(-1.58019187191962,-4.86333050978515,
-31.0874935638448));
#305973=CARTESIAN_POINT('Ctrl Pts',(-5.95586214200406E-16,-4.86333050978515,
-30.9999935638448));
#305974=CARTESIAN_POINT('Ctrl Pts',(1.58019187191962,-4.86333050978515,
-30.9124935638448));
#305975=CARTESIAN_POINT('Ctrl Pts',(2.85859395067575,-3.93451703167836,
-30.8249935638448));
#305976=CARTESIAN_POINT('Ctrl Pts',(4.13699602943187,-3.00570355357157,
-30.7374935638448));
#305977=CARTESIAN_POINT('Ctrl Pts',(4.6253021722282,-1.50285177678579,-30.6499935638448));
#305978=CARTESIAN_POINT('Ctrl Pts',(5.11360831502452,1.35886953446333E-15,
-30.5624935638448));
#305979=CARTESIAN_POINT('Ctrl Pts',(4.6253021722282,1.50285177678579,-30.4749935638448));
#305980=CARTESIAN_POINT('Ctrl Pts',(4.13699602943188,3.00570355357158,-30.3874935638448));
#305981=CARTESIAN_POINT('Ctrl Pts',(2.85859395067575,3.93451703167837,-30.2999935638448));
#305982=CARTESIAN_POINT('Ctrl Pts',(1.58019187191962,4.86333050978515,-30.2124935638448));
#305983=CARTESIAN_POINT('Ctrl Pts',(0.,4.86333050978515,-30.1249935638448));
#305984=CARTESIAN_POINT('Ctrl Pts',(-1.58019187191962,4.86333050978515,
-30.0374935638448));
#305985=CARTESIAN_POINT('Ctrl Pts',(-2.85859395067575,3.93451703167837,
-29.9499935638448));
#305986=CARTESIAN_POINT('Ctrl Pts',(-4.13699602943188,3.00570355357158,
-29.8624935638448));
#305987=CARTESIAN_POINT('Ctrl Pts',(-4.6253021722282,1.50285177678579,-29.7749935638448));
#305988=CARTESIAN_POINT('Ctrl Pts',(-5.11360831502452,2.63866727718692E-15,
-29.6874935638448));
#305989=CARTESIAN_POINT('Ctrl Pts',(-4.6253021722282,-1.50285177678579,
-29.5999935638448));
#305990=CARTESIAN_POINT('Ctrl Pts',(-4.13699602943188,-3.00570355357157,
-29.5124935638448));
#305991=CARTESIAN_POINT('Ctrl Pts',(-2.85859395067575,-3.93451703167836,
-29.4249935638448));
#305992=CARTESIAN_POINT('Ctrl Pts',(-1.58019187191962,-4.86333050978515,
-29.3374935638448));
#305993=CARTESIAN_POINT('Ctrl Pts',(-5.95586214200406E-16,-4.86333050978515,
-29.2499935638448));
#305994=CARTESIAN_POINT('Ctrl Pts',(1.58019187191962,-4.86333050978515,
-29.1624935638448));
#305995=CARTESIAN_POINT('Ctrl Pts',(2.85859395067575,-3.93451703167836,
-29.0749935638448));
#305996=CARTESIAN_POINT('Ctrl Pts',(4.13699602943187,-3.00570355357157,
-28.9874935638448));
#305997=CARTESIAN_POINT('Ctrl Pts',(4.6253021722282,-1.50285177678579,-28.8999935638448));
#305998=CARTESIAN_POINT('Ctrl Pts',(5.11360831502452,1.41351939787528E-15,
-28.8124935638448));
#305999=CARTESIAN_POINT('Ctrl Pts',(4.6253021722282,1.50285177678579,-28.7249935638448));
#306000=CARTESIAN_POINT('Ctrl Pts',(4.13699602943188,3.00570355357158,-28.6374935638448));
#306001=CARTESIAN_POINT('Ctrl Pts',(2.85859395067575,3.93451703167837,-28.5499935638448));
#306002=CARTESIAN_POINT('Ctrl Pts',(1.58019187191962,4.86333050978515,-28.4624935638448));
#306003=CARTESIAN_POINT('Ctrl Pts',(0.,4.86333050978515,-28.3749935638448));
#306004=CARTESIAN_POINT('Ctrl Pts',(-1.58019187191962,4.86333050978515,
-28.2874935638448));
#306005=CARTESIAN_POINT('Ctrl Pts',(-2.85859395067575,3.93451703167837,
-28.1999935638448));
#306006=CARTESIAN_POINT('Ctrl Pts',(-4.13699602943188,3.00570355357158,
-28.1124935638448));
#306007=CARTESIAN_POINT('Ctrl Pts',(-4.6253021722282,1.50285177678579,-28.0249935638448));
#306008=CARTESIAN_POINT('Ctrl Pts',(-5.11360831502452,2.69331714059887E-15,
-27.9374935638448));
#306009=CARTESIAN_POINT('Ctrl Pts',(-4.6253021722282,-1.50285177678579,
-27.8499935638448));
#306010=CARTESIAN_POINT('Ctrl Pts',(-4.13699602943188,-3.00570355357157,
-27.7624935638448));
#306011=CARTESIAN_POINT('Ctrl Pts',(-2.85859395067575,-3.93451703167836,
-27.6749935638448));
#306012=CARTESIAN_POINT('Ctrl Pts',(-1.58019187191962,-4.86333050978515,
-27.5874935638448));
#306013=CARTESIAN_POINT('Ctrl Pts',(-5.95586214200406E-16,-4.86333050978515,
-27.4999935638448));
#306014=CARTESIAN_POINT('Ctrl Pts',(1.58019187191962,-4.86333050978515,
-27.4124935638448));
#306015=CARTESIAN_POINT('Ctrl Pts',(2.85859395067575,-3.93451703167836,
-27.3249935638448));
#306016=CARTESIAN_POINT('Ctrl Pts',(4.13699602943187,-3.00570355357157,
-27.2374935638448));
#306017=CARTESIAN_POINT('Ctrl Pts',(4.6253021722282,-1.50285177678579,-27.1499935638448));
#306018=CARTESIAN_POINT('Ctrl Pts',(5.11360831502452,1.46816926128723E-15,
-27.0624935638448));
#306019=CARTESIAN_POINT('Ctrl Pts',(4.6253021722282,1.50285177678579,-26.9749935638448));
#306020=CARTESIAN_POINT('Ctrl Pts',(4.13699602943188,3.00570355357158,-26.8874935638448));
#306021=CARTESIAN_POINT('Ctrl Pts',(2.85859395067575,3.93451703167837,-26.7999935638448));
#306022=CARTESIAN_POINT('Ctrl Pts',(1.58019187191962,4.86333050978515,-26.7124935638448));
#306023=CARTESIAN_POINT('Ctrl Pts',(0.,4.86333050978515,-26.6249935638448));
#306024=CARTESIAN_POINT('Ctrl Pts',(-1.58019187191962,4.86333050978515,
-26.5374935638448));
#306025=CARTESIAN_POINT('Ctrl Pts',(-2.85859395067575,3.93451703167837,
-26.4499935638448));
#306026=CARTESIAN_POINT('Ctrl Pts',(-4.13699602943188,3.00570355357158,
-26.3624935638448));
#306027=CARTESIAN_POINT('Ctrl Pts',(-4.6253021722282,1.50285177678579,-26.2749935638448));
#306028=CARTESIAN_POINT('Ctrl Pts',(-5.11360831502452,2.74796700401082E-15,
-26.1874935638448));
#306029=CARTESIAN_POINT('Ctrl Pts',(-4.6253021722282,-1.50285177678579,
-26.0999935638448));
#306030=CARTESIAN_POINT('Ctrl Pts',(-4.13699602943188,-3.00570355357157,
-26.0124935638448));
#306031=CARTESIAN_POINT('Ctrl Pts',(-2.85859395067575,-3.93451703167836,
-25.9249935638448));
#306032=CARTESIAN_POINT('Ctrl Pts',(-1.58019187191962,-4.86333050978515,
-25.8374935638448));
#306033=CARTESIAN_POINT('Ctrl Pts',(-5.95586214200406E-16,-4.86333050978515,
-25.7499935638448));
#306034=CARTESIAN_POINT('Ctrl Pts',(1.58019187191962,-4.86333050978515,
-25.6624935638448));
#306035=CARTESIAN_POINT('Ctrl Pts',(2.85859395067575,-3.93451703167836,
-25.5749935638448));
#306036=CARTESIAN_POINT('Ctrl Pts',(4.13699602943187,-3.00570355357157,
-25.4874935638448));
#306037=CARTESIAN_POINT('Ctrl Pts',(4.6253021722282,-1.50285177678579,-25.3999935638448));
#306038=CARTESIAN_POINT('Ctrl Pts',(5.11360831502452,1.52281912469918E-15,
-25.3124935638448));
#306039=CARTESIAN_POINT('Ctrl Pts',(4.6253021722282,1.50285177678579,-25.2249935638448));
#306040=CARTESIAN_POINT('Ctrl Pts',(4.13699602943188,3.00570355357158,-25.1374935638448));
#306041=CARTESIAN_POINT('Ctrl Pts',(2.85859395067575,3.93451703167837,-25.0499935638448));
#306042=CARTESIAN_POINT('Ctrl Pts',(1.58019187191962,4.86333050978515,-24.9624935638448));
#306043=CARTESIAN_POINT('Ctrl Pts',(0.,4.86333050978515,-24.8749935638448));
#306044=CARTESIAN_POINT('Ctrl Pts',(-1.58019187191962,4.86333050978515,
-24.7874935638448));
#306045=CARTESIAN_POINT('Ctrl Pts',(-2.85859395067575,3.93451703167837,
-24.6999935638448));
#306046=CARTESIAN_POINT('Ctrl Pts',(-4.13699602943188,3.00570355357158,
-24.6124935638448));
#306047=CARTESIAN_POINT('Ctrl Pts',(-4.6253021722282,1.50285177678579,-24.5249935638448));
#306048=CARTESIAN_POINT('Ctrl Pts',(-5.11360831502452,2.80261686742278E-15,
-24.4374935638448));
#306049=CARTESIAN_POINT('Ctrl Pts',(-4.6253021722282,-1.50285177678579,
-24.3499935638448));
#306050=CARTESIAN_POINT('Ctrl Pts',(-4.13699602943188,-3.00570355357157,
-24.2624935638448));
#306051=CARTESIAN_POINT('Ctrl Pts',(-2.85859395067575,-3.93451703167836,
-24.1749935638448));
#306052=CARTESIAN_POINT('Ctrl Pts',(-1.58019187191962,-4.86333050978515,
-24.0874935638448));
#306053=CARTESIAN_POINT('Ctrl Pts',(-5.95586214200406E-16,-4.86333050978515,
-23.9999935638448));
#306054=CARTESIAN_POINT('Ctrl Pts',(1.58019187191962,-4.86333050978515,
-23.9124935638448));
#306055=CARTESIAN_POINT('Ctrl Pts',(2.85859395067575,-3.93451703167836,
-23.8249935638448));
#306056=CARTESIAN_POINT('Ctrl Pts',(4.13699602943187,-3.00570355357157,
-23.7374935638448));
#306057=CARTESIAN_POINT('Ctrl Pts',(4.6253021722282,-1.50285177678579,-23.6499935638448));
#306058=CARTESIAN_POINT('Ctrl Pts',(5.11360831502452,1.57746898811114E-15,
-23.5624935638448));
#306059=CARTESIAN_POINT('Ctrl Pts',(4.6253021722282,1.50285177678579,-23.4749935638448));
#306060=CARTESIAN_POINT('Ctrl Pts',(4.13699602943188,3.00570355357158,-23.3874935638448));
#306061=CARTESIAN_POINT('Ctrl Pts',(2.85859395067575,3.93451703167837,-23.2999935638448));
#306062=CARTESIAN_POINT('Ctrl Pts',(1.58019187191962,4.86333050978515,-23.2124935638448));
#306063=CARTESIAN_POINT('Ctrl Pts',(0.,4.86333050978515,-23.1249935638448));
#306064=CARTESIAN_POINT('Ctrl Pts',(-1.58019187191962,4.86333050978515,
-23.0374935638448));
#306065=CARTESIAN_POINT('Ctrl Pts',(-2.85859395067575,3.93451703167837,
-22.9499935638448));
#306066=CARTESIAN_POINT('Ctrl Pts',(-4.13699602943188,3.00570355357158,
-22.8624935638448));
#306067=CARTESIAN_POINT('Ctrl Pts',(-4.6253021722282,1.50285177678579,-22.7749935638448));
#306068=CARTESIAN_POINT('Ctrl Pts',(-5.11360831502452,2.85726673083472E-15,
-22.6874935638448));
#306069=CARTESIAN_POINT('Ctrl Pts',(-4.6253021722282,-1.50285177678579,
-22.5999935638448));
#306070=CARTESIAN_POINT('Ctrl Pts',(-4.13699602943188,-3.00570355357157,
-22.5124935638448));
#306071=CARTESIAN_POINT('Ctrl Pts',(-2.85859395067575,-3.93451703167836,
-22.4249935638448));
#306072=CARTESIAN_POINT('Ctrl Pts',(-1.58019187191962,-4.86333050978515,
-22.3374935638448));
#306073=CARTESIAN_POINT('Ctrl Pts',(-5.95586214200406E-16,-4.86333050978515,
-22.2499935638448));
#306074=CARTESIAN_POINT('Ctrl Pts',(1.58019187191962,-4.86333050978515,
-22.1624935638448));
#306075=CARTESIAN_POINT('Ctrl Pts',(2.85859395067575,-3.93451703167836,
-22.0749935638448));
#306076=CARTESIAN_POINT('Ctrl Pts',(4.13699602943187,-3.00570355357157,
-21.9874935638448));
#306077=CARTESIAN_POINT('Ctrl Pts',(4.6253021722282,-1.50285177678579,-21.8999935638448));
#306078=CARTESIAN_POINT('Ctrl Pts',(5.11360831502452,1.63211885152309E-15,
-21.8124935638448));
#306079=CARTESIAN_POINT('Ctrl Pts',(4.6253021722282,1.50285177678579,-21.7249935638448));
#306080=CARTESIAN_POINT('Ctrl Pts',(4.13699602943188,3.00570355357158,-21.6374935638448));
#306081=CARTESIAN_POINT('Ctrl Pts',(2.85859395067575,3.93451703167837,-21.5499935638448));
#306082=CARTESIAN_POINT('Ctrl Pts',(1.58019187191962,4.86333050978515,-21.4624935638448));
#306083=CARTESIAN_POINT('Ctrl Pts',(0.,4.86333050978515,-21.3749935638448));
#306084=CARTESIAN_POINT('Ctrl Pts',(-1.58019187191962,4.86333050978515,
-21.2874935638448));
#306085=CARTESIAN_POINT('Ctrl Pts',(-2.85859395067575,3.93451703167837,
-21.1999935638448));
#306086=CARTESIAN_POINT('Ctrl Pts',(-4.13699602943188,3.00570355357158,
-21.1124935638448));
#306087=CARTESIAN_POINT('Ctrl Pts',(-4.6253021722282,1.50285177678579,-21.0249935638448));
#306088=CARTESIAN_POINT('Ctrl Pts',(-5.11360831502452,2.91191659424667E-15,
-20.9374935638448));
#306089=CARTESIAN_POINT('Ctrl Pts',(-4.6253021722282,-1.50285177678579,
-20.8499935638448));
#306090=CARTESIAN_POINT('Ctrl Pts',(-4.13699602943188,-3.00570355357157,
-20.7624935638448));
#306091=CARTESIAN_POINT('Ctrl Pts',(-2.85859395067575,-3.93451703167836,
-20.6749935638448));
#306092=CARTESIAN_POINT('Ctrl Pts',(-1.58019187191962,-4.86333050978515,
-20.5874935638448));
#306093=CARTESIAN_POINT('Ctrl Pts',(-5.95586214200406E-16,-4.86333050978515,
-20.4999935638448));
#306094=CARTESIAN_POINT('Ctrl Pts',(1.58019187191962,-4.86333050978515,
-20.4124935638448));
#306095=CARTESIAN_POINT('Ctrl Pts',(2.85859395067575,-3.93451703167836,
-20.3249935638448));
#306096=CARTESIAN_POINT('Ctrl Pts',(4.13699602943187,-3.00570355357157,
-20.2374935638448));
#306097=CARTESIAN_POINT('Ctrl Pts',(4.6253021722282,-1.50285177678579,-20.1499935638448));
#306098=CARTESIAN_POINT('Ctrl Pts',(5.11360831502452,1.68676871493504E-15,
-20.0624935638448));
#306099=CARTESIAN_POINT('Ctrl Pts',(4.6253021722282,1.50285177678579,-19.9749935638448));
#306100=CARTESIAN_POINT('Ctrl Pts',(4.13699602943188,3.00570355357158,-19.8874935638448));
#306101=CARTESIAN_POINT('Ctrl Pts',(2.85859395067575,3.93451703167837,-19.7999935638448));
#306102=CARTESIAN_POINT('Ctrl Pts',(1.58019187191962,4.86333050978515,-19.7124935638448));
#306103=CARTESIAN_POINT('Ctrl Pts',(0.,4.86333050978515,-19.6249935638448));
#306104=CARTESIAN_POINT('Ctrl Pts',(-1.58019187191962,4.86333050978515,
-19.5374935638448));
#306105=CARTESIAN_POINT('Ctrl Pts',(-2.85859395067575,3.93451703167837,
-19.4499935638448));
#306106=CARTESIAN_POINT('Ctrl Pts',(-4.13699602943188,3.00570355357158,
-19.3624935638448));
#306107=CARTESIAN_POINT('Ctrl Pts',(-4.6253021722282,1.50285177678579,-19.2749935638448));
#306108=CARTESIAN_POINT('Ctrl Pts',(-5.11360831502452,2.96656645765862E-15,
-19.1874935638448));
#306109=CARTESIAN_POINT('Ctrl Pts',(-4.6253021722282,-1.50285177678579,
-19.0999935638448));
#306110=CARTESIAN_POINT('Ctrl Pts',(-4.13699602943188,-3.00570355357157,
-19.0124935638448));
#306111=CARTESIAN_POINT('Ctrl Pts',(-2.85859395067575,-3.93451703167836,
-18.9249935638448));
#306112=CARTESIAN_POINT('Ctrl Pts',(-1.58019187191962,-4.86333050978515,
-18.8374935638448));
#306113=CARTESIAN_POINT('Ctrl Pts',(-5.95586214200406E-16,-4.86333050978515,
-18.7499935638448));
#306114=CARTESIAN_POINT('Ctrl Pts',(1.58019187191962,-4.86333050978515,
-18.6624935638448));
#306115=CARTESIAN_POINT('Ctrl Pts',(2.85859395067575,-3.93451703167836,
-18.5749935638448));
#306116=CARTESIAN_POINT('Ctrl Pts',(4.13699602943187,-3.00570355357157,
-18.4874935638448));
#306117=CARTESIAN_POINT('Ctrl Pts',(4.6253021722282,-1.50285177678579,-18.3999935638448));
#306118=CARTESIAN_POINT('Ctrl Pts',(5.11360831502452,1.74141857834699E-15,
-18.3124935638448));
#306119=CARTESIAN_POINT('Ctrl Pts',(4.6253021722282,1.50285177678579,-18.2249935638448));
#306120=CARTESIAN_POINT('Ctrl Pts',(4.13699602943188,3.00570355357158,-18.1374935638448));
#306121=CARTESIAN_POINT('Ctrl Pts',(2.85859395067575,3.93451703167837,-18.0499935638448));
#306122=CARTESIAN_POINT('Ctrl Pts',(1.58019187191962,4.86333050978515,-17.9624935638448));
#306123=CARTESIAN_POINT('Ctrl Pts',(0.,4.86333050978515,-17.8749935638448));
#306124=CARTESIAN_POINT('Ctrl Pts',(-1.58019187191962,4.86333050978515,
-17.7874935638448));
#306125=CARTESIAN_POINT('Ctrl Pts',(-2.85859395067575,3.93451703167837,
-17.6999935638448));
#306126=CARTESIAN_POINT('Ctrl Pts',(-4.13699602943188,3.00570355357158,
-17.6124935638448));
#306127=CARTESIAN_POINT('Ctrl Pts',(-4.6253021722282,1.50285177678579,-17.5249935638448));
#306128=CARTESIAN_POINT('Ctrl Pts',(-5.11360831502452,3.02121632107057E-15,
-17.4374935638448));
#306129=CARTESIAN_POINT('Ctrl Pts',(-4.6253021722282,-1.50285177678579,
-17.3499935638448));
#306130=CARTESIAN_POINT('Ctrl Pts',(-4.13699602943188,-3.00570355357157,
-17.2624935638448));
#306131=CARTESIAN_POINT('Ctrl Pts',(-2.85859395067575,-3.93451703167836,
-17.1749935638448));
#306132=CARTESIAN_POINT('Ctrl Pts',(-1.58019187191962,-4.86333050978515,
-17.0874935638448));
#306133=CARTESIAN_POINT('Ctrl Pts',(-5.95586214200406E-16,-4.86333050978515,
-16.9999935638448));
#306134=CARTESIAN_POINT('Ctrl Pts',(1.58019187191962,-4.86333050978515,
-16.9124935638448));
#306135=CARTESIAN_POINT('Ctrl Pts',(2.85859395067575,-3.93451703167836,
-16.8249935638448));
#306136=CARTESIAN_POINT('Ctrl Pts',(4.13699602943187,-3.00570355357157,
-16.7374935638448));
#306137=CARTESIAN_POINT('Ctrl Pts',(4.6253021722282,-1.50285177678579,-16.6499935638448));
#306138=CARTESIAN_POINT('Ctrl Pts',(5.11360831502452,1.79606844175894E-15,
-16.5624935638448));
#306139=CARTESIAN_POINT('Ctrl Pts',(4.6253021722282,1.50285177678579,-16.4749935638448));
#306140=CARTESIAN_POINT('Ctrl Pts',(4.13699602943188,3.00570355357158,-16.3874935638448));
#306141=CARTESIAN_POINT('Ctrl Pts',(2.85859395067575,3.93451703167837,-16.2999935638448));
#306142=CARTESIAN_POINT('Ctrl Pts',(1.58019187191962,4.86333050978515,-16.2124935638448));
#306143=CARTESIAN_POINT('Ctrl Pts',(0.,4.86333050978515,-16.1249935638448));
#306144=CARTESIAN_POINT('Ctrl Pts',(-1.58019187191962,4.86333050978515,
-16.0374935638448));
#306145=CARTESIAN_POINT('Ctrl Pts',(-2.85859395067575,3.93451703167837,
-15.9499935638448));
#306146=CARTESIAN_POINT('Ctrl Pts',(-4.13699602943188,3.00570355357158,
-15.8624935638448));
#306147=CARTESIAN_POINT('Ctrl Pts',(-4.6253021722282,1.50285177678579,-15.7749935638448));
#306148=CARTESIAN_POINT('Ctrl Pts',(-5.11360831502452,3.07586618448253E-15,
-15.6874935638448));
#306149=CARTESIAN_POINT('Ctrl Pts',(-4.6253021722282,-1.50285177678579,
-15.5999935638448));
#306150=CARTESIAN_POINT('Ctrl Pts',(-4.13699602943188,-3.00570355357157,
-15.5124935638448));
#306151=CARTESIAN_POINT('Ctrl Pts',(-2.85859395067575,-3.93451703167836,
-15.4249935638448));
#306152=CARTESIAN_POINT('Ctrl Pts',(-1.58019187191962,-4.86333050978515,
-15.3374935638448));
#306153=CARTESIAN_POINT('Ctrl Pts',(-5.95586214200406E-16,-4.86333050978515,
-15.2499935638448));
#306154=CARTESIAN_POINT('Ctrl Pts',(1.58019187191962,-4.86333050978515,
-15.1624935638448));
#306155=CARTESIAN_POINT('Ctrl Pts',(2.85859395067575,-3.93451703167836,
-15.0749935638448));
#306156=CARTESIAN_POINT('Ctrl Pts',(4.13699602943187,-3.00570355357157,
-14.9874935638448));
#306157=CARTESIAN_POINT('Ctrl Pts',(4.6253021722282,-1.50285177678579,-14.8999935638448));
#306158=CARTESIAN_POINT('Ctrl Pts',(5.11360831502452,1.85071830517089E-15,
-14.8124935638448));
#306159=CARTESIAN_POINT('Ctrl Pts',(4.6253021722282,1.50285177678579,-14.7249935638448));
#306160=CARTESIAN_POINT('Ctrl Pts',(4.13699602943188,3.00570355357158,-14.6374935638448));
#306161=CARTESIAN_POINT('Ctrl Pts',(2.85859395067575,3.93451703167837,-14.5499935638448));
#306162=CARTESIAN_POINT('Ctrl Pts',(1.58019187191962,4.86333050978515,-14.4624935638448));
#306163=CARTESIAN_POINT('Ctrl Pts',(0.,4.86333050978515,-14.3749935638448));
#306164=CARTESIAN_POINT('Ctrl Pts',(-1.58019187191962,4.86333050978515,
-14.2874935638448));
#306165=CARTESIAN_POINT('Ctrl Pts',(-2.85859395067575,3.93451703167837,
-14.1999935638448));
#306166=CARTESIAN_POINT('Ctrl Pts',(-4.13699602943188,3.00570355357158,
-14.1124935638448));
#306167=CARTESIAN_POINT('Ctrl Pts',(-4.6253021722282,1.50285177678579,-14.0249935638448));
#306168=CARTESIAN_POINT('Ctrl Pts',(-5.11360831502452,3.13051604789448E-15,
-13.9374935638448));
#306169=CARTESIAN_POINT('Ctrl Pts',(-4.6253021722282,-1.50285177678579,
-13.8499935638448));
#306170=CARTESIAN_POINT('Ctrl Pts',(-4.13699602943188,-3.00570355357157,
-13.7624935638448));
#306171=CARTESIAN_POINT('Ctrl Pts',(-2.85859395067575,-3.93451703167836,
-13.6749935638448));
#306172=CARTESIAN_POINT('Ctrl Pts',(-1.58019187191962,-4.86333050978515,
-13.5874935638448));
#306173=CARTESIAN_POINT('Ctrl Pts',(-5.95586214200406E-16,-4.86333050978515,
-13.4999935638448));
#306174=CARTESIAN_POINT('Ctrl Pts',(1.58019187191962,-4.86333050978515,
-13.4124935638448));
#306175=CARTESIAN_POINT('Ctrl Pts',(2.85859395067575,-3.93451703167836,
-13.3249935638448));
#306176=CARTESIAN_POINT('Ctrl Pts',(4.13699602943187,-3.00570355357157,
-13.2374935638448));
#306177=CARTESIAN_POINT('Ctrl Pts',(4.6253021722282,-1.50285177678579,-13.1499935638448));
#306178=CARTESIAN_POINT('Ctrl Pts',(5.11360831502452,1.90536816858284E-15,
-13.0624935638448));
#306179=CARTESIAN_POINT('Ctrl Pts',(4.6253021722282,1.50285177678579,-12.9749935638448));
#306180=CARTESIAN_POINT('Ctrl Pts',(4.13699602943188,3.00570355357158,-12.8874935638448));
#306181=CARTESIAN_POINT('Ctrl Pts',(2.85859395067575,3.93451703167837,-12.7999935638448));
#306182=CARTESIAN_POINT('Ctrl Pts',(1.58019187191962,4.86333050978515,-12.7124935638448));
#306183=CARTESIAN_POINT('Ctrl Pts',(0.,4.86333050978515,-12.6249935638448));
#306184=CARTESIAN_POINT('Ctrl Pts',(-1.58019187191962,4.86333050978515,
-12.5374935638448));
#306185=CARTESIAN_POINT('Ctrl Pts',(-2.85859395067575,3.93451703167837,
-12.4499935638448));
#306186=CARTESIAN_POINT('Ctrl Pts',(-4.13699602943188,3.00570355357158,
-12.3624935638448));
#306187=CARTESIAN_POINT('Ctrl Pts',(-4.6253021722282,1.50285177678579,-12.2749935638448));
#306188=CARTESIAN_POINT('Ctrl Pts',(-5.11360831502452,3.18516591130643E-15,
-12.1874935638448));
#306189=CARTESIAN_POINT('Ctrl Pts',(-4.6253021722282,-1.50285177678579,
-12.0999935638448));
#306190=CARTESIAN_POINT('Ctrl Pts',(-4.13699602943188,-3.00570355357157,
-12.0124935638448));
#306191=CARTESIAN_POINT('Ctrl Pts',(-2.85859395067575,-3.93451703167836,
-11.9249935638448));
#306192=CARTESIAN_POINT('Ctrl Pts',(-1.58019187191962,-4.86333050978515,
-11.8374935638448));
#306193=CARTESIAN_POINT('Ctrl Pts',(-5.95586214200406E-16,-4.86333050978515,
-11.7499935638448));
#306194=CARTESIAN_POINT('Ctrl Pts',(1.58019187191962,-4.86333050978515,
-11.6624935638448));
#306195=CARTESIAN_POINT('Ctrl Pts',(2.85859395067575,-3.93451703167836,
-11.5749935638448));
#306196=CARTESIAN_POINT('Ctrl Pts',(4.13699602943187,-3.00570355357157,
-11.4874935638448));
#306197=CARTESIAN_POINT('Ctrl Pts',(4.6253021722282,-1.50285177678579,-11.3999935638448));
#306198=CARTESIAN_POINT('Ctrl Pts',(5.11360831502452,1.96001803199479E-15,
-11.3124935638448));
#306199=CARTESIAN_POINT('Ctrl Pts',(4.6253021722282,1.50285177678579,-11.2249935638448));
#306200=CARTESIAN_POINT('Ctrl Pts',(4.13699602943188,3.00570355357158,-11.1374935638448));
#306201=CARTESIAN_POINT('Ctrl Pts',(2.85859395067575,3.93451703167837,-11.0499935638448));
#306202=CARTESIAN_POINT('Ctrl Pts',(1.58019187191962,4.86333050978515,-10.9624935638448));
#306203=CARTESIAN_POINT('Ctrl Pts',(0.,4.86333050978515,-10.8749935638448));
#306204=CARTESIAN_POINT('Ctrl Pts',(-1.58019187191962,4.86333050978515,
-10.7874935638448));
#306205=CARTESIAN_POINT('Ctrl Pts',(-2.85859395067575,3.93451703167837,
-10.6999935638448));
#306206=CARTESIAN_POINT('Ctrl Pts',(-4.13699602943188,3.00570355357158,
-10.6124935638448));
#306207=CARTESIAN_POINT('Ctrl Pts',(-4.6253021722282,1.50285177678579,-10.5249935638448));
#306208=CARTESIAN_POINT('Ctrl Pts',(-5.11360831502452,3.23981577471838E-15,
-10.4374935638448));
#306209=CARTESIAN_POINT('Ctrl Pts',(-4.6253021722282,-1.50285177678579,
-10.3499935638448));
#306210=CARTESIAN_POINT('Ctrl Pts',(-4.13699602943188,-3.00570355357157,
-10.2624935638448));
#306211=CARTESIAN_POINT('Ctrl Pts',(-2.85859395067575,-3.93451703167836,
-10.1749935638448));
#306212=CARTESIAN_POINT('Ctrl Pts',(-1.58019187191962,-4.86333050978515,
-10.0874935638448));
#306213=CARTESIAN_POINT('Ctrl Pts',(-5.95586214200406E-16,-4.86333050978515,
-9.99999356384482));
#306214=CARTESIAN_POINT('Ctrl Pts',(1.58019187191962,-4.86333050978515,
-9.91249356384481));
#306215=CARTESIAN_POINT('Ctrl Pts',(2.85859395067575,-3.93451703167836,
-9.82499356384482));
#306216=CARTESIAN_POINT('Ctrl Pts',(4.13699602943187,-3.00570355357157,
-9.73749356384481));
#306217=CARTESIAN_POINT('Ctrl Pts',(4.6253021722282,-1.50285177678579,-9.64999356384482));
#306218=CARTESIAN_POINT('Ctrl Pts',(5.11360831502452,2.01466789540674E-15,
-9.56249356384481));
#306219=CARTESIAN_POINT('Ctrl Pts',(4.6253021722282,1.50285177678579,-9.47499356384482));
#306220=CARTESIAN_POINT('Ctrl Pts',(4.13699602943188,3.00570355357158,-9.3874935638448));
#306221=CARTESIAN_POINT('Ctrl Pts',(2.85859395067575,3.93451703167837,-9.29999356384481));
#306222=CARTESIAN_POINT('Ctrl Pts',(1.58019187191962,4.86333050978515,-9.21249356384481));
#306223=CARTESIAN_POINT('Ctrl Pts',(0.,4.86333050978515,-9.12499356384482));
#306224=CARTESIAN_POINT('Ctrl Pts',(-1.58019187191962,4.86333050978515,
-9.03749356384481));
#306225=CARTESIAN_POINT('Ctrl Pts',(-2.85859395067575,3.93451703167837,
-8.94999356384482));
#306226=CARTESIAN_POINT('Ctrl Pts',(-4.13699602943188,3.00570355357158,
-8.86249356384481));
#306227=CARTESIAN_POINT('Ctrl Pts',(-4.6253021722282,1.50285177678579,-8.77499356384481));
#306228=CARTESIAN_POINT('Ctrl Pts',(-5.11360831502452,3.29446563813033E-15,
-8.68749356384481));
#306229=CARTESIAN_POINT('Ctrl Pts',(-4.6253021722282,-1.50285177678579,
-8.59999356384482));
#306230=CARTESIAN_POINT('Ctrl Pts',(-4.13699602943188,-3.00570355357157,
-8.5124935638448));
#306231=CARTESIAN_POINT('Ctrl Pts',(-2.85859395067575,-3.93451703167836,
-8.42499356384482));
#306232=CARTESIAN_POINT('Ctrl Pts',(-1.58019187191962,-4.86333050978515,
-8.33749356384481));
#306233=CARTESIAN_POINT('Ctrl Pts',(-5.95586214200406E-16,-4.86333050978515,
-8.24999356384481));
#306234=CARTESIAN_POINT('Ctrl Pts',(1.58019187191962,-4.86333050978515,
-8.16249356384481));
#306235=CARTESIAN_POINT('Ctrl Pts',(2.85859395067575,-3.93451703167836,
-8.07499356384482));
#306236=CARTESIAN_POINT('Ctrl Pts',(4.13699602943187,-3.00570355357157,
-7.98749356384481));
#306237=CARTESIAN_POINT('Ctrl Pts',(4.6253021722282,-1.50285177678579,-7.89999356384481));
#306238=CARTESIAN_POINT('Ctrl Pts',(5.11360831502452,2.06931775881869E-15,
-7.81249356384481));
#306239=CARTESIAN_POINT('Ctrl Pts',(4.6253021722282,1.50285177678579,-7.72499356384482));
#306240=CARTESIAN_POINT('Ctrl Pts',(4.13699602943188,3.00570355357158,-7.6374935638448));
#306241=CARTESIAN_POINT('Ctrl Pts',(2.85859395067575,3.93451703167837,-7.54999356384482));
#306242=CARTESIAN_POINT('Ctrl Pts',(1.58019187191962,4.86333050978515,-7.46249356384481));
#306243=CARTESIAN_POINT('Ctrl Pts',(0.,4.86333050978515,-7.37499356384482));
#306244=CARTESIAN_POINT('Ctrl Pts',(-1.58019187191962,4.86333050978515,
-7.28749356384481));
#306245=CARTESIAN_POINT('Ctrl Pts',(-2.85859395067575,3.93451703167837,
-7.19999356384482));
#306246=CARTESIAN_POINT('Ctrl Pts',(-4.13699602943188,3.00570355357158,
-7.11249356384481));
#306247=CARTESIAN_POINT('Ctrl Pts',(-4.6253021722282,1.50285177678579,-7.02499356384482));
#306248=CARTESIAN_POINT('Ctrl Pts',(-5.11360831502452,3.34911550154228E-15,
-6.93749356384481));
#306249=CARTESIAN_POINT('Ctrl Pts',(-4.6253021722282,-1.50285177678579,
-6.84999356384481));
#306250=CARTESIAN_POINT('Ctrl Pts',(-4.13699602943188,-3.00570355357157,
-6.76249356384481));
#306251=CARTESIAN_POINT('Ctrl Pts',(-2.85859395067575,-3.93451703167836,
-6.67499356384482));
#306252=CARTESIAN_POINT('Ctrl Pts',(-1.58019187191962,-4.86333050978515,
-6.58749356384481));
#306253=CARTESIAN_POINT('Ctrl Pts',(-5.95586214200406E-16,-4.86333050978515,
-6.49999356384482));
#306254=CARTESIAN_POINT('Ctrl Pts',(1.58019187191962,-4.86333050978515,
-6.41249356384481));
#306255=CARTESIAN_POINT('Ctrl Pts',(2.85859395067575,-3.93451703167836,
-6.32499356384482));
#306256=CARTESIAN_POINT('Ctrl Pts',(4.13699602943187,-3.00570355357157,
-6.23749356384481));
#306257=CARTESIAN_POINT('Ctrl Pts',(4.6253021722282,-1.50285177678579,-6.14999356384482));
#306258=CARTESIAN_POINT('Ctrl Pts',(5.11360831502452,2.12396762223064E-15,
-6.06249356384482));
#306259=CARTESIAN_POINT('Ctrl Pts',(4.6253021722282,1.50285177678579,-5.97499356384481));
#306260=CARTESIAN_POINT('Ctrl Pts',(4.13699602943188,3.00570355357158,-5.88749356384482));
#306261=CARTESIAN_POINT('Ctrl Pts',(2.85859395067575,3.93451703167837,-5.79999356384481));
#306262=CARTESIAN_POINT('Ctrl Pts',(1.58019187191962,4.86333050978515,-5.71249356384481));
#306263=CARTESIAN_POINT('Ctrl Pts',(0.,4.86333050978515,-5.62499356384482));
#306264=CARTESIAN_POINT('Ctrl Pts',(-1.58019187191962,4.86333050978515,
-5.53749356384482));
#306265=CARTESIAN_POINT('Ctrl Pts',(-2.85859395067575,3.93451703167837,
-5.44999356384482));
#306266=CARTESIAN_POINT('Ctrl Pts',(-3.39156536058037,3.54729063617168,
-5.41351443169882));
#306267=CARTESIAN_POINT('Ctrl Pts',(-3.80231226593749,3.03222774205837,
-5.3751966204675));
#306268=CARTESIAN_POINT('Ctrl Pts',(0.,6.09472152853892,-37.8359375));
#306269=CARTESIAN_POINT('Ctrl Pts',(-1.98029506767702,6.09472152853892,
-37.7484375));
#306270=CARTESIAN_POINT('Ctrl Pts',(-3.58238743130462,4.93073329257085,
-37.6609375));
#306271=CARTESIAN_POINT('Ctrl Pts',(-5.18447979493222,3.76674505660277,
-37.5734375));
#306272=CARTESIAN_POINT('Ctrl Pts',(-5.7964246247213,1.88337252830138,-37.4859375));
#306273=CARTESIAN_POINT('Ctrl Pts',(-6.40836945451038,2.47714736979317E-15,
-37.3984375));
#306274=CARTESIAN_POINT('Ctrl Pts',(-5.7964246247213,-1.88337252830138,
-37.3109375));
#306275=CARTESIAN_POINT('Ctrl Pts',(-5.18447979493222,-3.76674505660276,
-37.2234375));
#306276=CARTESIAN_POINT('Ctrl Pts',(-3.58238743130462,-4.93073329257084,
-37.1359375));
#306277=CARTESIAN_POINT('Ctrl Pts',(-1.98029506767702,-6.09472152853892,
-37.0484374999999));
#306278=CARTESIAN_POINT('Ctrl Pts',(-7.46388121161966E-16,-6.09472152853892,
-36.9609375));
#306279=CARTESIAN_POINT('Ctrl Pts',(1.98029506767702,-6.09472152853892,
-36.8734375));
#306280=CARTESIAN_POINT('Ctrl Pts',(3.58238743130462,-4.93073329257084,
-36.7859375));
#306281=CARTESIAN_POINT('Ctrl Pts',(5.18447979493222,-3.76674505660277,
-36.6984375));
#306282=CARTESIAN_POINT('Ctrl Pts',(5.7964246247213,-1.88337252830138,-36.6109375));
#306283=CARTESIAN_POINT('Ctrl Pts',(6.40836945451038,9.34874473455184E-16,
-36.5234375));
#306284=CARTESIAN_POINT('Ctrl Pts',(5.7964246247213,1.88337252830138,-36.4359375));
#306285=CARTESIAN_POINT('Ctrl Pts',(5.18447979493222,3.76674505660277,-36.3484375));
#306286=CARTESIAN_POINT('Ctrl Pts',(3.58238743130462,4.93073329257085,-36.2609375));
#306287=CARTESIAN_POINT('Ctrl Pts',(1.98029506767702,6.09472152853892,-36.1734375));
#306288=CARTESIAN_POINT('Ctrl Pts',(0.,6.09472152853892,-36.0859375));
#306289=CARTESIAN_POINT('Ctrl Pts',(-1.98029506767702,6.09472152853892,
-35.9984375));
#306290=CARTESIAN_POINT('Ctrl Pts',(-3.58238743130462,4.93073329257085,
-35.9109375));
#306291=CARTESIAN_POINT('Ctrl Pts',(-5.18447979493222,3.76674505660277,
-35.8234375));
#306292=CARTESIAN_POINT('Ctrl Pts',(-5.7964246247213,1.88337252830138,-35.7359375));
#306293=CARTESIAN_POINT('Ctrl Pts',(-6.40836945451038,2.53179723320512E-15,
-35.6484375));
#306294=CARTESIAN_POINT('Ctrl Pts',(-5.7964246247213,-1.88337252830138,
-35.5609375));
#306295=CARTESIAN_POINT('Ctrl Pts',(-5.18447979493222,-3.76674505660276,
-35.4734375));
#306296=CARTESIAN_POINT('Ctrl Pts',(-3.58238743130462,-4.93073329257084,
-35.3859375));
#306297=CARTESIAN_POINT('Ctrl Pts',(-1.98029506767702,-6.09472152853892,
-35.2984375));
#306298=CARTESIAN_POINT('Ctrl Pts',(-7.46388121161966E-16,-6.09472152853892,
-35.2109375));
#306299=CARTESIAN_POINT('Ctrl Pts',(1.98029506767702,-6.09472152853892,
-35.1234375));
#306300=CARTESIAN_POINT('Ctrl Pts',(3.58238743130462,-4.93073329257084,
-35.0359375));
#306301=CARTESIAN_POINT('Ctrl Pts',(5.18447979493222,-3.76674505660277,
-34.9484375));
#306302=CARTESIAN_POINT('Ctrl Pts',(5.7964246247213,-1.88337252830138,-34.8609375));
#306303=CARTESIAN_POINT('Ctrl Pts',(6.40836945451038,9.89524336867135E-16,
-34.7734375));
#306304=CARTESIAN_POINT('Ctrl Pts',(5.7964246247213,1.88337252830138,-34.6859375));
#306305=CARTESIAN_POINT('Ctrl Pts',(5.18447979493222,3.76674505660277,-34.5984375));
#306306=CARTESIAN_POINT('Ctrl Pts',(3.58238743130462,4.93073329257085,-34.5109375));
#306307=CARTESIAN_POINT('Ctrl Pts',(1.98029506767702,6.09472152853892,-34.4234375));
#306308=CARTESIAN_POINT('Ctrl Pts',(0.,6.09472152853892,-34.3359375));
#306309=CARTESIAN_POINT('Ctrl Pts',(-1.98029506767702,6.09472152853892,
-34.2484375));
#306310=CARTESIAN_POINT('Ctrl Pts',(-3.58238743130462,4.93073329257085,
-34.1609375));
#306311=CARTESIAN_POINT('Ctrl Pts',(-5.18447979493222,3.76674505660277,
-34.0734375));
#306312=CARTESIAN_POINT('Ctrl Pts',(-5.7964246247213,1.88337252830138,-33.9859375));
#306313=CARTESIAN_POINT('Ctrl Pts',(-6.40836945451038,2.58644709661707E-15,
-33.8984375));
#306314=CARTESIAN_POINT('Ctrl Pts',(-5.7964246247213,-1.88337252830138,
-33.8109375));
#306315=CARTESIAN_POINT('Ctrl Pts',(-5.18447979493222,-3.76674505660276,
-33.7234375));
#306316=CARTESIAN_POINT('Ctrl Pts',(-3.58238743130462,-4.93073329257084,
-33.6359375));
#306317=CARTESIAN_POINT('Ctrl Pts',(-1.98029506767702,-6.09472152853892,
-33.5484375));
#306318=CARTESIAN_POINT('Ctrl Pts',(-7.46388121161966E-16,-6.09472152853892,
-33.4609375));
#306319=CARTESIAN_POINT('Ctrl Pts',(1.98029506767702,-6.09472152853892,
-33.3734375));
#306320=CARTESIAN_POINT('Ctrl Pts',(3.58238743130462,-4.93073329257084,
-33.2859375));
#306321=CARTESIAN_POINT('Ctrl Pts',(5.18447979493222,-3.76674505660277,
-33.1984375));
#306322=CARTESIAN_POINT('Ctrl Pts',(5.7964246247213,-1.88337252830138,-33.1109375));
#306323=CARTESIAN_POINT('Ctrl Pts',(6.40836945451038,1.04417420027908E-15,
-33.0234375));
#306324=CARTESIAN_POINT('Ctrl Pts',(5.7964246247213,1.88337252830138,-32.9359375));
#306325=CARTESIAN_POINT('Ctrl Pts',(5.18447979493222,3.76674505660277,-32.8484375));
#306326=CARTESIAN_POINT('Ctrl Pts',(3.58238743130462,4.93073329257085,-32.7609375));
#306327=CARTESIAN_POINT('Ctrl Pts',(1.98029506767702,6.09472152853892,-32.6734375));
#306328=CARTESIAN_POINT('Ctrl Pts',(0.,6.09472152853892,-32.5859375));
#306329=CARTESIAN_POINT('Ctrl Pts',(-1.98029506767702,6.09472152853892,
-32.4984375));
#306330=CARTESIAN_POINT('Ctrl Pts',(-3.58238743130462,4.93073329257085,
-32.4109375));
#306331=CARTESIAN_POINT('Ctrl Pts',(-5.18447979493222,3.76674505660277,
-32.3234375));
#306332=CARTESIAN_POINT('Ctrl Pts',(-5.7964246247213,1.88337252830138,-32.2359375));
#306333=CARTESIAN_POINT('Ctrl Pts',(-6.40836945451038,2.64109696002902E-15,
-32.1484375));
#306334=CARTESIAN_POINT('Ctrl Pts',(-5.7964246247213,-1.88337252830138,
-32.0609375));
#306335=CARTESIAN_POINT('Ctrl Pts',(-5.18447979493222,-3.76674505660276,
-31.9734375));
#306336=CARTESIAN_POINT('Ctrl Pts',(-3.58238743130462,-4.93073329257084,
-31.8859375));
#306337=CARTESIAN_POINT('Ctrl Pts',(-1.98029506767702,-6.09472152853892,
-31.7984375));
#306338=CARTESIAN_POINT('Ctrl Pts',(-7.46388121161966E-16,-6.09472152853892,
-31.7109375));
#306339=CARTESIAN_POINT('Ctrl Pts',(1.98029506767702,-6.09472152853892,
-31.6234375));
#306340=CARTESIAN_POINT('Ctrl Pts',(3.58238743130462,-4.93073329257084,
-31.5359375));
#306341=CARTESIAN_POINT('Ctrl Pts',(5.18447979493222,-3.76674505660277,
-31.4484375));
#306342=CARTESIAN_POINT('Ctrl Pts',(5.7964246247213,-1.88337252830138,-31.3609375));
#306343=CARTESIAN_POINT('Ctrl Pts',(6.40836945451038,1.09882406369103E-15,
-31.2734375));
#306344=CARTESIAN_POINT('Ctrl Pts',(5.7964246247213,1.88337252830138,-31.1859375));
#306345=CARTESIAN_POINT('Ctrl Pts',(5.18447979493222,3.76674505660277,-31.0984375));
#306346=CARTESIAN_POINT('Ctrl Pts',(3.58238743130462,4.93073329257085,-31.0109375));
#306347=CARTESIAN_POINT('Ctrl Pts',(1.98029506767702,6.09472152853892,-30.9234375));
#306348=CARTESIAN_POINT('Ctrl Pts',(0.,6.09472152853892,-30.8359375));
#306349=CARTESIAN_POINT('Ctrl Pts',(-1.98029506767702,6.09472152853892,
-30.7484375));
#306350=CARTESIAN_POINT('Ctrl Pts',(-3.58238743130462,4.93073329257085,
-30.6609375));
#306351=CARTESIAN_POINT('Ctrl Pts',(-5.18447979493222,3.76674505660277,
-30.5734375));
#306352=CARTESIAN_POINT('Ctrl Pts',(-5.7964246247213,1.88337252830138,-30.4859375));
#306353=CARTESIAN_POINT('Ctrl Pts',(-6.40836945451038,2.69574682344097E-15,
-30.3984375));
#306354=CARTESIAN_POINT('Ctrl Pts',(-5.7964246247213,-1.88337252830138,
-30.3109375));
#306355=CARTESIAN_POINT('Ctrl Pts',(-5.18447979493222,-3.76674505660276,
-30.2234375));
#306356=CARTESIAN_POINT('Ctrl Pts',(-3.58238743130462,-4.93073329257084,
-30.1359375));
#306357=CARTESIAN_POINT('Ctrl Pts',(-1.98029506767702,-6.09472152853892,
-30.0484375));
#306358=CARTESIAN_POINT('Ctrl Pts',(-7.46388121161966E-16,-6.09472152853892,
-29.9609375));
#306359=CARTESIAN_POINT('Ctrl Pts',(1.98029506767702,-6.09472152853892,
-29.8734375));
#306360=CARTESIAN_POINT('Ctrl Pts',(3.58238743130462,-4.93073329257084,
-29.7859375));
#306361=CARTESIAN_POINT('Ctrl Pts',(5.18447979493222,-3.76674505660277,
-29.6984375));
#306362=CARTESIAN_POINT('Ctrl Pts',(5.7964246247213,-1.88337252830138,-29.6109375));
#306363=CARTESIAN_POINT('Ctrl Pts',(6.40836945451038,1.15347392710299E-15,
-29.5234375));
#306364=CARTESIAN_POINT('Ctrl Pts',(5.7964246247213,1.88337252830138,-29.4359375));
#306365=CARTESIAN_POINT('Ctrl Pts',(5.18447979493222,3.76674505660277,-29.3484375));
#306366=CARTESIAN_POINT('Ctrl Pts',(3.58238743130462,4.93073329257085,-29.2609375));
#306367=CARTESIAN_POINT('Ctrl Pts',(1.98029506767702,6.09472152853892,-29.1734375));
#306368=CARTESIAN_POINT('Ctrl Pts',(0.,6.09472152853892,-29.0859375));
#306369=CARTESIAN_POINT('Ctrl Pts',(-1.98029506767702,6.09472152853892,
-28.9984375));
#306370=CARTESIAN_POINT('Ctrl Pts',(-3.58238743130462,4.93073329257085,
-28.9109375));
#306371=CARTESIAN_POINT('Ctrl Pts',(-5.18447979493222,3.76674505660277,
-28.8234375));
#306372=CARTESIAN_POINT('Ctrl Pts',(-5.7964246247213,1.88337252830138,-28.7359375));
#306373=CARTESIAN_POINT('Ctrl Pts',(-6.40836945451038,2.75039668685292E-15,
-28.6484375));
#306374=CARTESIAN_POINT('Ctrl Pts',(-5.7964246247213,-1.88337252830138,
-28.5609375));
#306375=CARTESIAN_POINT('Ctrl Pts',(-5.18447979493222,-3.76674505660276,
-28.4734375));
#306376=CARTESIAN_POINT('Ctrl Pts',(-3.58238743130462,-4.93073329257084,
-28.3859375));
#306377=CARTESIAN_POINT('Ctrl Pts',(-1.98029506767702,-6.09472152853892,
-28.2984375));
#306378=CARTESIAN_POINT('Ctrl Pts',(-7.46388121161966E-16,-6.09472152853892,
-28.2109375));
#306379=CARTESIAN_POINT('Ctrl Pts',(1.98029506767702,-6.09472152853892,
-28.1234375));
#306380=CARTESIAN_POINT('Ctrl Pts',(3.58238743130462,-4.93073329257084,
-28.0359375));
#306381=CARTESIAN_POINT('Ctrl Pts',(5.18447979493222,-3.76674505660277,
-27.9484375));
#306382=CARTESIAN_POINT('Ctrl Pts',(5.7964246247213,-1.88337252830138,-27.8609375));
#306383=CARTESIAN_POINT('Ctrl Pts',(6.40836945451038,1.20812379051494E-15,
-27.7734375));
#306384=CARTESIAN_POINT('Ctrl Pts',(5.7964246247213,1.88337252830138,-27.6859375));
#306385=CARTESIAN_POINT('Ctrl Pts',(5.18447979493222,3.76674505660277,-27.5984375));
#306386=CARTESIAN_POINT('Ctrl Pts',(3.58238743130462,4.93073329257085,-27.5109375));
#306387=CARTESIAN_POINT('Ctrl Pts',(1.98029506767702,6.09472152853892,-27.4234375));
#306388=CARTESIAN_POINT('Ctrl Pts',(0.,6.09472152853892,-27.3359375));
#306389=CARTESIAN_POINT('Ctrl Pts',(-1.98029506767702,6.09472152853892,
-27.2484375));
#306390=CARTESIAN_POINT('Ctrl Pts',(-3.58238743130462,4.93073329257085,
-27.1609375));
#306391=CARTESIAN_POINT('Ctrl Pts',(-5.18447979493222,3.76674505660277,
-27.0734375));
#306392=CARTESIAN_POINT('Ctrl Pts',(-5.7964246247213,1.88337252830138,-26.9859375));
#306393=CARTESIAN_POINT('Ctrl Pts',(-6.40836945451038,2.80504655026487E-15,
-26.8984375));
#306394=CARTESIAN_POINT('Ctrl Pts',(-5.7964246247213,-1.88337252830138,
-26.8109375));
#306395=CARTESIAN_POINT('Ctrl Pts',(-5.18447979493222,-3.76674505660276,
-26.7234375));
#306396=CARTESIAN_POINT('Ctrl Pts',(-3.58238743130462,-4.93073329257084,
-26.6359375));
#306397=CARTESIAN_POINT('Ctrl Pts',(-1.98029506767702,-6.09472152853892,
-26.5484375));
#306398=CARTESIAN_POINT('Ctrl Pts',(-7.46388121161966E-16,-6.09472152853892,
-26.4609375));
#306399=CARTESIAN_POINT('Ctrl Pts',(1.98029506767702,-6.09472152853892,
-26.3734375));
#306400=CARTESIAN_POINT('Ctrl Pts',(3.58238743130462,-4.93073329257084,
-26.2859375));
#306401=CARTESIAN_POINT('Ctrl Pts',(5.18447979493222,-3.76674505660277,
-26.1984375));
#306402=CARTESIAN_POINT('Ctrl Pts',(5.7964246247213,-1.88337252830138,-26.1109375));
#306403=CARTESIAN_POINT('Ctrl Pts',(6.40836945451038,1.26277365392689E-15,
-26.0234375));
#306404=CARTESIAN_POINT('Ctrl Pts',(5.7964246247213,1.88337252830138,-25.9359375));
#306405=CARTESIAN_POINT('Ctrl Pts',(5.18447979493222,3.76674505660277,-25.8484375));
#306406=CARTESIAN_POINT('Ctrl Pts',(3.58238743130462,4.93073329257085,-25.7609375));
#306407=CARTESIAN_POINT('Ctrl Pts',(1.98029506767702,6.09472152853892,-25.6734375));
#306408=CARTESIAN_POINT('Ctrl Pts',(0.,6.09472152853892,-25.5859375));
#306409=CARTESIAN_POINT('Ctrl Pts',(-1.98029506767702,6.09472152853892,
-25.4984375));
#306410=CARTESIAN_POINT('Ctrl Pts',(-3.58238743130462,4.93073329257085,
-25.4109375));
#306411=CARTESIAN_POINT('Ctrl Pts',(-5.18447979493222,3.76674505660277,
-25.3234375));
#306412=CARTESIAN_POINT('Ctrl Pts',(-5.7964246247213,1.88337252830138,-25.2359375));
#306413=CARTESIAN_POINT('Ctrl Pts',(-6.40836945451038,2.85969641367683E-15,
-25.1484375));
#306414=CARTESIAN_POINT('Ctrl Pts',(-5.7964246247213,-1.88337252830138,
-25.0609375));
#306415=CARTESIAN_POINT('Ctrl Pts',(-5.18447979493222,-3.76674505660276,
-24.9734375));
#306416=CARTESIAN_POINT('Ctrl Pts',(-3.58238743130462,-4.93073329257084,
-24.8859375));
#306417=CARTESIAN_POINT('Ctrl Pts',(-1.98029506767702,-6.09472152853892,
-24.7984375));
#306418=CARTESIAN_POINT('Ctrl Pts',(-7.46388121161966E-16,-6.09472152853892,
-24.7109375));
#306419=CARTESIAN_POINT('Ctrl Pts',(1.98029506767702,-6.09472152853892,
-24.6234375));
#306420=CARTESIAN_POINT('Ctrl Pts',(3.58238743130462,-4.93073329257084,
-24.5359375));
#306421=CARTESIAN_POINT('Ctrl Pts',(5.18447979493222,-3.76674505660277,
-24.4484375));
#306422=CARTESIAN_POINT('Ctrl Pts',(5.7964246247213,-1.88337252830138,-24.3609375));
#306423=CARTESIAN_POINT('Ctrl Pts',(6.40836945451038,1.31742351733884E-15,
-24.2734375));
#306424=CARTESIAN_POINT('Ctrl Pts',(5.7964246247213,1.88337252830138,-24.1859375));
#306425=CARTESIAN_POINT('Ctrl Pts',(5.18447979493222,3.76674505660277,-24.0984375));
#306426=CARTESIAN_POINT('Ctrl Pts',(3.58238743130462,4.93073329257085,-24.0109375));
#306427=CARTESIAN_POINT('Ctrl Pts',(1.98029506767702,6.09472152853892,-23.9234375));
#306428=CARTESIAN_POINT('Ctrl Pts',(0.,6.09472152853893,-23.8359375));
#306429=CARTESIAN_POINT('Ctrl Pts',(-1.98029506767702,6.09472152853892,
-23.7484375));
#306430=CARTESIAN_POINT('Ctrl Pts',(-3.58238743130462,4.93073329257085,
-23.6609375));
#306431=CARTESIAN_POINT('Ctrl Pts',(-5.18447979493222,3.76674505660277,
-23.5734375));
#306432=CARTESIAN_POINT('Ctrl Pts',(-5.7964246247213,1.88337252830138,-23.4859375));
#306433=CARTESIAN_POINT('Ctrl Pts',(-6.40836945451038,2.91434627708878E-15,
-23.3984375));
#306434=CARTESIAN_POINT('Ctrl Pts',(-5.7964246247213,-1.88337252830138,
-23.3109375));
#306435=CARTESIAN_POINT('Ctrl Pts',(-5.18447979493222,-3.76674505660276,
-23.2234375));
#306436=CARTESIAN_POINT('Ctrl Pts',(-3.58238743130462,-4.93073329257084,
-23.1359375));
#306437=CARTESIAN_POINT('Ctrl Pts',(-1.98029506767702,-6.09472152853892,
-23.0484375));
#306438=CARTESIAN_POINT('Ctrl Pts',(-7.46388121161966E-16,-6.09472152853892,
-22.9609375));
#306439=CARTESIAN_POINT('Ctrl Pts',(1.98029506767702,-6.09472152853892,
-22.8734375));
#306440=CARTESIAN_POINT('Ctrl Pts',(3.58238743130462,-4.93073329257084,
-22.7859375));
#306441=CARTESIAN_POINT('Ctrl Pts',(5.18447979493222,-3.76674505660277,
-22.6984375));
#306442=CARTESIAN_POINT('Ctrl Pts',(5.7964246247213,-1.88337252830138,-22.6109375));
#306443=CARTESIAN_POINT('Ctrl Pts',(6.40836945451038,1.37207338075079E-15,
-22.5234375));
#306444=CARTESIAN_POINT('Ctrl Pts',(5.7964246247213,1.88337252830138,-22.4359375));
#306445=CARTESIAN_POINT('Ctrl Pts',(5.18447979493222,3.76674505660277,-22.3484375));
#306446=CARTESIAN_POINT('Ctrl Pts',(3.58238743130462,4.93073329257085,-22.2609375));
#306447=CARTESIAN_POINT('Ctrl Pts',(1.98029506767702,6.09472152853892,-22.1734375));
#306448=CARTESIAN_POINT('Ctrl Pts',(0.,6.09472152853893,-22.0859375));
#306449=CARTESIAN_POINT('Ctrl Pts',(-1.98029506767702,6.09472152853892,
-21.9984375));
#306450=CARTESIAN_POINT('Ctrl Pts',(-3.58238743130462,4.93073329257085,
-21.9109375));
#306451=CARTESIAN_POINT('Ctrl Pts',(-5.18447979493222,3.76674505660277,
-21.8234375));
#306452=CARTESIAN_POINT('Ctrl Pts',(-5.7964246247213,1.88337252830138,-21.7359375));
#306453=CARTESIAN_POINT('Ctrl Pts',(-6.40836945451038,2.96899614050073E-15,
-21.6484375));
#306454=CARTESIAN_POINT('Ctrl Pts',(-5.7964246247213,-1.88337252830138,
-21.5609375));
#306455=CARTESIAN_POINT('Ctrl Pts',(-5.18447979493222,-3.76674505660276,
-21.4734375));
#306456=CARTESIAN_POINT('Ctrl Pts',(-3.58238743130462,-4.93073329257084,
-21.3859375));
#306457=CARTESIAN_POINT('Ctrl Pts',(-1.98029506767702,-6.09472152853892,
-21.2984375));
#306458=CARTESIAN_POINT('Ctrl Pts',(-7.46388121161966E-16,-6.09472152853892,
-21.2109375));
#306459=CARTESIAN_POINT('Ctrl Pts',(1.98029506767702,-6.09472152853892,
-21.1234375));
#306460=CARTESIAN_POINT('Ctrl Pts',(3.58238743130462,-4.93073329257084,
-21.0359375));
#306461=CARTESIAN_POINT('Ctrl Pts',(5.18447979493222,-3.76674505660277,
-20.9484375));
#306462=CARTESIAN_POINT('Ctrl Pts',(5.7964246247213,-1.88337252830138,-20.8609375));
#306463=CARTESIAN_POINT('Ctrl Pts',(6.40836945451038,1.42672324416274E-15,
-20.7734375));
#306464=CARTESIAN_POINT('Ctrl Pts',(5.7964246247213,1.88337252830138,-20.6859375));
#306465=CARTESIAN_POINT('Ctrl Pts',(5.18447979493222,3.76674505660277,-20.5984375));
#306466=CARTESIAN_POINT('Ctrl Pts',(3.58238743130462,4.93073329257085,-20.5109375));
#306467=CARTESIAN_POINT('Ctrl Pts',(1.98029506767702,6.09472152853892,-20.4234375));
#306468=CARTESIAN_POINT('Ctrl Pts',(0.,6.09472152853893,-20.3359375));
#306469=CARTESIAN_POINT('Ctrl Pts',(-1.98029506767702,6.09472152853892,
-20.2484375));
#306470=CARTESIAN_POINT('Ctrl Pts',(-3.58238743130462,4.93073329257085,
-20.1609375));
#306471=CARTESIAN_POINT('Ctrl Pts',(-5.18447979493222,3.76674505660277,
-20.0734375));
#306472=CARTESIAN_POINT('Ctrl Pts',(-5.7964246247213,1.88337252830138,-19.9859375));
#306473=CARTESIAN_POINT('Ctrl Pts',(-6.40836945451038,3.02364600391268E-15,
-19.8984375));
#306474=CARTESIAN_POINT('Ctrl Pts',(-5.7964246247213,-1.88337252830138,
-19.8109375));
#306475=CARTESIAN_POINT('Ctrl Pts',(-5.18447979493222,-3.76674505660276,
-19.7234375));
#306476=CARTESIAN_POINT('Ctrl Pts',(-3.58238743130462,-4.93073329257084,
-19.6359375));
#306477=CARTESIAN_POINT('Ctrl Pts',(-1.98029506767702,-6.09472152853892,
-19.5484375));
#306478=CARTESIAN_POINT('Ctrl Pts',(-7.46388121161966E-16,-6.09472152853892,
-19.4609375));
#306479=CARTESIAN_POINT('Ctrl Pts',(1.98029506767702,-6.09472152853892,
-19.3734375));
#306480=CARTESIAN_POINT('Ctrl Pts',(3.58238743130462,-4.93073329257084,
-19.2859375));
#306481=CARTESIAN_POINT('Ctrl Pts',(5.18447979493222,-3.76674505660277,
-19.1984375));
#306482=CARTESIAN_POINT('Ctrl Pts',(5.7964246247213,-1.88337252830138,-19.1109375));
#306483=CARTESIAN_POINT('Ctrl Pts',(6.40836945451038,1.48137310757469E-15,
-19.0234375));
#306484=CARTESIAN_POINT('Ctrl Pts',(5.7964246247213,1.88337252830138,-18.9359375));
#306485=CARTESIAN_POINT('Ctrl Pts',(5.18447979493222,3.76674505660277,-18.8484375));
#306486=CARTESIAN_POINT('Ctrl Pts',(3.58238743130462,4.93073329257085,-18.7609375));
#306487=CARTESIAN_POINT('Ctrl Pts',(1.98029506767702,6.09472152853892,-18.6734375));
#306488=CARTESIAN_POINT('Ctrl Pts',(0.,6.09472152853893,-18.5859375));
#306489=CARTESIAN_POINT('Ctrl Pts',(-1.98029506767702,6.09472152853892,
-18.4984375));
#306490=CARTESIAN_POINT('Ctrl Pts',(-3.58238743130462,4.93073329257085,
-18.4109375));
#306491=CARTESIAN_POINT('Ctrl Pts',(-5.18447979493222,3.76674505660277,
-18.3234375));
#306492=CARTESIAN_POINT('Ctrl Pts',(-5.7964246247213,1.88337252830138,-18.2359375));
#306493=CARTESIAN_POINT('Ctrl Pts',(-6.40836945451038,3.07829586732463E-15,
-18.1484375));
#306494=CARTESIAN_POINT('Ctrl Pts',(-5.7964246247213,-1.88337252830138,
-18.0609375));
#306495=CARTESIAN_POINT('Ctrl Pts',(-5.18447979493222,-3.76674505660276,
-17.9734375));
#306496=CARTESIAN_POINT('Ctrl Pts',(-3.58238743130462,-4.93073329257084,
-17.8859375));
#306497=CARTESIAN_POINT('Ctrl Pts',(-1.98029506767702,-6.09472152853892,
-17.7984375));
#306498=CARTESIAN_POINT('Ctrl Pts',(-7.46388121161966E-16,-6.09472152853892,
-17.7109375));
#306499=CARTESIAN_POINT('Ctrl Pts',(1.98029506767702,-6.09472152853892,
-17.6234375));
#306500=CARTESIAN_POINT('Ctrl Pts',(3.58238743130462,-4.93073329257084,
-17.5359375));
#306501=CARTESIAN_POINT('Ctrl Pts',(5.18447979493222,-3.76674505660277,
-17.4484375));
#306502=CARTESIAN_POINT('Ctrl Pts',(5.7964246247213,-1.88337252830138,-17.3609375));
#306503=CARTESIAN_POINT('Ctrl Pts',(6.40836945451038,1.53602297098664E-15,
-17.2734375));
#306504=CARTESIAN_POINT('Ctrl Pts',(5.7964246247213,1.88337252830138,-17.1859375));
#306505=CARTESIAN_POINT('Ctrl Pts',(5.18447979493222,3.76674505660277,-17.0984375));
#306506=CARTESIAN_POINT('Ctrl Pts',(3.58238743130462,4.93073329257085,-17.0109375));
#306507=CARTESIAN_POINT('Ctrl Pts',(1.98029506767702,6.09472152853892,-16.9234375));
#306508=CARTESIAN_POINT('Ctrl Pts',(0.,6.09472152853893,-16.8359375));
#306509=CARTESIAN_POINT('Ctrl Pts',(-1.98029506767702,6.09472152853892,
-16.7484375));
#306510=CARTESIAN_POINT('Ctrl Pts',(-3.58238743130462,4.93073329257085,
-16.6609375));
#306511=CARTESIAN_POINT('Ctrl Pts',(-5.18447979493222,3.76674505660277,
-16.5734375));
#306512=CARTESIAN_POINT('Ctrl Pts',(-5.7964246247213,1.88337252830138,-16.4859375));
#306513=CARTESIAN_POINT('Ctrl Pts',(-6.40836945451038,3.13294573073658E-15,
-16.3984375));
#306514=CARTESIAN_POINT('Ctrl Pts',(-5.7964246247213,-1.88337252830138,
-16.3109375));
#306515=CARTESIAN_POINT('Ctrl Pts',(-5.18447979493222,-3.76674505660276,
-16.2234375));
#306516=CARTESIAN_POINT('Ctrl Pts',(-3.58238743130462,-4.93073329257084,
-16.1359375));
#306517=CARTESIAN_POINT('Ctrl Pts',(-1.98029506767702,-6.09472152853892,
-16.0484375));
#306518=CARTESIAN_POINT('Ctrl Pts',(-7.46388121161966E-16,-6.09472152853892,
-15.9609375));
#306519=CARTESIAN_POINT('Ctrl Pts',(1.98029506767702,-6.09472152853892,
-15.8734375));
#306520=CARTESIAN_POINT('Ctrl Pts',(3.58238743130462,-4.93073329257084,
-15.7859375));
#306521=CARTESIAN_POINT('Ctrl Pts',(5.18447979493222,-3.76674505660277,
-15.6984375));
#306522=CARTESIAN_POINT('Ctrl Pts',(5.7964246247213,-1.88337252830138,-15.6109375));
#306523=CARTESIAN_POINT('Ctrl Pts',(6.40836945451038,1.59067283439859E-15,
-15.5234375));
#306524=CARTESIAN_POINT('Ctrl Pts',(5.7964246247213,1.88337252830138,-15.4359375));
#306525=CARTESIAN_POINT('Ctrl Pts',(5.18447979493222,3.76674505660277,-15.3484375));
#306526=CARTESIAN_POINT('Ctrl Pts',(3.58238743130462,4.93073329257085,-15.2609375));
#306527=CARTESIAN_POINT('Ctrl Pts',(1.98029506767702,6.09472152853892,-15.1734375));
#306528=CARTESIAN_POINT('Ctrl Pts',(0.,6.09472152853893,-15.0859375));
#306529=CARTESIAN_POINT('Ctrl Pts',(-1.98029506767702,6.09472152853892,
-14.9984375));
#306530=CARTESIAN_POINT('Ctrl Pts',(-3.58238743130462,4.93073329257085,
-14.9109375));
#306531=CARTESIAN_POINT('Ctrl Pts',(-5.18447979493222,3.76674505660277,
-14.8234375));
#306532=CARTESIAN_POINT('Ctrl Pts',(-5.7964246247213,1.88337252830138,-14.7359375));
#306533=CARTESIAN_POINT('Ctrl Pts',(-6.40836945451038,3.18759559414853E-15,
-14.6484375));
#306534=CARTESIAN_POINT('Ctrl Pts',(-5.7964246247213,-1.88337252830138,
-14.5609375));
#306535=CARTESIAN_POINT('Ctrl Pts',(-5.18447979493222,-3.76674505660276,
-14.4734375));
#306536=CARTESIAN_POINT('Ctrl Pts',(-3.58238743130462,-4.93073329257084,
-14.3859375));
#306537=CARTESIAN_POINT('Ctrl Pts',(-1.98029506767702,-6.09472152853892,
-14.2984375));
#306538=CARTESIAN_POINT('Ctrl Pts',(-7.46388121161966E-16,-6.09472152853892,
-14.2109375));
#306539=CARTESIAN_POINT('Ctrl Pts',(1.98029506767702,-6.09472152853892,
-14.1234375));
#306540=CARTESIAN_POINT('Ctrl Pts',(3.58238743130462,-4.93073329257084,
-14.0359375));
#306541=CARTESIAN_POINT('Ctrl Pts',(5.18447979493222,-3.76674505660277,
-13.9484375));
#306542=CARTESIAN_POINT('Ctrl Pts',(5.7964246247213,-1.88337252830138,-13.8609375));
#306543=CARTESIAN_POINT('Ctrl Pts',(6.40836945451038,1.64532269781054E-15,
-13.7734375));
#306544=CARTESIAN_POINT('Ctrl Pts',(5.7964246247213,1.88337252830138,-13.6859375));
#306545=CARTESIAN_POINT('Ctrl Pts',(5.18447979493222,3.76674505660277,-13.5984375));
#306546=CARTESIAN_POINT('Ctrl Pts',(3.58238743130462,4.93073329257085,-13.5109375));
#306547=CARTESIAN_POINT('Ctrl Pts',(1.98029506767702,6.09472152853892,-13.4234375));
#306548=CARTESIAN_POINT('Ctrl Pts',(0.,6.09472152853893,-13.3359375));
#306549=CARTESIAN_POINT('Ctrl Pts',(-1.98029506767702,6.09472152853892,
-13.2484375));
#306550=CARTESIAN_POINT('Ctrl Pts',(-3.58238743130462,4.93073329257085,
-13.1609375));
#306551=CARTESIAN_POINT('Ctrl Pts',(-5.18447979493222,3.76674505660277,
-13.0734375));
#306552=CARTESIAN_POINT('Ctrl Pts',(-5.7964246247213,1.88337252830138,-12.9859375));
#306553=CARTESIAN_POINT('Ctrl Pts',(-6.40836945451038,3.24224545756048E-15,
-12.8984375));
#306554=CARTESIAN_POINT('Ctrl Pts',(-5.7964246247213,-1.88337252830138,
-12.8109375));
#306555=CARTESIAN_POINT('Ctrl Pts',(-5.18447979493222,-3.76674505660276,
-12.7234375));
#306556=CARTESIAN_POINT('Ctrl Pts',(-3.58238743130462,-4.93073329257084,
-12.6359375));
#306557=CARTESIAN_POINT('Ctrl Pts',(-1.98029506767702,-6.09472152853892,
-12.5484375));
#306558=CARTESIAN_POINT('Ctrl Pts',(-7.46388121161966E-16,-6.09472152853892,
-12.4609375));
#306559=CARTESIAN_POINT('Ctrl Pts',(1.98029506767702,-6.09472152853892,
-12.3734375));
#306560=CARTESIAN_POINT('Ctrl Pts',(3.58238743130462,-4.93073329257084,
-12.2859375));
#306561=CARTESIAN_POINT('Ctrl Pts',(5.18447979493222,-3.76674505660277,
-12.1984375));
#306562=CARTESIAN_POINT('Ctrl Pts',(5.7964246247213,-1.88337252830138,-12.1109375));
#306563=CARTESIAN_POINT('Ctrl Pts',(6.40836945451038,1.69997256122249E-15,
-12.0234375));
#306564=CARTESIAN_POINT('Ctrl Pts',(5.7964246247213,1.88337252830138,-11.9359375));
#306565=CARTESIAN_POINT('Ctrl Pts',(5.18447979493222,3.76674505660277,-11.8484375));
#306566=CARTESIAN_POINT('Ctrl Pts',(3.58238743130462,4.93073329257085,-11.7609375));
#306567=CARTESIAN_POINT('Ctrl Pts',(1.98029506767702,6.09472152853892,-11.6734375));
#306568=CARTESIAN_POINT('Ctrl Pts',(0.,6.09472152853893,-11.5859375));
#306569=CARTESIAN_POINT('Ctrl Pts',(-1.98029506767702,6.09472152853892,
-11.4984375));
#306570=CARTESIAN_POINT('Ctrl Pts',(-3.58238743130462,4.93073329257085,
-11.4109375));
#306571=CARTESIAN_POINT('Ctrl Pts',(-5.18447979493222,3.76674505660277,
-11.3234375));
#306572=CARTESIAN_POINT('Ctrl Pts',(-5.7964246247213,1.88337252830138,-11.2359375));
#306573=CARTESIAN_POINT('Ctrl Pts',(-6.40836945451038,3.29689532097243E-15,
-11.1484375));
#306574=CARTESIAN_POINT('Ctrl Pts',(-5.7964246247213,-1.88337252830138,
-11.0609375));
#306575=CARTESIAN_POINT('Ctrl Pts',(-5.18447979493222,-3.76674505660276,
-10.9734375));
#306576=CARTESIAN_POINT('Ctrl Pts',(-3.58238743130462,-4.93073329257084,
-10.8859375));
#306577=CARTESIAN_POINT('Ctrl Pts',(-1.98029506767702,-6.09472152853892,
-10.7984375));
#306578=CARTESIAN_POINT('Ctrl Pts',(-7.46388121161966E-16,-6.09472152853892,
-10.7109375));
#306579=CARTESIAN_POINT('Ctrl Pts',(1.98029506767702,-6.09472152853892,
-10.6234375));
#306580=CARTESIAN_POINT('Ctrl Pts',(3.58238743130462,-4.93073329257084,
-10.5359375));
#306581=CARTESIAN_POINT('Ctrl Pts',(5.18447979493222,-3.76674505660277,
-10.4484375));
#306582=CARTESIAN_POINT('Ctrl Pts',(5.7964246247213,-1.88337252830138,-10.3609375));
#306583=CARTESIAN_POINT('Ctrl Pts',(6.40836945451038,1.75462242463444E-15,
-10.2734375));
#306584=CARTESIAN_POINT('Ctrl Pts',(5.7964246247213,1.88337252830138,-10.1859375));
#306585=CARTESIAN_POINT('Ctrl Pts',(5.18447979493222,3.76674505660277,-10.0984375));
#306586=CARTESIAN_POINT('Ctrl Pts',(3.58238743130462,4.93073329257085,-10.0109375));
#306587=CARTESIAN_POINT('Ctrl Pts',(1.98029506767702,6.09472152853892,-9.9234375));
#306588=CARTESIAN_POINT('Ctrl Pts',(0.,6.09472152853893,-9.8359375));
#306589=CARTESIAN_POINT('Ctrl Pts',(-1.98029506767702,6.09472152853892,
-9.74843749999999));
#306590=CARTESIAN_POINT('Ctrl Pts',(-3.58238743130462,4.93073329257085,
-9.6609375));
#306591=CARTESIAN_POINT('Ctrl Pts',(-5.18447979493222,3.76674505660277,
-9.57343749999999));
#306592=CARTESIAN_POINT('Ctrl Pts',(-5.7964246247213,1.88337252830138,-9.4859375));
#306593=CARTESIAN_POINT('Ctrl Pts',(-6.40836945451038,3.35154518438438E-15,
-9.39843749999999));
#306594=CARTESIAN_POINT('Ctrl Pts',(-5.7964246247213,-1.88337252830138,
-9.3109375));
#306595=CARTESIAN_POINT('Ctrl Pts',(-5.18447979493222,-3.76674505660276,
-9.2234375));
#306596=CARTESIAN_POINT('Ctrl Pts',(-3.58238743130462,-4.93073329257084,
-9.1359375));
#306597=CARTESIAN_POINT('Ctrl Pts',(-1.98029506767702,-6.09472152853892,
-9.0484375));
#306598=CARTESIAN_POINT('Ctrl Pts',(-7.46388121161966E-16,-6.09472152853892,
-8.9609375));
#306599=CARTESIAN_POINT('Ctrl Pts',(1.98029506767702,-6.09472152853892,
-8.8734375));
#306600=CARTESIAN_POINT('Ctrl Pts',(3.58238743130462,-4.93073329257084,
-8.7859375));
#306601=CARTESIAN_POINT('Ctrl Pts',(5.18447979493222,-3.76674505660277,
-8.6984375));
#306602=CARTESIAN_POINT('Ctrl Pts',(5.7964246247213,-1.88337252830138,-8.6109375));
#306603=CARTESIAN_POINT('Ctrl Pts',(6.40836945451038,1.80927228804639E-15,
-8.5234375));
#306604=CARTESIAN_POINT('Ctrl Pts',(5.7964246247213,1.88337252830138,-8.4359375));
#306605=CARTESIAN_POINT('Ctrl Pts',(5.18447979493222,3.76674505660277,-8.34843749999999));
#306606=CARTESIAN_POINT('Ctrl Pts',(3.58238743130462,4.93073329257085,-8.2609375));
#306607=CARTESIAN_POINT('Ctrl Pts',(1.98029506767702,6.09472152853892,-8.1734375));
#306608=CARTESIAN_POINT('Ctrl Pts',(0.,6.09472152853893,-8.0859375));
#306609=CARTESIAN_POINT('Ctrl Pts',(-1.98029506767702,6.09472152853892,
-7.9984375));
#306610=CARTESIAN_POINT('Ctrl Pts',(-3.58238743130462,4.93073329257085,
-7.9109375));
#306611=CARTESIAN_POINT('Ctrl Pts',(-5.18447979493222,3.76674505660277,
-7.8234375));
#306612=CARTESIAN_POINT('Ctrl Pts',(-5.7964246247213,1.88337252830138,-7.7359375));
#306613=CARTESIAN_POINT('Ctrl Pts',(-6.40836945451038,3.40619504779633E-15,
-7.64843749999999));
#306614=CARTESIAN_POINT('Ctrl Pts',(-5.7964246247213,-1.88337252830138,
-7.5609375));
#306615=CARTESIAN_POINT('Ctrl Pts',(-5.18447979493222,-3.76674505660276,
-7.47343749999999));
#306616=CARTESIAN_POINT('Ctrl Pts',(-3.58238743130462,-4.93073329257084,
-7.3859375));
#306617=CARTESIAN_POINT('Ctrl Pts',(-1.98029506767702,-6.09472152853892,
-7.2984375));
#306618=CARTESIAN_POINT('Ctrl Pts',(-7.46388121161966E-16,-6.09472152853892,
-7.2109375));
#306619=CARTESIAN_POINT('Ctrl Pts',(1.98029506767702,-6.09472152853892,
-7.1234375));
#306620=CARTESIAN_POINT('Ctrl Pts',(3.58238743130462,-4.93073329257084,
-7.0359375));
#306621=CARTESIAN_POINT('Ctrl Pts',(5.18447979493222,-3.76674505660277,
-6.9484375));
#306622=CARTESIAN_POINT('Ctrl Pts',(5.7964246247213,-1.88337252830138,-6.8609375));
#306623=CARTESIAN_POINT('Ctrl Pts',(6.40836945451038,1.86392215145835E-15,
-6.7734375));
#306624=CARTESIAN_POINT('Ctrl Pts',(5.7964246247213,1.88337252830138,-6.6859375));
#306625=CARTESIAN_POINT('Ctrl Pts',(5.18447979493222,3.76674505660277,-6.59843749999999));
#306626=CARTESIAN_POINT('Ctrl Pts',(3.58238743130462,4.93073329257085,-6.5109375));
#306627=CARTESIAN_POINT('Ctrl Pts',(1.98029506767702,6.09472152853892,-6.4234375));
#306628=CARTESIAN_POINT('Ctrl Pts',(0.,6.09472152853893,-6.3359375));
#306629=CARTESIAN_POINT('Ctrl Pts',(-1.98029506767702,6.09472152853892,
-6.2484375));
#306630=CARTESIAN_POINT('Ctrl Pts',(-3.58238743130462,4.93073329257085,
-6.1609375));
#306631=CARTESIAN_POINT('Ctrl Pts',(-4.25030673465153,4.4454615134136,-6.12445836785401));
#306632=CARTESIAN_POINT('Ctrl Pts',(-4.76505439612012,3.79998514634624,
-6.08614055662269));
#306633=CARTESIAN_POINT('Ctrl Pts',(6.66133814775094E-15,6.00000000000001,
-8.03125));
#306634=CARTESIAN_POINT('Ctrl Pts',(-0.298350089586693,6.00000000000001,
-8.01785918726406));
#306635=CARTESIAN_POINT('Ctrl Pts',(-0.596925028388715,5.97774819526054,
-8.00413377716093));
#306636=CARTESIAN_POINT('Ctrl Pts',(-1.66924937211483,5.81630856274366,
-7.95365043907342));
#306637=CARTESIAN_POINT('Ctrl Pts',(-2.41486229564473,5.54836098887262,
-7.91627761124828));
#306638=CARTESIAN_POINT('Ctrl Pts',(-3.75967261426721,4.74120264916727,
-7.84414758536147));
#306639=CARTESIAN_POINT('Ctrl Pts',(-4.34613026038862,4.21014287943788,
-7.8089338812994));
#306640=CARTESIAN_POINT('Ctrl Pts',(-5.27616152650459,2.96004444542891,
-7.73540726990233));
#306641=CARTESIAN_POINT('Ctrl Pts',(-5.61376950107607,2.2550567903524,-7.70017212388947));
#306642=CARTESIAN_POINT('Ctrl Pts',(-6.00669408698858,0.739124739792806,
-7.62863126106828));
#306643=CARTESIAN_POINT('Ctrl Pts',(-6.05170607345556,-0.0589509747342593,
-7.59096794681035));
#306644=CARTESIAN_POINT('Ctrl Pts',(-5.83151436888551,-1.61117175748842,
-7.51771452226127));
#306645=CARTESIAN_POINT('Ctrl Pts',(-5.57442451266052,-2.35121606288477,
-7.48361115339666));
#306646=CARTESIAN_POINT('Ctrl Pts',(-4.79076292912546,-3.69551058096904,
-7.4105483376614));
#306647=CARTESIAN_POINT('Ctrl Pts',(-4.27036201929517,-4.28629300582258,
-7.37355698610541));
#306648=CARTESIAN_POINT('Ctrl Pts',(-3.02301551530211,-5.24296670219167,
-7.30243117764194));
#306649=CARTESIAN_POINT('Ctrl Pts',(-2.30522251047422,-5.59584071305071,
-7.26560902624741));
#306650=CARTESIAN_POINT('Ctrl Pts',(-0.792137449271004,-5.99755024079105,
-7.19183913962938));
#306651=CARTESIAN_POINT('Ctrl Pts',(-0.0133123538000254,-6.04962216438536,
-7.1575711534076));
#306652=CARTESIAN_POINT('Ctrl Pts',(1.53424879406655,-5.85360958345414,
-7.08525362770043));
#306653=CARTESIAN_POINT('Ctrl Pts',(2.28757340913091,-5.60229241516888,
-7.04777720365975));
#306654=CARTESIAN_POINT('Ctrl Pts',(3.64967592975576,-4.82599117489345,
-6.97532105322719));
#306655=CARTESIAN_POINT('Ctrl Pts',(4.24636514478383,-4.31030147320438,
-6.94052530193557));
#306656=CARTESIAN_POINT('Ctrl Pts',(5.20498502284638,-3.08375106151128,
-6.86710472233009));
#306657=CARTESIAN_POINT('Ctrl Pts',(5.55955074770865,-2.38593173989502,
-6.8313484606247));
#306658=CARTESIAN_POINT('Ctrl Pts',(5.98838803540964,-0.876802577728364,
-6.7601286441889));
#306659=CARTESIAN_POINT('Ctrl Pts',(6.05172653326255,-0.0780941398890815,
-6.72243547003608));
#306660=CARTESIAN_POINT('Ctrl Pts',(5.86620171282064,1.47928141572156,-6.64893877805449));
#306661=CARTESIAN_POINT('Ctrl Pts',(5.62630539476616,2.22379961680138,-6.61491500177162));
#306662=CARTESIAN_POINT('Ctrl Pts',(4.87340782866889,3.58619747205795,-6.54201437438082));
#306663=CARTESIAN_POINT('Ctrl Pts',(4.36528719811434,4.18989905677479,-6.50487041815271));
#306664=CARTESIAN_POINT('Ctrl Pts',(3.1405741703139,5.17290477810806,-6.43336709522222));
#306665=CARTESIAN_POINT('Ctrl Pts',(2.43405248916498,5.54054391885069,-6.39719769893698));
#306666=CARTESIAN_POINT('Ctrl Pts',(1.13079062593595,5.91984127184233,-6.33317212698165));
#306667=CARTESIAN_POINT('Ctrl Pts',(0.566258670473045,6.00000000000003,
-6.30666532274017));
#306668=CARTESIAN_POINT('Ctrl Pts',(-2.35089725464377E-13,6.00000000000001,
-6.28124999999999));
#306669=CARTESIAN_POINT('Ctrl Pts',(-0.683563368987388,5.96093458449081,
-6.24999999999999));
#306670=CARTESIAN_POINT('Ctrl Pts',(-0.0383159840272598,6.02151021407911,
-6.2722728378837));
#306671=CARTESIAN_POINT('Ctrl Pts',(0.613802036334531,5.97768570738805,
-6.29369507965025));
#306672=CARTESIAN_POINT('Ctrl Pts',(1.86095346059866,5.68339189538494,-6.33868681212296));
#306673=CARTESIAN_POINT('Ctrl Pts',(2.44827655643883,5.44153698589087,-6.36115046126864));
#306674=CARTESIAN_POINT('Ctrl Pts',(3.31527595182957,4.91053707074575,-6.3964523351205));
#306675=CARTESIAN_POINT('Ctrl Pts',(3.62530031161791,4.67669984037455,-6.40939585433822));
#306676=CARTESIAN_POINT('Ctrl Pts',(4.46934833248225,3.89702715050554,-6.44942871893781));
#306677=CARTESIAN_POINT('Ctrl Pts',(4.92290194524358,3.27617829245186,-6.47696465561948));
#306678=CARTESIAN_POINT('Ctrl Pts',(5.40410302848904,2.24559647875469,-6.517292807541));
#306679=CARTESIAN_POINT('Ctrl Pts',(5.53060158549463,1.88938934315057,-6.53018354451336));
#306680=CARTESIAN_POINT('Ctrl Pts',(5.74574294589262,1.02496405516718,-6.56123991687386));
#306681=CARTESIAN_POINT('Ctrl Pts',(5.80264385515304,0.512322540210554,
-6.57975809488675));
#306682=CARTESIAN_POINT('Ctrl Pts',(5.79150251002447,-4.08715104815993E-8,
-6.59837392003554));
#306683=CARTESIAN_POINT('Origin',(-3.81730450148946E-15,-2.22044604925031E-15,
-37.015625));
#306684=CARTESIAN_POINT('Origin',(0.,0.,36.25));
#306685=CARTESIAN_POINT('',(-1.53209212662338,6.06688311688312,36.25));
#306686=CARTESIAN_POINT('',(-2.04107142857143,5.43420251623377,36.25));
#306687=CARTESIAN_POINT('Ctrl Pts',(-1.53209212662338,6.06688311688312,
36.25));
#306688=CARTESIAN_POINT('Ctrl Pts',(-1.54951650473831,6.066434027441,36.25));
#306689=CARTESIAN_POINT('Ctrl Pts',(-1.58393065600793,6.06554704990339,
36.25));
#306690=CARTESIAN_POINT('Ctrl Pts',(-1.63443083923324,6.05712286492333,
36.25));
#306691=CARTESIAN_POINT('Ctrl Pts',(-1.68245238910184,6.04224031339717,
36.25));
#306692=CARTESIAN_POINT('Ctrl Pts',(-1.72937966613072,6.02430730620351,
36.25));
#306693=CARTESIAN_POINT('Ctrl Pts',(-1.77322121904902,5.9981366813217,36.25));
#306694=CARTESIAN_POINT('Ctrl Pts',(-1.81610239307926,5.96827285277195,
36.25));
#306695=CARTESIAN_POINT('Ctrl Pts',(-1.85592360031061,5.93155196527191,
36.25));
#306696=CARTESIAN_POINT('Ctrl Pts',(-1.89389884878363,5.89060348709459,
36.25));
#306697=CARTESIAN_POINT('Ctrl Pts',(-1.92842298904565,5.84507968533497,
36.25));
#306698=CARTESIAN_POINT('Ctrl Pts',(-1.95895617838667,5.79605922055842,
36.25));
#306699=CARTESIAN_POINT('Ctrl Pts',(-1.98409150523322,5.74343345049149,
36.25));
#306700=CARTESIAN_POINT('Ctrl Pts',(-2.00454652849223,5.68767671276928,
36.25));
#306701=CARTESIAN_POINT('Ctrl Pts',(-2.02161548775311,5.6290296721576,36.25));
#306702=CARTESIAN_POINT('Ctrl Pts',(-2.03309476195626,5.56687880407454,
36.25));
#306703=CARTESIAN_POINT('Ctrl Pts',(-2.03932413346711,5.50155035955671,
36.25));
#306704=CARTESIAN_POINT('Ctrl Pts',(-2.04048048892973,5.45697972788144,
36.25));
#306705=CARTESIAN_POINT('Ctrl Pts',(-2.04107142857143,5.43420251623377,
36.25));
#306706=CARTESIAN_POINT('',(-1.52371651785714,4.78863636363636,36.25));
#306707=CARTESIAN_POINT('Ctrl Pts',(-2.04107142857143,5.43420251623377,
36.25));
#306708=CARTESIAN_POINT('Ctrl Pts',(-2.0405543266768,5.41055942108448,36.25));
#306709=CARTESIAN_POINT('Ctrl Pts',(-2.03954125408768,5.36423939815085,
36.25));
#306710=CARTESIAN_POINT('Ctrl Pts',(-2.03228105709878,5.2966367303295,36.25));
#306711=CARTESIAN_POINT('Ctrl Pts',(-2.02107341871046,5.23250639408275,
36.25));
#306712=CARTESIAN_POINT('Ctrl Pts',(-2.00398348773993,5.17226185872411,
36.25));
#306713=CARTESIAN_POINT('Ctrl Pts',(-1.98289443792092,5.11515155101266,
36.25));
#306714=CARTESIAN_POINT('Ctrl Pts',(-1.95643257885054,5.06166487648077,
36.25));
#306715=CARTESIAN_POINT('Ctrl Pts',(-1.92516888970118,5.0117585395718,36.25));
#306716=CARTESIAN_POINT('Ctrl Pts',(-1.89024117171633,4.96538056994282,
36.25));
#306717=CARTESIAN_POINT('Ctrl Pts',(-1.85077488100797,4.9247537203412,36.25));
#306718=CARTESIAN_POINT('Ctrl Pts',(-1.81007783686995,4.8879898300525,36.25));
#306719=CARTESIAN_POINT('Ctrl Pts',(-1.76718752939314,4.85710381362087,
36.25));
#306720=CARTESIAN_POINT('Ctrl Pts',(-1.72190013812572,4.83218747720399,
36.25));
#306721=CARTESIAN_POINT('Ctrl Pts',(-1.67490398148407,4.81303741070313,
36.25));
#306722=CARTESIAN_POINT('Ctrl Pts',(-1.62621370039499,4.79855444913016,
36.25));
#306723=CARTESIAN_POINT('Ctrl Pts',(-1.57556683534013,4.78994040169141,
36.25));
#306724=CARTESIAN_POINT('Ctrl Pts',(-1.54114485828132,4.789074687262,36.25));
#306725=CARTESIAN_POINT('Ctrl Pts',(-1.52371651785714,4.78863636363636,
36.25));
#306726=CARTESIAN_POINT('',(-1.01022727272727,5.42131696428571,36.25));
#306727=CARTESIAN_POINT('Ctrl Pts',(-1.52371651785714,4.78863636363636,
36.25));
#306728=CARTESIAN_POINT('Ctrl Pts',(-1.50606613811182,4.78904075129562,
36.25));
#306729=CARTESIAN_POINT('Ctrl Pts',(-1.4714149990235,4.78983464316812,36.25));
#306730=CARTESIAN_POINT('Ctrl Pts',(-1.42050302431008,4.79884546139153,
36.25));
#306731=CARTESIAN_POINT('Ctrl Pts',(-1.37159611734391,4.81206099883602,
36.25));
#306732=CARTESIAN_POINT('Ctrl Pts',(-1.32477571753144,4.83107657862712,
36.25));
#306733=CARTESIAN_POINT('Ctrl Pts',(-1.27989304559387,4.85499849822356,
36.25));
#306734=CARTESIAN_POINT('Ctrl Pts',(-1.23739271777899,4.88475706229418,
36.25));
#306735=CARTESIAN_POINT('Ctrl Pts',(-1.19710037531277,4.92023184841449,
36.25));
#306736=CARTESIAN_POINT('Ctrl Pts',(-1.15864753037992,4.96016808484432,
36.25));
#306737=CARTESIAN_POINT('Ctrl Pts',(-1.12433596830973,5.00550562421531,
36.25));
#306738=CARTESIAN_POINT('Ctrl Pts',(-1.09262300577192,5.05353436556821,
36.25));
#306739=CARTESIAN_POINT('Ctrl Pts',(-1.0681718193395,5.10649857927001,36.25));
#306740=CARTESIAN_POINT('Ctrl Pts',(-1.04618243948374,5.16193679017606,
36.25));
#306741=CARTESIAN_POINT('Ctrl Pts',(-1.03075200559165,5.22177284922642,
36.25));
#306742=CARTESIAN_POINT('Ctrl Pts',(-1.0178443165815,5.28488392294487,36.25));
#306743=CARTESIAN_POINT('Ctrl Pts',(-1.01206974131962,5.35205975094169,
36.25));
#306744=CARTESIAN_POINT('Ctrl Pts',(-1.01085017356999,5.39790252089427,
36.25));
#306745=CARTESIAN_POINT('Ctrl Pts',(-1.01022727272727,5.42131696428571,
36.25));
#306746=CARTESIAN_POINT('Ctrl Pts',(-1.01022727272727,5.42131696428571,
36.25));
#306747=CARTESIAN_POINT('Ctrl Pts',(-1.01076599462072,5.44495600403826,
36.25));
#306748=CARTESIAN_POINT('Ctrl Pts',(-1.0118214237133,5.49126808190085,36.25));
#306749=CARTESIAN_POINT('Ctrl Pts',(-1.01878267475616,5.55896687878814,
36.25));
#306750=CARTESIAN_POINT('Ctrl Pts',(-1.03107800379365,5.62293356367208,
36.25));
#306751=CARTESIAN_POINT('Ctrl Pts',(-1.04789745408079,5.68327106051297,
36.25));
#306752=CARTESIAN_POINT('Ctrl Pts',(-1.06908652243424,5.74035420483588,
36.25));
#306753=CARTESIAN_POINT('Ctrl Pts',(-1.09547159489994,5.79399835274014,
36.25));
#306754=CARTESIAN_POINT('Ctrl Pts',(-1.12719592427129,5.8437725973715,36.25));
#306755=CARTESIAN_POINT('Ctrl Pts',(-1.1634661665603,5.88934000071629,36.25));
#306756=CARTESIAN_POINT('Ctrl Pts',(-1.20222138279797,5.93098943621083,
36.25));
#306757=CARTESIAN_POINT('Ctrl Pts',(-1.24358478999076,5.96739207884556,
36.25));
#306758=CARTESIAN_POINT('Ctrl Pts',(-1.28715520747738,5.99780008387924,
36.25));
#306759=CARTESIAN_POINT('Ctrl Pts',(-1.33229168731682,6.02332207855003,
36.25));
#306760=CARTESIAN_POINT('Ctrl Pts',(-1.37963229428386,6.04244867323907,
36.25));
#306761=CARTESIAN_POINT('Ctrl Pts',(-1.42850133450328,6.05706063884487,
36.25));
#306762=CARTESIAN_POINT('Ctrl Pts',(-1.47960608156579,6.0655628055813,36.25));
#306763=CARTESIAN_POINT('Ctrl Pts',(-1.51445101604866,6.06643934639816,
36.25));
#306764=CARTESIAN_POINT('Ctrl Pts',(-1.53209212662338,6.06688311688312,
36.25));
#306765=CARTESIAN_POINT('Origin',(0.,0.,36.25));
#306766=CARTESIAN_POINT('',(-1.52758218344156,7.38636363636364,36.25));
#306767=CARTESIAN_POINT('',(-1.91737012987013,6.90444399350649,36.25));
#306768=CARTESIAN_POINT('Ctrl Pts',(-1.52758218344156,7.38636363636364,
36.25));
#306769=CARTESIAN_POINT('Ctrl Pts',(-1.55358237022155,7.38486930154146,
36.25));
#306770=CARTESIAN_POINT('Ctrl Pts',(-1.60499794902611,7.38191424239284,
36.25));
#306771=CARTESIAN_POINT('Ctrl Pts',(-1.67863965341545,7.354443366284,36.25));
#306772=CARTESIAN_POINT('Ctrl Pts',(-1.74575926016136,7.30974046602882,
36.25));
#306773=CARTESIAN_POINT('Ctrl Pts',(-1.80513211335571,7.24931351323173,
36.25));
#306774=CARTESIAN_POINT('Ctrl Pts',(-1.85584586752056,7.17700242184242,
36.25));
#306775=CARTESIAN_POINT('Ctrl Pts',(-1.8909492802511,7.09344714231162,36.25));
#306776=CARTESIAN_POINT('Ctrl Pts',(-1.91396932214169,7.00188822714751,
36.25));
#306777=CARTESIAN_POINT('Ctrl Pts',(-1.91621068652427,6.93766582705582,
36.25));
#306778=CARTESIAN_POINT('Ctrl Pts',(-1.91737012987013,6.90444399350649,
36.25));
#306779=CARTESIAN_POINT('',(-1.52371651785714,6.39675324675325,36.25));
#306780=CARTESIAN_POINT('Ctrl Pts',(-1.91737012987013,6.90444399350649,
36.25));
#306781=CARTESIAN_POINT('Ctrl Pts',(-1.91613148952843,6.8676136615146,36.25));
#306782=CARTESIAN_POINT('Ctrl Pts',(-1.91376144516393,6.79714161418861,
36.25));
#306783=CARTESIAN_POINT('Ctrl Pts',(-1.89249074922576,6.69694686802566,
36.25));
#306784=CARTESIAN_POINT('Ctrl Pts',(-1.85626188657584,6.60868448959127,
36.25));
#306785=CARTESIAN_POINT('Ctrl Pts',(-1.80667059916436,6.53319043392833,
36.25));
#306786=CARTESIAN_POINT('Ctrl Pts',(-1.74600279585425,6.47327605218271,
36.25));
#306787=CARTESIAN_POINT('Ctrl Pts',(-1.67833795046176,6.42829274914181,
36.25));
#306788=CARTESIAN_POINT('Ctrl Pts',(-1.60297996097691,6.4012532984509,36.25));
#306789=CARTESIAN_POINT('Ctrl Pts',(-1.5503437032771,6.39826496143831,36.25));
#306790=CARTESIAN_POINT('Ctrl Pts',(-1.52371651785714,6.39675324675325,
36.25));
#306791=CARTESIAN_POINT('',(-1.13392857142857,6.88318283279221,36.25));
#306792=CARTESIAN_POINT('Ctrl Pts',(-1.52371651785714,6.39675324675325,
36.25));
#306793=CARTESIAN_POINT('Ctrl Pts',(-1.49749406178753,6.39823178023093,
36.25));
#306794=CARTESIAN_POINT('Ctrl Pts',(-1.44564553849367,6.40115522024948,
36.25));
#306795=CARTESIAN_POINT('Ctrl Pts',(-1.37190501458764,6.42869442089,36.25));
#306796=CARTESIAN_POINT('Ctrl Pts',(-1.30436731865975,6.47176243493413,
36.25));
#306797=CARTESIAN_POINT('Ctrl Pts',(-1.24507578007146,6.5313545752525,36.25));
#306798=CARTESIAN_POINT('Ctrl Pts',(-1.19545427309708,6.60421240376617,
36.25));
#306799=CARTESIAN_POINT('Ctrl Pts',(-1.15909489053248,6.68851996626879,
36.25));
#306800=CARTESIAN_POINT('Ctrl Pts',(-1.13760625764887,6.78290098418177,
36.25));
#306801=CARTESIAN_POINT('Ctrl Pts',(-1.13518507442834,6.84892095288905,
36.25));
#306802=CARTESIAN_POINT('Ctrl Pts',(-1.13392857142857,6.88318283279221,
36.25));
#306803=CARTESIAN_POINT('Ctrl Pts',(-1.13392857142857,6.88318283279221,
36.25));
#306804=CARTESIAN_POINT('Ctrl Pts',(-1.13513622427257,6.91852455417192,
36.25));
#306805=CARTESIAN_POINT('Ctrl Pts',(-1.13746675383528,6.98672704040914,
36.25));
#306806=CARTESIAN_POINT('Ctrl Pts',(-1.15960212713315,7.08387655284218,
36.25));
#306807=CARTESIAN_POINT('Ctrl Pts',(-1.1967070851926,7.17101343023865,36.25));
#306808=CARTESIAN_POINT('Ctrl Pts',(-1.248366652071,7.24570928090529,36.25));
#306809=CARTESIAN_POINT('Ctrl Pts',(-1.30855629123278,7.30781082924543,
36.25));
#306810=CARTESIAN_POINT('Ctrl Pts',(-1.3763696724576,7.35293658272662,36.25));
#306811=CARTESIAN_POINT('Ctrl Pts',(-1.45006627196568,7.38129222806274,
36.25));
#306812=CARTESIAN_POINT('Ctrl Pts',(-1.50156524889417,7.38466150198483,
36.25));
#306813=CARTESIAN_POINT('Ctrl Pts',(-1.52758218344156,7.38636363636364,
36.25));
#306814=CARTESIAN_POINT('Origin',(0.,0.,36.25));
#306815=CARTESIAN_POINT('',(1.51920657467533,6.06688311688312,36.25));
#306816=CARTESIAN_POINT('',(1.01022727272727,5.43420251623377,36.25));
#306817=CARTESIAN_POINT('Ctrl Pts',(1.51920657467533,6.06688311688312,36.25));
#306818=CARTESIAN_POINT('Ctrl Pts',(1.5017821965604,6.066434027441,36.25));
#306819=CARTESIAN_POINT('Ctrl Pts',(1.46736804529077,6.06554704990339,36.25));
#306820=CARTESIAN_POINT('Ctrl Pts',(1.41686786206546,6.05712286492333,36.25));
#306821=CARTESIAN_POINT('Ctrl Pts',(1.36884631219687,6.04224031339717,36.25));
#306822=CARTESIAN_POINT('Ctrl Pts',(1.32191903516798,6.02430730620351,36.25));
#306823=CARTESIAN_POINT('Ctrl Pts',(1.27807748224968,5.99813668132169,36.25));
#306824=CARTESIAN_POINT('Ctrl Pts',(1.23519630821944,5.96827285277196,36.25));
#306825=CARTESIAN_POINT('Ctrl Pts',(1.19537510098809,5.93155196527191,36.25));
#306826=CARTESIAN_POINT('Ctrl Pts',(1.15739985251507,5.89060348709459,36.25));
#306827=CARTESIAN_POINT('Ctrl Pts',(1.12287571225305,5.84507968533496,36.25));
#306828=CARTESIAN_POINT('Ctrl Pts',(1.09234252291203,5.79605922055842,36.25));
#306829=CARTESIAN_POINT('Ctrl Pts',(1.06720719606548,5.74343345049149,36.25));
#306830=CARTESIAN_POINT('Ctrl Pts',(1.04675217280647,5.68767671276929,36.25));
#306831=CARTESIAN_POINT('Ctrl Pts',(1.02968321354559,5.6290296721576,36.25));
#306832=CARTESIAN_POINT('Ctrl Pts',(1.01820393934243,5.56687880407454,36.25));
#306833=CARTESIAN_POINT('Ctrl Pts',(1.01197456783159,5.50155035955671,36.25));
#306834=CARTESIAN_POINT('Ctrl Pts',(1.01081821236896,5.45697972788144,36.25));
#306835=CARTESIAN_POINT('Ctrl Pts',(1.01022727272727,5.43420251623377,36.25));
#306836=CARTESIAN_POINT('',(1.52758218344156,4.78863636363636,36.25));
#306837=CARTESIAN_POINT('Ctrl Pts',(1.01022727272727,5.43420251623377,36.25));
#306838=CARTESIAN_POINT('Ctrl Pts',(1.01074437462189,5.41055942108448,36.25));
#306839=CARTESIAN_POINT('Ctrl Pts',(1.01175744721102,5.36423939815086,36.25));
#306840=CARTESIAN_POINT('Ctrl Pts',(1.01901764419993,5.2966367303295,36.25));
#306841=CARTESIAN_POINT('Ctrl Pts',(1.03022528258824,5.23250639408275,36.25));
#306842=CARTESIAN_POINT('Ctrl Pts',(1.04731521355877,5.17226185872411,36.25));
#306843=CARTESIAN_POINT('Ctrl Pts',(1.06840426337778,5.11515155101266,36.25));
#306844=CARTESIAN_POINT('Ctrl Pts',(1.09486612244816,5.06166487648077,36.25));
#306845=CARTESIAN_POINT('Ctrl Pts',(1.12612981159753,5.0117585395718,36.25));
#306846=CARTESIAN_POINT('Ctrl Pts',(1.16105752958236,4.96538056994282,36.25));
#306847=CARTESIAN_POINT('Ctrl Pts',(1.20052382029073,4.9247537203412,36.25));
#306848=CARTESIAN_POINT('Ctrl Pts',(1.24122086442875,4.88798983005251,36.25));
#306849=CARTESIAN_POINT('Ctrl Pts',(1.28411117190556,4.85710381362087,36.25));
#306850=CARTESIAN_POINT('Ctrl Pts',(1.32939856317298,4.83218747720399,36.25));
#306851=CARTESIAN_POINT('Ctrl Pts',(1.37639471981463,4.81303741070312,36.25));
#306852=CARTESIAN_POINT('Ctrl Pts',(1.42508500090371,4.79855444913016,36.25));
#306853=CARTESIAN_POINT('Ctrl Pts',(1.47573186595857,4.78994040169141,36.25));
#306854=CARTESIAN_POINT('Ctrl Pts',(1.51015384301738,4.789074687262,36.25));
#306855=CARTESIAN_POINT('Ctrl Pts',(1.52758218344156,4.78863636363636,36.25));
#306856=CARTESIAN_POINT('',(2.04107142857143,5.42131696428571,36.25));
#306857=CARTESIAN_POINT('Ctrl Pts',(1.52758218344156,4.78863636363636,36.25));
#306858=CARTESIAN_POINT('Ctrl Pts',(1.54523256318688,4.78904075129562,36.25));
#306859=CARTESIAN_POINT('Ctrl Pts',(1.5798837022752,4.78983464316812,36.25));
#306860=CARTESIAN_POINT('Ctrl Pts',(1.63079567698862,4.79884546139153,36.25));
#306861=CARTESIAN_POINT('Ctrl Pts',(1.67970258395479,4.81206099883602,36.25));
#306862=CARTESIAN_POINT('Ctrl Pts',(1.72652298376726,4.83107657862712,36.25));
#306863=CARTESIAN_POINT('Ctrl Pts',(1.77140565570483,4.85499849822356,36.25));
#306864=CARTESIAN_POINT('Ctrl Pts',(1.81390598351971,4.88475706229418,36.25));
#306865=CARTESIAN_POINT('Ctrl Pts',(1.85419832598593,4.92023184841449,36.25));
#306866=CARTESIAN_POINT('Ctrl Pts',(1.89265117091878,4.96016808484432,36.25));
#306867=CARTESIAN_POINT('Ctrl Pts',(1.92696273298897,5.00550562421531,36.25));
#306868=CARTESIAN_POINT('Ctrl Pts',(1.95867569552678,5.05353436556821,36.25));
#306869=CARTESIAN_POINT('Ctrl Pts',(1.9831268819592,5.10649857927001,36.25));
#306870=CARTESIAN_POINT('Ctrl Pts',(2.00511626181496,5.16193679017606,36.25));
#306871=CARTESIAN_POINT('Ctrl Pts',(2.02054669570705,5.22177284922642,36.25));
#306872=CARTESIAN_POINT('Ctrl Pts',(2.0334543847172,5.28488392294487,36.25));
#306873=CARTESIAN_POINT('Ctrl Pts',(2.03922895997908,5.35205975094169,36.25));
#306874=CARTESIAN_POINT('Ctrl Pts',(2.04044852772871,5.39790252089427,36.25));
#306875=CARTESIAN_POINT('Ctrl Pts',(2.04107142857143,5.42131696428571,36.25));
#306876=CARTESIAN_POINT('Ctrl Pts',(2.04107142857143,5.42131696428571,36.25));
#306877=CARTESIAN_POINT('Ctrl Pts',(2.04053270667799,5.44495600403826,36.25));
#306878=CARTESIAN_POINT('Ctrl Pts',(2.0394772775854,5.49126808190085,36.25));
#306879=CARTESIAN_POINT('Ctrl Pts',(2.03251602654254,5.55896687878814,36.25));
#306880=CARTESIAN_POINT('Ctrl Pts',(2.02022069750506,5.62293356367208,36.25));
#306881=CARTESIAN_POINT('Ctrl Pts',(2.00340124721791,5.68327106051297,36.25));
#306882=CARTESIAN_POINT('Ctrl Pts',(1.98221217886446,5.74035420483588,36.25));
#306883=CARTESIAN_POINT('Ctrl Pts',(1.95582710639876,5.79399835274014,36.25));
#306884=CARTESIAN_POINT('Ctrl Pts',(1.92410277702741,5.84377259737151,36.25));
#306885=CARTESIAN_POINT('Ctrl Pts',(1.88783253473841,5.88934000071629,36.25));
#306886=CARTESIAN_POINT('Ctrl Pts',(1.84907731850073,5.93098943621083,36.25));
#306887=CARTESIAN_POINT('Ctrl Pts',(1.80771391130794,5.96739207884556,36.25));
#306888=CARTESIAN_POINT('Ctrl Pts',(1.76414349382133,5.99780008387924,36.25));
#306889=CARTESIAN_POINT('Ctrl Pts',(1.71900701398188,6.02332207855003,36.25));
#306890=CARTESIAN_POINT('Ctrl Pts',(1.67166640701484,6.04244867323907,36.25));
#306891=CARTESIAN_POINT('Ctrl Pts',(1.62279736679542,6.05706063884487,36.25));
#306892=CARTESIAN_POINT('Ctrl Pts',(1.57169261973291,6.0655628055813,36.25));
#306893=CARTESIAN_POINT('Ctrl Pts',(1.53684768525004,6.06643934639816,36.25));
#306894=CARTESIAN_POINT('Ctrl Pts',(1.51920657467533,6.06688311688312,36.25));
#306895=CARTESIAN_POINT('Origin',(0.,0.,36.25));
#306896=CARTESIAN_POINT('',(1.52371651785715,7.38636363636364,36.25));
#306897=CARTESIAN_POINT('',(1.13392857142857,6.90444399350649,36.25));
#306898=CARTESIAN_POINT('Ctrl Pts',(1.52371651785715,7.38636363636364,36.25));
#306899=CARTESIAN_POINT('Ctrl Pts',(1.49771633107715,7.38486930154146,36.25));
#306900=CARTESIAN_POINT('Ctrl Pts',(1.4463007522726,7.38191424239284,36.25));
#306901=CARTESIAN_POINT('Ctrl Pts',(1.37265904788325,7.354443366284,36.25));
#306902=CARTESIAN_POINT('Ctrl Pts',(1.30553944113734,7.30974046602882,36.25));
#306903=CARTESIAN_POINT('Ctrl Pts',(1.246166587943,7.24931351323173,36.25));
#306904=CARTESIAN_POINT('Ctrl Pts',(1.19545283377814,7.17700242184241,36.25));
#306905=CARTESIAN_POINT('Ctrl Pts',(1.16034942104761,7.09344714231162,36.25));
#306906=CARTESIAN_POINT('Ctrl Pts',(1.13732937915702,7.0018882271475,36.25));
#306907=CARTESIAN_POINT('Ctrl Pts',(1.13508801477443,6.93766582705582,36.25));
#306908=CARTESIAN_POINT('Ctrl Pts',(1.13392857142857,6.90444399350649,36.25));
#306909=CARTESIAN_POINT('',(1.52758218344156,6.39675324675325,36.25));
#306910=CARTESIAN_POINT('Ctrl Pts',(1.13392857142857,6.90444399350649,36.25));
#306911=CARTESIAN_POINT('Ctrl Pts',(1.13516721177027,6.8676136615146,36.25));
#306912=CARTESIAN_POINT('Ctrl Pts',(1.13753725613477,6.79714161418862,36.25));
#306913=CARTESIAN_POINT('Ctrl Pts',(1.15880795207294,6.69694686802566,36.25));
#306914=CARTESIAN_POINT('Ctrl Pts',(1.19503681472287,6.60868448959127,36.25));
#306915=CARTESIAN_POINT('Ctrl Pts',(1.24462810213434,6.53319043392833,36.25));
#306916=CARTESIAN_POINT('Ctrl Pts',(1.30529590544445,6.47327605218271,36.25));
#306917=CARTESIAN_POINT('Ctrl Pts',(1.37296075083694,6.42829274914181,36.25));
#306918=CARTESIAN_POINT('Ctrl Pts',(1.44831874032179,6.4012532984509,36.25));
#306919=CARTESIAN_POINT('Ctrl Pts',(1.50095499802161,6.39826496143831,36.25));
#306920=CARTESIAN_POINT('Ctrl Pts',(1.52758218344156,6.39675324675325,36.25));
#306921=CARTESIAN_POINT('',(1.91737012987013,6.88318283279221,36.25));
#306922=CARTESIAN_POINT('Ctrl Pts',(1.52758218344156,6.39675324675325,36.25));
#306923=CARTESIAN_POINT('Ctrl Pts',(1.55380463951118,6.39823178023093,36.25));
#306924=CARTESIAN_POINT('Ctrl Pts',(1.60565316280503,6.40115522024948,36.25));
#306925=CARTESIAN_POINT('Ctrl Pts',(1.67939368671106,6.42869442089,36.25));
#306926=CARTESIAN_POINT('Ctrl Pts',(1.74693138263896,6.47176243493413,36.25));
#306927=CARTESIAN_POINT('Ctrl Pts',(1.80622292122723,6.5313545752525,36.25));
#306928=CARTESIAN_POINT('Ctrl Pts',(1.85584442820162,6.60421240376617,36.25));
#306929=CARTESIAN_POINT('Ctrl Pts',(1.89220381076623,6.68851996626879,36.25));
#306930=CARTESIAN_POINT('Ctrl Pts',(1.91369244364984,6.78290098418177,36.25));
#306931=CARTESIAN_POINT('Ctrl Pts',(1.91611362687036,6.84892095288905,36.25));
#306932=CARTESIAN_POINT('Ctrl Pts',(1.91737012987013,6.88318283279221,36.25));
#306933=CARTESIAN_POINT('Ctrl Pts',(1.91737012987013,6.88318283279221,36.25));
#306934=CARTESIAN_POINT('Ctrl Pts',(1.91616247702613,6.91852455417192,36.25));
#306935=CARTESIAN_POINT('Ctrl Pts',(1.91383194746342,6.98672704040914,36.25));
#306936=CARTESIAN_POINT('Ctrl Pts',(1.89169657416555,7.08387655284218,36.25));
#306937=CARTESIAN_POINT('Ctrl Pts',(1.8545916161061,7.17101343023865,36.25));
#306938=CARTESIAN_POINT('Ctrl Pts',(1.80293204922771,7.24570928090529,36.25));
#306939=CARTESIAN_POINT('Ctrl Pts',(1.74274241006592,7.30781082924543,36.25));
#306940=CARTESIAN_POINT('Ctrl Pts',(1.6749290288411,7.35293658272662,36.25));
#306941=CARTESIAN_POINT('Ctrl Pts',(1.60123242933302,7.38129222806274,36.25));
#306942=CARTESIAN_POINT('Ctrl Pts',(1.54973345240453,7.38466150198483,36.25));
#306943=CARTESIAN_POINT('Ctrl Pts',(1.52371651785715,7.38636363636364,36.25));
#306944=CARTESIAN_POINT('Ctrl Pts',(-1.52371651785714,4.78863636363636,
36.05));
#306945=CARTESIAN_POINT('Ctrl Pts',(-1.52371651785714,4.78863636363636,
36.29));
#306946=CARTESIAN_POINT('Ctrl Pts',(-1.50606613811182,4.78904075129562,
36.05));
#306947=CARTESIAN_POINT('Ctrl Pts',(-1.50606613811182,4.78904075129562,
36.29));
#306948=CARTESIAN_POINT('Ctrl Pts',(-1.4714149990235,4.78983464316812,36.05));
#306949=CARTESIAN_POINT('Ctrl Pts',(-1.4714149990235,4.78983464316812,36.29));
#306950=CARTESIAN_POINT('Ctrl Pts',(-1.42050302431008,4.79884546139153,
36.05));
#306951=CARTESIAN_POINT('Ctrl Pts',(-1.42050302431008,4.79884546139153,
36.29));
#306952=CARTESIAN_POINT('Ctrl Pts',(-1.37159611734391,4.81206099883602,
36.05));
#306953=CARTESIAN_POINT('Ctrl Pts',(-1.37159611734391,4.81206099883602,
36.29));
#306954=CARTESIAN_POINT('Ctrl Pts',(-1.32477571753144,4.83107657862712,
36.05));
#306955=CARTESIAN_POINT('Ctrl Pts',(-1.32477571753144,4.83107657862712,
36.29));
#306956=CARTESIAN_POINT('Ctrl Pts',(-1.27989304559387,4.85499849822356,
36.05));
#306957=CARTESIAN_POINT('Ctrl Pts',(-1.27989304559387,4.85499849822356,
36.29));
#306958=CARTESIAN_POINT('Ctrl Pts',(-1.23739271777899,4.88475706229418,
36.05));
#306959=CARTESIAN_POINT('Ctrl Pts',(-1.23739271777899,4.88475706229418,
36.29));
#306960=CARTESIAN_POINT('Ctrl Pts',(-1.19710037531277,4.92023184841449,
36.05));
#306961=CARTESIAN_POINT('Ctrl Pts',(-1.19710037531277,4.92023184841449,
36.29));
#306962=CARTESIAN_POINT('Ctrl Pts',(-1.15864753037992,4.96016808484432,
36.05));
#306963=CARTESIAN_POINT('Ctrl Pts',(-1.15864753037992,4.96016808484432,
36.29));
#306964=CARTESIAN_POINT('Ctrl Pts',(-1.12433596830973,5.00550562421531,
36.05));
#306965=CARTESIAN_POINT('Ctrl Pts',(-1.12433596830973,5.00550562421531,
36.29));
#306966=CARTESIAN_POINT('Ctrl Pts',(-1.09262300577192,5.05353436556821,
36.05));
#306967=CARTESIAN_POINT('Ctrl Pts',(-1.09262300577192,5.05353436556821,
36.29));
#306968=CARTESIAN_POINT('Ctrl Pts',(-1.0681718193395,5.10649857927001,36.05));
#306969=CARTESIAN_POINT('Ctrl Pts',(-1.0681718193395,5.10649857927001,36.29));
#306970=CARTESIAN_POINT('Ctrl Pts',(-1.04618243948374,5.16193679017606,
36.05));
#306971=CARTESIAN_POINT('Ctrl Pts',(-1.04618243948374,5.16193679017606,
36.29));
#306972=CARTESIAN_POINT('Ctrl Pts',(-1.03075200559165,5.22177284922642,
36.05));
#306973=CARTESIAN_POINT('Ctrl Pts',(-1.03075200559165,5.22177284922642,
36.29));
#306974=CARTESIAN_POINT('Ctrl Pts',(-1.0178443165815,5.28488392294487,36.05));
#306975=CARTESIAN_POINT('Ctrl Pts',(-1.0178443165815,5.28488392294487,36.29));
#306976=CARTESIAN_POINT('Ctrl Pts',(-1.01206974131962,5.35205975094169,
36.05));
#306977=CARTESIAN_POINT('Ctrl Pts',(-1.01206974131962,5.35205975094169,
36.29));
#306978=CARTESIAN_POINT('Ctrl Pts',(-1.01085017356999,5.39790252089427,
36.05));
#306979=CARTESIAN_POINT('Ctrl Pts',(-1.01085017356999,5.39790252089427,
36.29));
#306980=CARTESIAN_POINT('Ctrl Pts',(-1.01022727272727,5.42131696428571,
36.05));
#306981=CARTESIAN_POINT('Ctrl Pts',(-1.01022727272727,5.42131696428571,
36.29));
#306982=CARTESIAN_POINT('',(-1.52371651785714,4.78863636363636,36.05));
#306983=CARTESIAN_POINT('',(-1.52371651785714,4.78863636363636,32.1799631621335));
#306984=CARTESIAN_POINT('',(-1.01022727272727,5.42131696428571,36.05));
#306985=CARTESIAN_POINT('Ctrl Pts',(-1.01022727272727,5.42131696428571,
36.05));
#306986=CARTESIAN_POINT('Ctrl Pts',(-1.01085017356999,5.39790252089427,
36.05));
#306987=CARTESIAN_POINT('Ctrl Pts',(-1.01206974131962,5.35205975094169,
36.05));
#306988=CARTESIAN_POINT('Ctrl Pts',(-1.0178443165815,5.28488392294487,36.05));
#306989=CARTESIAN_POINT('Ctrl Pts',(-1.03075200559165,5.22177284922642,
36.05));
#306990=CARTESIAN_POINT('Ctrl Pts',(-1.04618243948374,5.16193679017606,
36.05));
#306991=CARTESIAN_POINT('Ctrl Pts',(-1.0681718193395,5.10649857927001,36.05));
#306992=CARTESIAN_POINT('Ctrl Pts',(-1.09262300577192,5.05353436556821,
36.05));
#306993=CARTESIAN_POINT('Ctrl Pts',(-1.12433596830973,5.00550562421531,
36.05));
#306994=CARTESIAN_POINT('Ctrl Pts',(-1.15864753037992,4.96016808484432,
36.05));
#306995=CARTESIAN_POINT('Ctrl Pts',(-1.19710037531277,4.92023184841449,
36.05));
#306996=CARTESIAN_POINT('Ctrl Pts',(-1.23739271777899,4.88475706229418,
36.05));
#306997=CARTESIAN_POINT('Ctrl Pts',(-1.27989304559387,4.85499849822356,
36.05));
#306998=CARTESIAN_POINT('Ctrl Pts',(-1.32477571753144,4.83107657862712,
36.05));
#306999=CARTESIAN_POINT('Ctrl Pts',(-1.37159611734391,4.81206099883602,
36.05));
#307000=CARTESIAN_POINT('Ctrl Pts',(-1.42050302431008,4.79884546139153,
36.05));
#307001=CARTESIAN_POINT('Ctrl Pts',(-1.4714149990235,4.78983464316812,36.05));
#307002=CARTESIAN_POINT('Ctrl Pts',(-1.50606613811182,4.78904075129562,
36.05));
#307003=CARTESIAN_POINT('Ctrl Pts',(-1.52371651785714,4.78863636363636,
36.05));
#307004=CARTESIAN_POINT('',(-1.01022727272727,5.42131696428571,32.1799631621335));
#307005=CARTESIAN_POINT('Ctrl Pts',(-1.01022727272727,5.42131696428571,
36.05));
#307006=CARTESIAN_POINT('Ctrl Pts',(-1.01022727272727,5.42131696428571,
36.29));
#307007=CARTESIAN_POINT('Ctrl Pts',(-1.01076599462072,5.44495600403826,
36.05));
#307008=CARTESIAN_POINT('Ctrl Pts',(-1.01076599462072,5.44495600403826,
36.29));
#307009=CARTESIAN_POINT('Ctrl Pts',(-1.0118214237133,5.49126808190085,36.05));
#307010=CARTESIAN_POINT('Ctrl Pts',(-1.0118214237133,5.49126808190085,36.29));
#307011=CARTESIAN_POINT('Ctrl Pts',(-1.01878267475616,5.55896687878814,
36.05));
#307012=CARTESIAN_POINT('Ctrl Pts',(-1.01878267475616,5.55896687878814,
36.29));
#307013=CARTESIAN_POINT('Ctrl Pts',(-1.03107800379365,5.62293356367208,
36.05));
#307014=CARTESIAN_POINT('Ctrl Pts',(-1.03107800379365,5.62293356367208,
36.29));
#307015=CARTESIAN_POINT('Ctrl Pts',(-1.04789745408079,5.68327106051297,
36.05));
#307016=CARTESIAN_POINT('Ctrl Pts',(-1.04789745408079,5.68327106051297,
36.29));
#307017=CARTESIAN_POINT('Ctrl Pts',(-1.06908652243424,5.74035420483588,
36.05));
#307018=CARTESIAN_POINT('Ctrl Pts',(-1.06908652243424,5.74035420483588,
36.29));
#307019=CARTESIAN_POINT('Ctrl Pts',(-1.09547159489994,5.79399835274014,
36.05));
#307020=CARTESIAN_POINT('Ctrl Pts',(-1.09547159489994,5.79399835274014,
36.29));
#307021=CARTESIAN_POINT('Ctrl Pts',(-1.12719592427129,5.8437725973715,36.05));
#307022=CARTESIAN_POINT('Ctrl Pts',(-1.12719592427129,5.8437725973715,36.29));
#307023=CARTESIAN_POINT('Ctrl Pts',(-1.1634661665603,5.88934000071629,36.05));
#307024=CARTESIAN_POINT('Ctrl Pts',(-1.1634661665603,5.88934000071629,36.29));
#307025=CARTESIAN_POINT('Ctrl Pts',(-1.20222138279797,5.93098943621083,
36.05));
#307026=CARTESIAN_POINT('Ctrl Pts',(-1.20222138279797,5.93098943621083,
36.29));
#307027=CARTESIAN_POINT('Ctrl Pts',(-1.24358478999076,5.96739207884556,
36.05));
#307028=CARTESIAN_POINT('Ctrl Pts',(-1.24358478999076,5.96739207884556,
36.29));
#307029=CARTESIAN_POINT('Ctrl Pts',(-1.28715520747738,5.99780008387924,
36.05));
#307030=CARTESIAN_POINT('Ctrl Pts',(-1.28715520747738,5.99780008387924,
36.29));
#307031=CARTESIAN_POINT('Ctrl Pts',(-1.33229168731682,6.02332207855003,
36.05));
#307032=CARTESIAN_POINT('Ctrl Pts',(-1.33229168731682,6.02332207855003,
36.29));
#307033=CARTESIAN_POINT('Ctrl Pts',(-1.37963229428386,6.04244867323907,
36.05));
#307034=CARTESIAN_POINT('Ctrl Pts',(-1.37963229428386,6.04244867323907,
36.29));
#307035=CARTESIAN_POINT('Ctrl Pts',(-1.42850133450328,6.05706063884487,
36.05));
#307036=CARTESIAN_POINT('Ctrl Pts',(-1.42850133450328,6.05706063884487,
36.29));
#307037=CARTESIAN_POINT('Ctrl Pts',(-1.47960608156579,6.0655628055813,36.05));
#307038=CARTESIAN_POINT('Ctrl Pts',(-1.47960608156579,6.0655628055813,36.29));
#307039=CARTESIAN_POINT('Ctrl Pts',(-1.51445101604866,6.06643934639816,
36.05));
#307040=CARTESIAN_POINT('Ctrl Pts',(-1.51445101604866,6.06643934639816,
36.29));
#307041=CARTESIAN_POINT('Ctrl Pts',(-1.53209212662338,6.06688311688312,
36.05));
#307042=CARTESIAN_POINT('Ctrl Pts',(-1.53209212662338,6.06688311688312,
36.29));
#307043=CARTESIAN_POINT('',(-1.53209212662338,6.06688311688312,36.05));
#307044=CARTESIAN_POINT('Ctrl Pts',(-1.53209212662338,6.06688311688312,
36.05));
#307045=CARTESIAN_POINT('Ctrl Pts',(-1.51445101604866,6.06643934639816,
36.05));
#307046=CARTESIAN_POINT('Ctrl Pts',(-1.47960608156579,6.0655628055813,36.05));
#307047=CARTESIAN_POINT('Ctrl Pts',(-1.42850133450328,6.05706063884487,
36.05));
#307048=CARTESIAN_POINT('Ctrl Pts',(-1.37963229428386,6.04244867323907,
36.05));
#307049=CARTESIAN_POINT('Ctrl Pts',(-1.33229168731682,6.02332207855003,
36.05));
#307050=CARTESIAN_POINT('Ctrl Pts',(-1.28715520747738,5.99780008387924,
36.05));
#307051=CARTESIAN_POINT('Ctrl Pts',(-1.24358478999076,5.96739207884556,
36.05));
#307052=CARTESIAN_POINT('Ctrl Pts',(-1.20222138279797,5.93098943621083,
36.05));
#307053=CARTESIAN_POINT('Ctrl Pts',(-1.1634661665603,5.88934000071629,36.05));
#307054=CARTESIAN_POINT('Ctrl Pts',(-1.12719592427129,5.8437725973715,36.05));
#307055=CARTESIAN_POINT('Ctrl Pts',(-1.09547159489994,5.79399835274014,
36.05));
#307056=CARTESIAN_POINT('Ctrl Pts',(-1.06908652243424,5.74035420483588,
36.05));
#307057=CARTESIAN_POINT('Ctrl Pts',(-1.04789745408079,5.68327106051297,
36.05));
#307058=CARTESIAN_POINT('Ctrl Pts',(-1.03107800379365,5.62293356367208,
36.05));
#307059=CARTESIAN_POINT('Ctrl Pts',(-1.01878267475616,5.55896687878814,
36.05));
#307060=CARTESIAN_POINT('Ctrl Pts',(-1.0118214237133,5.49126808190085,36.05));
#307061=CARTESIAN_POINT('Ctrl Pts',(-1.01076599462072,5.44495600403826,
36.05));
#307062=CARTESIAN_POINT('Ctrl Pts',(-1.01022727272727,5.42131696428571,
36.05));
#307063=CARTESIAN_POINT('',(-1.53209212662338,6.06688311688312,32.1799631621335));
#307064=CARTESIAN_POINT('Ctrl Pts',(-1.53209212662338,6.06688311688312,
36.05));
#307065=CARTESIAN_POINT('Ctrl Pts',(-1.53209212662338,6.06688311688312,
36.29));
#307066=CARTESIAN_POINT('Ctrl Pts',(-1.54951650473831,6.066434027441,36.05));
#307067=CARTESIAN_POINT('Ctrl Pts',(-1.54951650473831,6.066434027441,36.29));
#307068=CARTESIAN_POINT('Ctrl Pts',(-1.58393065600793,6.06554704990339,
36.05));
#307069=CARTESIAN_POINT('Ctrl Pts',(-1.58393065600793,6.06554704990339,
36.29));
#307070=CARTESIAN_POINT('Ctrl Pts',(-1.63443083923324,6.05712286492333,
36.05));
#307071=CARTESIAN_POINT('Ctrl Pts',(-1.63443083923324,6.05712286492333,
36.29));
#307072=CARTESIAN_POINT('Ctrl Pts',(-1.68245238910184,6.04224031339717,
36.05));
#307073=CARTESIAN_POINT('Ctrl Pts',(-1.68245238910184,6.04224031339717,
36.29));
#307074=CARTESIAN_POINT('Ctrl Pts',(-1.72937966613072,6.02430730620351,
36.05));
#307075=CARTESIAN_POINT('Ctrl Pts',(-1.72937966613072,6.02430730620351,
36.29));
#307076=CARTESIAN_POINT('Ctrl Pts',(-1.77322121904902,5.9981366813217,36.05));
#307077=CARTESIAN_POINT('Ctrl Pts',(-1.77322121904902,5.9981366813217,36.29));
#307078=CARTESIAN_POINT('Ctrl Pts',(-1.81610239307926,5.96827285277195,
36.05));
#307079=CARTESIAN_POINT('Ctrl Pts',(-1.81610239307926,5.96827285277195,
36.29));
#307080=CARTESIAN_POINT('Ctrl Pts',(-1.85592360031061,5.93155196527191,
36.05));
#307081=CARTESIAN_POINT('Ctrl Pts',(-1.85592360031061,5.93155196527191,
36.29));
#307082=CARTESIAN_POINT('Ctrl Pts',(-1.89389884878363,5.89060348709459,
36.05));
#307083=CARTESIAN_POINT('Ctrl Pts',(-1.89389884878363,5.89060348709459,
36.29));
#307084=CARTESIAN_POINT('Ctrl Pts',(-1.92842298904565,5.84507968533497,
36.05));
#307085=CARTESIAN_POINT('Ctrl Pts',(-1.92842298904565,5.84507968533497,
36.29));
#307086=CARTESIAN_POINT('Ctrl Pts',(-1.95895617838667,5.79605922055842,
36.05));
#307087=CARTESIAN_POINT('Ctrl Pts',(-1.95895617838667,5.79605922055842,
36.29));
#307088=CARTESIAN_POINT('Ctrl Pts',(-1.98409150523322,5.74343345049149,
36.05));
#307089=CARTESIAN_POINT('Ctrl Pts',(-1.98409150523322,5.74343345049149,
36.29));
#307090=CARTESIAN_POINT('Ctrl Pts',(-2.00454652849223,5.68767671276928,
36.05));
#307091=CARTESIAN_POINT('Ctrl Pts',(-2.00454652849223,5.68767671276928,
36.29));
#307092=CARTESIAN_POINT('Ctrl Pts',(-2.02161548775311,5.6290296721576,36.05));
#307093=CARTESIAN_POINT('Ctrl Pts',(-2.02161548775311,5.6290296721576,36.29));
#307094=CARTESIAN_POINT('Ctrl Pts',(-2.03309476195626,5.56687880407454,
36.05));
#307095=CARTESIAN_POINT('Ctrl Pts',(-2.03309476195626,5.56687880407454,
36.29));
#307096=CARTESIAN_POINT('Ctrl Pts',(-2.03932413346711,5.50155035955671,
36.05));
#307097=CARTESIAN_POINT('Ctrl Pts',(-2.03932413346711,5.50155035955671,
36.29));
#307098=CARTESIAN_POINT('Ctrl Pts',(-2.04048048892973,5.45697972788144,
36.05));
#307099=CARTESIAN_POINT('Ctrl Pts',(-2.04048048892973,5.45697972788144,
36.29));
#307100=CARTESIAN_POINT('Ctrl Pts',(-2.04107142857143,5.43420251623377,
36.05));
#307101=CARTESIAN_POINT('Ctrl Pts',(-2.04107142857143,5.43420251623377,
36.29));
#307102=CARTESIAN_POINT('',(-2.04107142857143,5.43420251623377,36.05));
#307103=CARTESIAN_POINT('Ctrl Pts',(-2.04107142857143,5.43420251623377,
36.05));
#307104=CARTESIAN_POINT('Ctrl Pts',(-2.04048048892973,5.45697972788144,
36.05));
#307105=CARTESIAN_POINT('Ctrl Pts',(-2.03932413346711,5.50155035955671,
36.05));
#307106=CARTESIAN_POINT('Ctrl Pts',(-2.03309476195626,5.56687880407454,
36.05));
#307107=CARTESIAN_POINT('Ctrl Pts',(-2.02161548775311,5.6290296721576,36.05));
#307108=CARTESIAN_POINT('Ctrl Pts',(-2.00454652849223,5.68767671276928,
36.05));
#307109=CARTESIAN_POINT('Ctrl Pts',(-1.98409150523322,5.74343345049149,
36.05));
#307110=CARTESIAN_POINT('Ctrl Pts',(-1.95895617838667,5.79605922055842,
36.05));
#307111=CARTESIAN_POINT('Ctrl Pts',(-1.92842298904565,5.84507968533497,
36.05));
#307112=CARTESIAN_POINT('Ctrl Pts',(-1.89389884878363,5.89060348709459,
36.05));
#307113=CARTESIAN_POINT('Ctrl Pts',(-1.85592360031061,5.93155196527191,
36.05));
#307114=CARTESIAN_POINT('Ctrl Pts',(-1.81610239307926,5.96827285277195,
36.05));
#307115=CARTESIAN_POINT('Ctrl Pts',(-1.77322121904902,5.9981366813217,36.05));
#307116=CARTESIAN_POINT('Ctrl Pts',(-1.72937966613072,6.02430730620351,
36.05));
#307117=CARTESIAN_POINT('Ctrl Pts',(-1.68245238910184,6.04224031339717,
36.05));
#307118=CARTESIAN_POINT('Ctrl Pts',(-1.63443083923324,6.05712286492333,
36.05));
#307119=CARTESIAN_POINT('Ctrl Pts',(-1.58393065600793,6.06554704990339,
36.05));
#307120=CARTESIAN_POINT('Ctrl Pts',(-1.54951650473831,6.066434027441,36.05));
#307121=CARTESIAN_POINT('Ctrl Pts',(-1.53209212662338,6.06688311688312,
36.05));
#307122=CARTESIAN_POINT('',(-2.04107142857143,5.43420251623377,32.1799631621335));
#307123=CARTESIAN_POINT('Ctrl Pts',(-2.04107142857143,5.43420251623377,
36.05));
#307124=CARTESIAN_POINT('Ctrl Pts',(-2.04107142857143,5.43420251623377,
36.29));
#307125=CARTESIAN_POINT('Ctrl Pts',(-2.0405543266768,5.41055942108448,36.05));
#307126=CARTESIAN_POINT('Ctrl Pts',(-2.0405543266768,5.41055942108448,36.29));
#307127=CARTESIAN_POINT('Ctrl Pts',(-2.03954125408768,5.36423939815085,
36.05));
#307128=CARTESIAN_POINT('Ctrl Pts',(-2.03954125408768,5.36423939815085,
36.29));
#307129=CARTESIAN_POINT('Ctrl Pts',(-2.03228105709878,5.2966367303295,36.05));
#307130=CARTESIAN_POINT('Ctrl Pts',(-2.03228105709878,5.2966367303295,36.29));
#307131=CARTESIAN_POINT('Ctrl Pts',(-2.02107341871046,5.23250639408275,
36.05));
#307132=CARTESIAN_POINT('Ctrl Pts',(-2.02107341871046,5.23250639408275,
36.29));
#307133=CARTESIAN_POINT('Ctrl Pts',(-2.00398348773993,5.17226185872411,
36.05));
#307134=CARTESIAN_POINT('Ctrl Pts',(-2.00398348773993,5.17226185872411,
36.29));
#307135=CARTESIAN_POINT('Ctrl Pts',(-1.98289443792092,5.11515155101266,
36.05));
#307136=CARTESIAN_POINT('Ctrl Pts',(-1.98289443792092,5.11515155101266,
36.29));
#307137=CARTESIAN_POINT('Ctrl Pts',(-1.95643257885054,5.06166487648077,
36.05));
#307138=CARTESIAN_POINT('Ctrl Pts',(-1.95643257885054,5.06166487648077,
36.29));
#307139=CARTESIAN_POINT('Ctrl Pts',(-1.92516888970118,5.0117585395718,36.05));
#307140=CARTESIAN_POINT('Ctrl Pts',(-1.92516888970118,5.0117585395718,36.29));
#307141=CARTESIAN_POINT('Ctrl Pts',(-1.89024117171633,4.96538056994282,
36.05));
#307142=CARTESIAN_POINT('Ctrl Pts',(-1.89024117171633,4.96538056994282,
36.29));
#307143=CARTESIAN_POINT('Ctrl Pts',(-1.85077488100797,4.9247537203412,36.05));
#307144=CARTESIAN_POINT('Ctrl Pts',(-1.85077488100797,4.9247537203412,36.29));
#307145=CARTESIAN_POINT('Ctrl Pts',(-1.81007783686995,4.8879898300525,36.05));
#307146=CARTESIAN_POINT('Ctrl Pts',(-1.81007783686995,4.8879898300525,36.29));
#307147=CARTESIAN_POINT('Ctrl Pts',(-1.76718752939314,4.85710381362087,
36.05));
#307148=CARTESIAN_POINT('Ctrl Pts',(-1.76718752939314,4.85710381362087,
36.29));
#307149=CARTESIAN_POINT('Ctrl Pts',(-1.72190013812572,4.83218747720399,
36.05));
#307150=CARTESIAN_POINT('Ctrl Pts',(-1.72190013812572,4.83218747720399,
36.29));
#307151=CARTESIAN_POINT('Ctrl Pts',(-1.67490398148407,4.81303741070313,
36.05));
#307152=CARTESIAN_POINT('Ctrl Pts',(-1.67490398148407,4.81303741070313,
36.29));
#307153=CARTESIAN_POINT('Ctrl Pts',(-1.62621370039499,4.79855444913016,
36.05));
#307154=CARTESIAN_POINT('Ctrl Pts',(-1.62621370039499,4.79855444913016,
36.29));
#307155=CARTESIAN_POINT('Ctrl Pts',(-1.57556683534013,4.78994040169141,
36.05));
#307156=CARTESIAN_POINT('Ctrl Pts',(-1.57556683534013,4.78994040169141,
36.29));
#307157=CARTESIAN_POINT('Ctrl Pts',(-1.54114485828132,4.789074687262,36.05));
#307158=CARTESIAN_POINT('Ctrl Pts',(-1.54114485828132,4.789074687262,36.29));
#307159=CARTESIAN_POINT('Ctrl Pts',(-1.52371651785714,4.78863636363636,
36.05));
#307160=CARTESIAN_POINT('Ctrl Pts',(-1.52371651785714,4.78863636363636,
36.29));
#307161=CARTESIAN_POINT('Ctrl Pts',(-1.52371651785714,4.78863636363636,
36.05));
#307162=CARTESIAN_POINT('Ctrl Pts',(-1.54114485828132,4.789074687262,36.05));
#307163=CARTESIAN_POINT('Ctrl Pts',(-1.57556683534013,4.78994040169141,
36.05));
#307164=CARTESIAN_POINT('Ctrl Pts',(-1.62621370039499,4.79855444913016,
36.05));
#307165=CARTESIAN_POINT('Ctrl Pts',(-1.67490398148407,4.81303741070313,
36.05));
#307166=CARTESIAN_POINT('Ctrl Pts',(-1.72190013812572,4.83218747720399,
36.05));
#307167=CARTESIAN_POINT('Ctrl Pts',(-1.76718752939314,4.85710381362087,
36.05));
#307168=CARTESIAN_POINT('Ctrl Pts',(-1.81007783686995,4.8879898300525,36.05));
#307169=CARTESIAN_POINT('Ctrl Pts',(-1.85077488100797,4.9247537203412,36.05));
#307170=CARTESIAN_POINT('Ctrl Pts',(-1.89024117171633,4.96538056994282,
36.05));
#307171=CARTESIAN_POINT('Ctrl Pts',(-1.92516888970118,5.0117585395718,36.05));
#307172=CARTESIAN_POINT('Ctrl Pts',(-1.95643257885054,5.06166487648077,
36.05));
#307173=CARTESIAN_POINT('Ctrl Pts',(-1.98289443792092,5.11515155101266,
36.05));
#307174=CARTESIAN_POINT('Ctrl Pts',(-2.00398348773993,5.17226185872411,
36.05));
#307175=CARTESIAN_POINT('Ctrl Pts',(-2.02107341871046,5.23250639408275,
36.05));
#307176=CARTESIAN_POINT('Ctrl Pts',(-2.03228105709878,5.2966367303295,36.05));
#307177=CARTESIAN_POINT('Ctrl Pts',(-2.03954125408768,5.36423939815085,
36.05));
#307178=CARTESIAN_POINT('Ctrl Pts',(-2.0405543266768,5.41055942108448,36.05));
#307179=CARTESIAN_POINT('Ctrl Pts',(-2.04107142857143,5.43420251623377,
36.05));
#307180=CARTESIAN_POINT('Ctrl Pts',(-1.52371651785714,6.39675324675325,
36.05));
#307181=CARTESIAN_POINT('Ctrl Pts',(-1.52371651785714,6.39675324675325,
36.29));
#307182=CARTESIAN_POINT('Ctrl Pts',(-1.49749406178753,6.39823178023093,
36.05));
#307183=CARTESIAN_POINT('Ctrl Pts',(-1.49749406178753,6.39823178023093,
36.29));
#307184=CARTESIAN_POINT('Ctrl Pts',(-1.44564553849367,6.40115522024948,
36.05));
#307185=CARTESIAN_POINT('Ctrl Pts',(-1.44564553849367,6.40115522024948,
36.29));
#307186=CARTESIAN_POINT('Ctrl Pts',(-1.37190501458764,6.42869442089,36.05));
#307187=CARTESIAN_POINT('Ctrl Pts',(-1.37190501458764,6.42869442089,36.29));
#307188=CARTESIAN_POINT('Ctrl Pts',(-1.30436731865975,6.47176243493413,
36.05));
#307189=CARTESIAN_POINT('Ctrl Pts',(-1.30436731865975,6.47176243493413,
36.29));
#307190=CARTESIAN_POINT('Ctrl Pts',(-1.24507578007146,6.5313545752525,36.05));
#307191=CARTESIAN_POINT('Ctrl Pts',(-1.24507578007146,6.5313545752525,36.29));
#307192=CARTESIAN_POINT('Ctrl Pts',(-1.19545427309708,6.60421240376617,
36.05));
#307193=CARTESIAN_POINT('Ctrl Pts',(-1.19545427309708,6.60421240376617,
36.29));
#307194=CARTESIAN_POINT('Ctrl Pts',(-1.15909489053248,6.68851996626879,
36.05));
#307195=CARTESIAN_POINT('Ctrl Pts',(-1.15909489053248,6.68851996626879,
36.29));
#307196=CARTESIAN_POINT('Ctrl Pts',(-1.13760625764887,6.78290098418177,
36.05));
#307197=CARTESIAN_POINT('Ctrl Pts',(-1.13760625764887,6.78290098418177,
36.29));
#307198=CARTESIAN_POINT('Ctrl Pts',(-1.13518507442834,6.84892095288905,
36.05));
#307199=CARTESIAN_POINT('Ctrl Pts',(-1.13518507442834,6.84892095288905,
36.29));
#307200=CARTESIAN_POINT('Ctrl Pts',(-1.13392857142857,6.88318283279221,
36.05));
#307201=CARTESIAN_POINT('Ctrl Pts',(-1.13392857142857,6.88318283279221,
36.29));
#307202=CARTESIAN_POINT('',(-1.52371651785714,6.39675324675325,36.05));
#307203=CARTESIAN_POINT('',(-1.52371651785714,6.39675324675325,32.1799631621335));
#307204=CARTESIAN_POINT('',(-1.13392857142857,6.88318283279221,36.05));
#307205=CARTESIAN_POINT('Ctrl Pts',(-1.13392857142857,6.88318283279221,
36.05));
#307206=CARTESIAN_POINT('Ctrl Pts',(-1.13518507442834,6.84892095288905,
36.05));
#307207=CARTESIAN_POINT('Ctrl Pts',(-1.13760625764887,6.78290098418177,
36.05));
#307208=CARTESIAN_POINT('Ctrl Pts',(-1.15909489053248,6.68851996626879,
36.05));
#307209=CARTESIAN_POINT('Ctrl Pts',(-1.19545427309708,6.60421240376617,
36.05));
#307210=CARTESIAN_POINT('Ctrl Pts',(-1.24507578007146,6.5313545752525,36.05));
#307211=CARTESIAN_POINT('Ctrl Pts',(-1.30436731865975,6.47176243493413,
36.05));
#307212=CARTESIAN_POINT('Ctrl Pts',(-1.37190501458764,6.42869442089,36.05));
#307213=CARTESIAN_POINT('Ctrl Pts',(-1.44564553849367,6.40115522024948,
36.05));
#307214=CARTESIAN_POINT('Ctrl Pts',(-1.49749406178753,6.39823178023093,
36.05));
#307215=CARTESIAN_POINT('Ctrl Pts',(-1.52371651785714,6.39675324675325,
36.05));
#307216=CARTESIAN_POINT('',(-1.13392857142857,6.88318283279221,32.1799631621335));
#307217=CARTESIAN_POINT('Ctrl Pts',(-1.13392857142857,6.88318283279221,
36.05));
#307218=CARTESIAN_POINT('Ctrl Pts',(-1.13392857142857,6.88318283279221,
36.29));
#307219=CARTESIAN_POINT('Ctrl Pts',(-1.13513622427257,6.91852455417192,
36.05));
#307220=CARTESIAN_POINT('Ctrl Pts',(-1.13513622427257,6.91852455417192,
36.29));
#307221=CARTESIAN_POINT('Ctrl Pts',(-1.13746675383528,6.98672704040914,
36.05));
#307222=CARTESIAN_POINT('Ctrl Pts',(-1.13746675383528,6.98672704040914,
36.29));
#307223=CARTESIAN_POINT('Ctrl Pts',(-1.15960212713315,7.08387655284218,
36.05));
#307224=CARTESIAN_POINT('Ctrl Pts',(-1.15960212713315,7.08387655284218,
36.29));
#307225=CARTESIAN_POINT('Ctrl Pts',(-1.1967070851926,7.17101343023865,36.05));
#307226=CARTESIAN_POINT('Ctrl Pts',(-1.1967070851926,7.17101343023865,36.29));
#307227=CARTESIAN_POINT('Ctrl Pts',(-1.248366652071,7.24570928090529,36.05));
#307228=CARTESIAN_POINT('Ctrl Pts',(-1.248366652071,7.24570928090529,36.29));
#307229=CARTESIAN_POINT('Ctrl Pts',(-1.30855629123278,7.30781082924543,
36.05));
#307230=CARTESIAN_POINT('Ctrl Pts',(-1.30855629123278,7.30781082924543,
36.29));
#307231=CARTESIAN_POINT('Ctrl Pts',(-1.3763696724576,7.35293658272662,36.05));
#307232=CARTESIAN_POINT('Ctrl Pts',(-1.3763696724576,7.35293658272662,36.29));
#307233=CARTESIAN_POINT('Ctrl Pts',(-1.45006627196568,7.38129222806274,
36.05));
#307234=CARTESIAN_POINT('Ctrl Pts',(-1.45006627196568,7.38129222806274,
36.29));
#307235=CARTESIAN_POINT('Ctrl Pts',(-1.50156524889417,7.38466150198483,
36.05));
#307236=CARTESIAN_POINT('Ctrl Pts',(-1.50156524889417,7.38466150198483,
36.29));
#307237=CARTESIAN_POINT('Ctrl Pts',(-1.52758218344156,7.38636363636364,
36.05));
#307238=CARTESIAN_POINT('Ctrl Pts',(-1.52758218344156,7.38636363636364,
36.29));
#307239=CARTESIAN_POINT('',(-1.52758218344156,7.38636363636364,36.05));
#307240=CARTESIAN_POINT('Ctrl Pts',(-1.52758218344156,7.38636363636364,
36.05));
#307241=CARTESIAN_POINT('Ctrl Pts',(-1.50156524889417,7.38466150198483,
36.05));
#307242=CARTESIAN_POINT('Ctrl Pts',(-1.45006627196568,7.38129222806274,
36.05));
#307243=CARTESIAN_POINT('Ctrl Pts',(-1.3763696724576,7.35293658272662,36.05));
#307244=CARTESIAN_POINT('Ctrl Pts',(-1.30855629123278,7.30781082924543,
36.05));
#307245=CARTESIAN_POINT('Ctrl Pts',(-1.248366652071,7.24570928090529,36.05));
#307246=CARTESIAN_POINT('Ctrl Pts',(-1.1967070851926,7.17101343023865,36.05));
#307247=CARTESIAN_POINT('Ctrl Pts',(-1.15960212713315,7.08387655284218,
36.05));
#307248=CARTESIAN_POINT('Ctrl Pts',(-1.13746675383528,6.98672704040914,
36.05));
#307249=CARTESIAN_POINT('Ctrl Pts',(-1.13513622427257,6.91852455417192,
36.05));
#307250=CARTESIAN_POINT('Ctrl Pts',(-1.13392857142857,6.88318283279221,
36.05));
#307251=CARTESIAN_POINT('',(-1.52758218344156,7.38636363636364,32.1799631621335));
#307252=CARTESIAN_POINT('Ctrl Pts',(-1.52758218344156,7.38636363636364,
36.05));
#307253=CARTESIAN_POINT('Ctrl Pts',(-1.52758218344156,7.38636363636364,
36.29));
#307254=CARTESIAN_POINT('Ctrl Pts',(-1.55358237022155,7.38486930154146,
36.05));
#307255=CARTESIAN_POINT('Ctrl Pts',(-1.55358237022155,7.38486930154146,
36.29));
#307256=CARTESIAN_POINT('Ctrl Pts',(-1.60499794902611,7.38191424239284,
36.05));
#307257=CARTESIAN_POINT('Ctrl Pts',(-1.60499794902611,7.38191424239284,
36.29));
#307258=CARTESIAN_POINT('Ctrl Pts',(-1.67863965341545,7.354443366284,36.05));
#307259=CARTESIAN_POINT('Ctrl Pts',(-1.67863965341545,7.354443366284,36.29));
#307260=CARTESIAN_POINT('Ctrl Pts',(-1.74575926016136,7.30974046602882,
36.05));
#307261=CARTESIAN_POINT('Ctrl Pts',(-1.74575926016136,7.30974046602882,
36.29));
#307262=CARTESIAN_POINT('Ctrl Pts',(-1.80513211335571,7.24931351323173,
36.05));
#307263=CARTESIAN_POINT('Ctrl Pts',(-1.80513211335571,7.24931351323173,
36.29));
#307264=CARTESIAN_POINT('Ctrl Pts',(-1.85584586752056,7.17700242184242,
36.05));
#307265=CARTESIAN_POINT('Ctrl Pts',(-1.85584586752056,7.17700242184242,
36.29));
#307266=CARTESIAN_POINT('Ctrl Pts',(-1.8909492802511,7.09344714231162,36.05));
#307267=CARTESIAN_POINT('Ctrl Pts',(-1.8909492802511,7.09344714231162,36.29));
#307268=CARTESIAN_POINT('Ctrl Pts',(-1.91396932214169,7.00188822714751,
36.05));
#307269=CARTESIAN_POINT('Ctrl Pts',(-1.91396932214169,7.00188822714751,
36.29));
#307270=CARTESIAN_POINT('Ctrl Pts',(-1.91621068652427,6.93766582705582,
36.05));
#307271=CARTESIAN_POINT('Ctrl Pts',(-1.91621068652427,6.93766582705582,
36.29));
#307272=CARTESIAN_POINT('Ctrl Pts',(-1.91737012987013,6.90444399350649,
36.05));
#307273=CARTESIAN_POINT('Ctrl Pts',(-1.91737012987013,6.90444399350649,
36.29));
#307274=CARTESIAN_POINT('',(-1.91737012987013,6.90444399350649,36.05));
#307275=CARTESIAN_POINT('Ctrl Pts',(-1.91737012987013,6.90444399350649,
36.05));
#307276=CARTESIAN_POINT('Ctrl Pts',(-1.91621068652427,6.93766582705582,
36.05));
#307277=CARTESIAN_POINT('Ctrl Pts',(-1.91396932214169,7.00188822714751,
36.05));
#307278=CARTESIAN_POINT('Ctrl Pts',(-1.8909492802511,7.09344714231162,36.05));
#307279=CARTESIAN_POINT('Ctrl Pts',(-1.85584586752056,7.17700242184242,
36.05));
#307280=CARTESIAN_POINT('Ctrl Pts',(-1.80513211335571,7.24931351323173,
36.05));
#307281=CARTESIAN_POINT('Ctrl Pts',(-1.74575926016136,7.30974046602882,
36.05));
#307282=CARTESIAN_POINT('Ctrl Pts',(-1.67863965341545,7.354443366284,36.05));
#307283=CARTESIAN_POINT('Ctrl Pts',(-1.60499794902611,7.38191424239284,
36.05));
#307284=CARTESIAN_POINT('Ctrl Pts',(-1.55358237022155,7.38486930154146,
36.05));
#307285=CARTESIAN_POINT('Ctrl Pts',(-1.52758218344156,7.38636363636364,
36.05));
#307286=CARTESIAN_POINT('',(-1.91737012987013,6.90444399350649,32.1799631621335));
#307287=CARTESIAN_POINT('Ctrl Pts',(-1.91737012987013,6.90444399350649,
36.05));
#307288=CARTESIAN_POINT('Ctrl Pts',(-1.91737012987013,6.90444399350649,
36.29));
#307289=CARTESIAN_POINT('Ctrl Pts',(-1.91613148952843,6.8676136615146,36.05));
#307290=CARTESIAN_POINT('Ctrl Pts',(-1.91613148952843,6.8676136615146,36.29));
#307291=CARTESIAN_POINT('Ctrl Pts',(-1.91376144516393,6.79714161418861,
36.05));
#307292=CARTESIAN_POINT('Ctrl Pts',(-1.91376144516393,6.79714161418861,
36.29));
#307293=CARTESIAN_POINT('Ctrl Pts',(-1.89249074922576,6.69694686802566,
36.05));
#307294=CARTESIAN_POINT('Ctrl Pts',(-1.89249074922576,6.69694686802566,
36.29));
#307295=CARTESIAN_POINT('Ctrl Pts',(-1.85626188657584,6.60868448959127,
36.05));
#307296=CARTESIAN_POINT('Ctrl Pts',(-1.85626188657584,6.60868448959127,
36.29));
#307297=CARTESIAN_POINT('Ctrl Pts',(-1.80667059916436,6.53319043392833,
36.05));
#307298=CARTESIAN_POINT('Ctrl Pts',(-1.80667059916436,6.53319043392833,
36.29));
#307299=CARTESIAN_POINT('Ctrl Pts',(-1.74600279585425,6.47327605218271,
36.05));
#307300=CARTESIAN_POINT('Ctrl Pts',(-1.74600279585425,6.47327605218271,
36.29));
#307301=CARTESIAN_POINT('Ctrl Pts',(-1.67833795046176,6.42829274914181,
36.05));
#307302=CARTESIAN_POINT('Ctrl Pts',(-1.67833795046176,6.42829274914181,
36.29));
#307303=CARTESIAN_POINT('Ctrl Pts',(-1.60297996097691,6.4012532984509,36.05));
#307304=CARTESIAN_POINT('Ctrl Pts',(-1.60297996097691,6.4012532984509,36.29));
#307305=CARTESIAN_POINT('Ctrl Pts',(-1.5503437032771,6.39826496143831,36.05));
#307306=CARTESIAN_POINT('Ctrl Pts',(-1.5503437032771,6.39826496143831,36.29));
#307307=CARTESIAN_POINT('Ctrl Pts',(-1.52371651785714,6.39675324675325,
36.05));
#307308=CARTESIAN_POINT('Ctrl Pts',(-1.52371651785714,6.39675324675325,
36.29));
#307309=CARTESIAN_POINT('Ctrl Pts',(-1.52371651785714,6.39675324675325,
36.05));
#307310=CARTESIAN_POINT('Ctrl Pts',(-1.5503437032771,6.39826496143831,36.05));
#307311=CARTESIAN_POINT('Ctrl Pts',(-1.60297996097691,6.4012532984509,36.05));
#307312=CARTESIAN_POINT('Ctrl Pts',(-1.67833795046176,6.42829274914181,
36.05));
#307313=CARTESIAN_POINT('Ctrl Pts',(-1.74600279585425,6.47327605218271,
36.05));
#307314=CARTESIAN_POINT('Ctrl Pts',(-1.80667059916436,6.53319043392833,
36.05));
#307315=CARTESIAN_POINT('Ctrl Pts',(-1.85626188657584,6.60868448959127,
36.05));
#307316=CARTESIAN_POINT('Ctrl Pts',(-1.89249074922576,6.69694686802566,
36.05));
#307317=CARTESIAN_POINT('Ctrl Pts',(-1.91376144516393,6.79714161418861,
36.05));
#307318=CARTESIAN_POINT('Ctrl Pts',(-1.91613148952843,6.8676136615146,36.05));
#307319=CARTESIAN_POINT('Ctrl Pts',(-1.91737012987013,6.90444399350649,
36.05));
#307320=CARTESIAN_POINT('Ctrl Pts',(1.52758218344156,4.78863636363636,36.05));
#307321=CARTESIAN_POINT('Ctrl Pts',(1.52758218344156,4.78863636363636,36.29));
#307322=CARTESIAN_POINT('Ctrl Pts',(1.54523256318688,4.78904075129562,36.05));
#307323=CARTESIAN_POINT('Ctrl Pts',(1.54523256318688,4.78904075129562,36.29));
#307324=CARTESIAN_POINT('Ctrl Pts',(1.5798837022752,4.78983464316812,36.05));
#307325=CARTESIAN_POINT('Ctrl Pts',(1.5798837022752,4.78983464316812,36.29));
#307326=CARTESIAN_POINT('Ctrl Pts',(1.63079567698862,4.79884546139153,36.05));
#307327=CARTESIAN_POINT('Ctrl Pts',(1.63079567698862,4.79884546139153,36.29));
#307328=CARTESIAN_POINT('Ctrl Pts',(1.67970258395479,4.81206099883602,36.05));
#307329=CARTESIAN_POINT('Ctrl Pts',(1.67970258395479,4.81206099883602,36.29));
#307330=CARTESIAN_POINT('Ctrl Pts',(1.72652298376726,4.83107657862712,36.05));
#307331=CARTESIAN_POINT('Ctrl Pts',(1.72652298376726,4.83107657862712,36.29));
#307332=CARTESIAN_POINT('Ctrl Pts',(1.77140565570483,4.85499849822356,36.05));
#307333=CARTESIAN_POINT('Ctrl Pts',(1.77140565570483,4.85499849822356,36.29));
#307334=CARTESIAN_POINT('Ctrl Pts',(1.81390598351971,4.88475706229418,36.05));
#307335=CARTESIAN_POINT('Ctrl Pts',(1.81390598351971,4.88475706229418,36.29));
#307336=CARTESIAN_POINT('Ctrl Pts',(1.85419832598593,4.92023184841449,36.05));
#307337=CARTESIAN_POINT('Ctrl Pts',(1.85419832598593,4.92023184841449,36.29));
#307338=CARTESIAN_POINT('Ctrl Pts',(1.89265117091878,4.96016808484432,36.05));
#307339=CARTESIAN_POINT('Ctrl Pts',(1.89265117091878,4.96016808484432,36.29));
#307340=CARTESIAN_POINT('Ctrl Pts',(1.92696273298897,5.00550562421531,36.05));
#307341=CARTESIAN_POINT('Ctrl Pts',(1.92696273298897,5.00550562421531,36.29));
#307342=CARTESIAN_POINT('Ctrl Pts',(1.95867569552678,5.05353436556821,36.05));
#307343=CARTESIAN_POINT('Ctrl Pts',(1.95867569552678,5.05353436556821,36.29));
#307344=CARTESIAN_POINT('Ctrl Pts',(1.9831268819592,5.10649857927001,36.05));
#307345=CARTESIAN_POINT('Ctrl Pts',(1.9831268819592,5.10649857927001,36.29));
#307346=CARTESIAN_POINT('Ctrl Pts',(2.00511626181496,5.16193679017606,36.05));
#307347=CARTESIAN_POINT('Ctrl Pts',(2.00511626181496,5.16193679017606,36.29));
#307348=CARTESIAN_POINT('Ctrl Pts',(2.02054669570705,5.22177284922642,36.05));
#307349=CARTESIAN_POINT('Ctrl Pts',(2.02054669570705,5.22177284922642,36.29));
#307350=CARTESIAN_POINT('Ctrl Pts',(2.0334543847172,5.28488392294487,36.05));
#307351=CARTESIAN_POINT('Ctrl Pts',(2.0334543847172,5.28488392294487,36.29));
#307352=CARTESIAN_POINT('Ctrl Pts',(2.03922895997908,5.35205975094169,36.05));
#307353=CARTESIAN_POINT('Ctrl Pts',(2.03922895997908,5.35205975094169,36.29));
#307354=CARTESIAN_POINT('Ctrl Pts',(2.04044852772871,5.39790252089427,36.05));
#307355=CARTESIAN_POINT('Ctrl Pts',(2.04044852772871,5.39790252089427,36.29));
#307356=CARTESIAN_POINT('Ctrl Pts',(2.04107142857143,5.42131696428571,36.05));
#307357=CARTESIAN_POINT('Ctrl Pts',(2.04107142857143,5.42131696428571,36.29));
#307358=CARTESIAN_POINT('',(1.52758218344156,4.78863636363636,36.05));
#307359=CARTESIAN_POINT('',(1.52758218344156,4.78863636363636,32.1799631621335));
#307360=CARTESIAN_POINT('',(2.04107142857143,5.42131696428571,36.05));
#307361=CARTESIAN_POINT('Ctrl Pts',(2.04107142857143,5.42131696428571,36.05));
#307362=CARTESIAN_POINT('Ctrl Pts',(2.04044852772871,5.39790252089427,36.05));
#307363=CARTESIAN_POINT('Ctrl Pts',(2.03922895997908,5.35205975094169,36.05));
#307364=CARTESIAN_POINT('Ctrl Pts',(2.0334543847172,5.28488392294487,36.05));
#307365=CARTESIAN_POINT('Ctrl Pts',(2.02054669570705,5.22177284922642,36.05));
#307366=CARTESIAN_POINT('Ctrl Pts',(2.00511626181496,5.16193679017606,36.05));
#307367=CARTESIAN_POINT('Ctrl Pts',(1.9831268819592,5.10649857927001,36.05));
#307368=CARTESIAN_POINT('Ctrl Pts',(1.95867569552678,5.05353436556821,36.05));
#307369=CARTESIAN_POINT('Ctrl Pts',(1.92696273298897,5.00550562421531,36.05));
#307370=CARTESIAN_POINT('Ctrl Pts',(1.89265117091878,4.96016808484432,36.05));
#307371=CARTESIAN_POINT('Ctrl Pts',(1.85419832598593,4.92023184841449,36.05));
#307372=CARTESIAN_POINT('Ctrl Pts',(1.81390598351971,4.88475706229418,36.05));
#307373=CARTESIAN_POINT('Ctrl Pts',(1.77140565570483,4.85499849822356,36.05));
#307374=CARTESIAN_POINT('Ctrl Pts',(1.72652298376726,4.83107657862712,36.05));
#307375=CARTESIAN_POINT('Ctrl Pts',(1.67970258395479,4.81206099883602,36.05));
#307376=CARTESIAN_POINT('Ctrl Pts',(1.63079567698862,4.79884546139153,36.05));
#307377=CARTESIAN_POINT('Ctrl Pts',(1.5798837022752,4.78983464316812,36.05));
#307378=CARTESIAN_POINT('Ctrl Pts',(1.54523256318688,4.78904075129562,36.05));
#307379=CARTESIAN_POINT('Ctrl Pts',(1.52758218344156,4.78863636363636,36.05));
#307380=CARTESIAN_POINT('',(2.04107142857143,5.42131696428571,32.1799631621335));
#307381=CARTESIAN_POINT('Ctrl Pts',(2.04107142857143,5.42131696428571,36.05));
#307382=CARTESIAN_POINT('Ctrl Pts',(2.04107142857143,5.42131696428571,36.29));
#307383=CARTESIAN_POINT('Ctrl Pts',(2.04053270667799,5.44495600403826,36.05));
#307384=CARTESIAN_POINT('Ctrl Pts',(2.04053270667799,5.44495600403826,36.29));
#307385=CARTESIAN_POINT('Ctrl Pts',(2.0394772775854,5.49126808190085,36.05));
#307386=CARTESIAN_POINT('Ctrl Pts',(2.0394772775854,5.49126808190085,36.29));
#307387=CARTESIAN_POINT('Ctrl Pts',(2.03251602654254,5.55896687878814,36.05));
#307388=CARTESIAN_POINT('Ctrl Pts',(2.03251602654254,5.55896687878814,36.29));
#307389=CARTESIAN_POINT('Ctrl Pts',(2.02022069750506,5.62293356367208,36.05));
#307390=CARTESIAN_POINT('Ctrl Pts',(2.02022069750506,5.62293356367208,36.29));
#307391=CARTESIAN_POINT('Ctrl Pts',(2.00340124721791,5.68327106051297,36.05));
#307392=CARTESIAN_POINT('Ctrl Pts',(2.00340124721791,5.68327106051297,36.29));
#307393=CARTESIAN_POINT('Ctrl Pts',(1.98221217886446,5.74035420483588,36.05));
#307394=CARTESIAN_POINT('Ctrl Pts',(1.98221217886446,5.74035420483588,36.29));
#307395=CARTESIAN_POINT('Ctrl Pts',(1.95582710639876,5.79399835274014,36.05));
#307396=CARTESIAN_POINT('Ctrl Pts',(1.95582710639876,5.79399835274014,36.29));
#307397=CARTESIAN_POINT('Ctrl Pts',(1.92410277702741,5.84377259737151,36.05));
#307398=CARTESIAN_POINT('Ctrl Pts',(1.92410277702741,5.84377259737151,36.29));
#307399=CARTESIAN_POINT('Ctrl Pts',(1.88783253473841,5.88934000071629,36.05));
#307400=CARTESIAN_POINT('Ctrl Pts',(1.88783253473841,5.88934000071629,36.29));
#307401=CARTESIAN_POINT('Ctrl Pts',(1.84907731850073,5.93098943621083,36.05));
#307402=CARTESIAN_POINT('Ctrl Pts',(1.84907731850073,5.93098943621083,36.29));
#307403=CARTESIAN_POINT('Ctrl Pts',(1.80771391130794,5.96739207884556,36.05));
#307404=CARTESIAN_POINT('Ctrl Pts',(1.80771391130794,5.96739207884556,36.29));
#307405=CARTESIAN_POINT('Ctrl Pts',(1.76414349382133,5.99780008387924,36.05));
#307406=CARTESIAN_POINT('Ctrl Pts',(1.76414349382133,5.99780008387924,36.29));
#307407=CARTESIAN_POINT('Ctrl Pts',(1.71900701398188,6.02332207855003,36.05));
#307408=CARTESIAN_POINT('Ctrl Pts',(1.71900701398188,6.02332207855003,36.29));
#307409=CARTESIAN_POINT('Ctrl Pts',(1.67166640701484,6.04244867323907,36.05));
#307410=CARTESIAN_POINT('Ctrl Pts',(1.67166640701484,6.04244867323907,36.29));
#307411=CARTESIAN_POINT('Ctrl Pts',(1.62279736679542,6.05706063884487,36.05));
#307412=CARTESIAN_POINT('Ctrl Pts',(1.62279736679542,6.05706063884487,36.29));
#307413=CARTESIAN_POINT('Ctrl Pts',(1.57169261973291,6.0655628055813,36.05));
#307414=CARTESIAN_POINT('Ctrl Pts',(1.57169261973291,6.0655628055813,36.29));
#307415=CARTESIAN_POINT('Ctrl Pts',(1.53684768525004,6.06643934639816,36.05));
#307416=CARTESIAN_POINT('Ctrl Pts',(1.53684768525004,6.06643934639816,36.29));
#307417=CARTESIAN_POINT('Ctrl Pts',(1.51920657467533,6.06688311688312,36.05));
#307418=CARTESIAN_POINT('Ctrl Pts',(1.51920657467533,6.06688311688312,36.29));
#307419=CARTESIAN_POINT('',(1.51920657467533,6.06688311688312,36.05));
#307420=CARTESIAN_POINT('Ctrl Pts',(1.51920657467533,6.06688311688312,36.05));
#307421=CARTESIAN_POINT('Ctrl Pts',(1.53684768525004,6.06643934639816,36.05));
#307422=CARTESIAN_POINT('Ctrl Pts',(1.57169261973291,6.0655628055813,36.05));
#307423=CARTESIAN_POINT('Ctrl Pts',(1.62279736679542,6.05706063884487,36.05));
#307424=CARTESIAN_POINT('Ctrl Pts',(1.67166640701484,6.04244867323907,36.05));
#307425=CARTESIAN_POINT('Ctrl Pts',(1.71900701398188,6.02332207855003,36.05));
#307426=CARTESIAN_POINT('Ctrl Pts',(1.76414349382133,5.99780008387924,36.05));
#307427=CARTESIAN_POINT('Ctrl Pts',(1.80771391130794,5.96739207884556,36.05));
#307428=CARTESIAN_POINT('Ctrl Pts',(1.84907731850073,5.93098943621083,36.05));
#307429=CARTESIAN_POINT('Ctrl Pts',(1.88783253473841,5.88934000071629,36.05));
#307430=CARTESIAN_POINT('Ctrl Pts',(1.92410277702741,5.84377259737151,36.05));
#307431=CARTESIAN_POINT('Ctrl Pts',(1.95582710639876,5.79399835274014,36.05));
#307432=CARTESIAN_POINT('Ctrl Pts',(1.98221217886446,5.74035420483588,36.05));
#307433=CARTESIAN_POINT('Ctrl Pts',(2.00340124721791,5.68327106051297,36.05));
#307434=CARTESIAN_POINT('Ctrl Pts',(2.02022069750506,5.62293356367208,36.05));
#307435=CARTESIAN_POINT('Ctrl Pts',(2.03251602654254,5.55896687878814,36.05));
#307436=CARTESIAN_POINT('Ctrl Pts',(2.0394772775854,5.49126808190085,36.05));
#307437=CARTESIAN_POINT('Ctrl Pts',(2.04053270667799,5.44495600403826,36.05));
#307438=CARTESIAN_POINT('Ctrl Pts',(2.04107142857143,5.42131696428571,36.05));
#307439=CARTESIAN_POINT('',(1.51920657467533,6.06688311688312,32.1799631621335));
#307440=CARTESIAN_POINT('Ctrl Pts',(1.51920657467533,6.06688311688312,36.05));
#307441=CARTESIAN_POINT('Ctrl Pts',(1.51920657467533,6.06688311688312,36.29));
#307442=CARTESIAN_POINT('Ctrl Pts',(1.5017821965604,6.066434027441,36.05));
#307443=CARTESIAN_POINT('Ctrl Pts',(1.5017821965604,6.066434027441,36.29));
#307444=CARTESIAN_POINT('Ctrl Pts',(1.46736804529077,6.06554704990339,36.05));
#307445=CARTESIAN_POINT('Ctrl Pts',(1.46736804529077,6.06554704990339,36.29));
#307446=CARTESIAN_POINT('Ctrl Pts',(1.41686786206546,6.05712286492333,36.05));
#307447=CARTESIAN_POINT('Ctrl Pts',(1.41686786206546,6.05712286492333,36.29));
#307448=CARTESIAN_POINT('Ctrl Pts',(1.36884631219687,6.04224031339717,36.05));
#307449=CARTESIAN_POINT('Ctrl Pts',(1.36884631219687,6.04224031339717,36.29));
#307450=CARTESIAN_POINT('Ctrl Pts',(1.32191903516798,6.02430730620351,36.05));
#307451=CARTESIAN_POINT('Ctrl Pts',(1.32191903516798,6.02430730620351,36.29));
#307452=CARTESIAN_POINT('Ctrl Pts',(1.27807748224968,5.99813668132169,36.05));
#307453=CARTESIAN_POINT('Ctrl Pts',(1.27807748224968,5.99813668132169,36.29));
#307454=CARTESIAN_POINT('Ctrl Pts',(1.23519630821944,5.96827285277196,36.05));
#307455=CARTESIAN_POINT('Ctrl Pts',(1.23519630821944,5.96827285277196,36.29));
#307456=CARTESIAN_POINT('Ctrl Pts',(1.19537510098809,5.93155196527191,36.05));
#307457=CARTESIAN_POINT('Ctrl Pts',(1.19537510098809,5.93155196527191,36.29));
#307458=CARTESIAN_POINT('Ctrl Pts',(1.15739985251507,5.89060348709459,36.05));
#307459=CARTESIAN_POINT('Ctrl Pts',(1.15739985251507,5.89060348709459,36.29));
#307460=CARTESIAN_POINT('Ctrl Pts',(1.12287571225305,5.84507968533496,36.05));
#307461=CARTESIAN_POINT('Ctrl Pts',(1.12287571225305,5.84507968533496,36.29));
#307462=CARTESIAN_POINT('Ctrl Pts',(1.09234252291203,5.79605922055842,36.05));
#307463=CARTESIAN_POINT('Ctrl Pts',(1.09234252291203,5.79605922055842,36.29));
#307464=CARTESIAN_POINT('Ctrl Pts',(1.06720719606548,5.74343345049149,36.05));
#307465=CARTESIAN_POINT('Ctrl Pts',(1.06720719606548,5.74343345049149,36.29));
#307466=CARTESIAN_POINT('Ctrl Pts',(1.04675217280647,5.68767671276929,36.05));
#307467=CARTESIAN_POINT('Ctrl Pts',(1.04675217280647,5.68767671276929,36.29));
#307468=CARTESIAN_POINT('Ctrl Pts',(1.02968321354559,5.6290296721576,36.05));
#307469=CARTESIAN_POINT('Ctrl Pts',(1.02968321354559,5.6290296721576,36.29));
#307470=CARTESIAN_POINT('Ctrl Pts',(1.01820393934243,5.56687880407454,36.05));
#307471=CARTESIAN_POINT('Ctrl Pts',(1.01820393934243,5.56687880407454,36.29));
#307472=CARTESIAN_POINT('Ctrl Pts',(1.01197456783159,5.50155035955671,36.05));
#307473=CARTESIAN_POINT('Ctrl Pts',(1.01197456783159,5.50155035955671,36.29));
#307474=CARTESIAN_POINT('Ctrl Pts',(1.01081821236896,5.45697972788144,36.05));
#307475=CARTESIAN_POINT('Ctrl Pts',(1.01081821236896,5.45697972788144,36.29));
#307476=CARTESIAN_POINT('Ctrl Pts',(1.01022727272727,5.43420251623377,36.05));
#307477=CARTESIAN_POINT('Ctrl Pts',(1.01022727272727,5.43420251623377,36.29));
#307478=CARTESIAN_POINT('',(1.01022727272727,5.43420251623377,36.05));
#307479=CARTESIAN_POINT('Ctrl Pts',(1.01022727272727,5.43420251623377,36.05));
#307480=CARTESIAN_POINT('Ctrl Pts',(1.01081821236896,5.45697972788144,36.05));
#307481=CARTESIAN_POINT('Ctrl Pts',(1.01197456783159,5.50155035955671,36.05));
#307482=CARTESIAN_POINT('Ctrl Pts',(1.01820393934243,5.56687880407454,36.05));
#307483=CARTESIAN_POINT('Ctrl Pts',(1.02968321354559,5.6290296721576,36.05));
#307484=CARTESIAN_POINT('Ctrl Pts',(1.04675217280647,5.68767671276929,36.05));
#307485=CARTESIAN_POINT('Ctrl Pts',(1.06720719606548,5.74343345049149,36.05));
#307486=CARTESIAN_POINT('Ctrl Pts',(1.09234252291203,5.79605922055842,36.05));
#307487=CARTESIAN_POINT('Ctrl Pts',(1.12287571225305,5.84507968533496,36.05));
#307488=CARTESIAN_POINT('Ctrl Pts',(1.15739985251507,5.89060348709459,36.05));
#307489=CARTESIAN_POINT('Ctrl Pts',(1.19537510098809,5.93155196527191,36.05));
#307490=CARTESIAN_POINT('Ctrl Pts',(1.23519630821944,5.96827285277196,36.05));
#307491=CARTESIAN_POINT('Ctrl Pts',(1.27807748224968,5.99813668132169,36.05));
#307492=CARTESIAN_POINT('Ctrl Pts',(1.32191903516798,6.02430730620351,36.05));
#307493=CARTESIAN_POINT('Ctrl Pts',(1.36884631219687,6.04224031339717,36.05));
#307494=CARTESIAN_POINT('Ctrl Pts',(1.41686786206546,6.05712286492333,36.05));
#307495=CARTESIAN_POINT('Ctrl Pts',(1.46736804529077,6.06554704990339,36.05));
#307496=CARTESIAN_POINT('Ctrl Pts',(1.5017821965604,6.066434027441,36.05));
#307497=CARTESIAN_POINT('Ctrl Pts',(1.51920657467533,6.06688311688312,36.05));
#307498=CARTESIAN_POINT('',(1.01022727272727,5.43420251623377,32.1799631621335));
#307499=CARTESIAN_POINT('Ctrl Pts',(1.01022727272727,5.43420251623377,36.05));
#307500=CARTESIAN_POINT('Ctrl Pts',(1.01022727272727,5.43420251623377,36.29));
#307501=CARTESIAN_POINT('Ctrl Pts',(1.01074437462189,5.41055942108448,36.05));
#307502=CARTESIAN_POINT('Ctrl Pts',(1.01074437462189,5.41055942108448,36.29));
#307503=CARTESIAN_POINT('Ctrl Pts',(1.01175744721102,5.36423939815086,36.05));
#307504=CARTESIAN_POINT('Ctrl Pts',(1.01175744721102,5.36423939815086,36.29));
#307505=CARTESIAN_POINT('Ctrl Pts',(1.01901764419993,5.2966367303295,36.05));
#307506=CARTESIAN_POINT('Ctrl Pts',(1.01901764419993,5.2966367303295,36.29));
#307507=CARTESIAN_POINT('Ctrl Pts',(1.03022528258824,5.23250639408275,36.05));
#307508=CARTESIAN_POINT('Ctrl Pts',(1.03022528258824,5.23250639408275,36.29));
#307509=CARTESIAN_POINT('Ctrl Pts',(1.04731521355877,5.17226185872411,36.05));
#307510=CARTESIAN_POINT('Ctrl Pts',(1.04731521355877,5.17226185872411,36.29));
#307511=CARTESIAN_POINT('Ctrl Pts',(1.06840426337778,5.11515155101266,36.05));
#307512=CARTESIAN_POINT('Ctrl Pts',(1.06840426337778,5.11515155101266,36.29));
#307513=CARTESIAN_POINT('Ctrl Pts',(1.09486612244816,5.06166487648077,36.05));
#307514=CARTESIAN_POINT('Ctrl Pts',(1.09486612244816,5.06166487648077,36.29));
#307515=CARTESIAN_POINT('Ctrl Pts',(1.12612981159753,5.0117585395718,36.05));
#307516=CARTESIAN_POINT('Ctrl Pts',(1.12612981159753,5.0117585395718,36.29));
#307517=CARTESIAN_POINT('Ctrl Pts',(1.16105752958236,4.96538056994282,36.05));
#307518=CARTESIAN_POINT('Ctrl Pts',(1.16105752958236,4.96538056994282,36.29));
#307519=CARTESIAN_POINT('Ctrl Pts',(1.20052382029073,4.9247537203412,36.05));
#307520=CARTESIAN_POINT('Ctrl Pts',(1.20052382029073,4.9247537203412,36.29));
#307521=CARTESIAN_POINT('Ctrl Pts',(1.24122086442875,4.88798983005251,36.05));
#307522=CARTESIAN_POINT('Ctrl Pts',(1.24122086442875,4.88798983005251,36.29));
#307523=CARTESIAN_POINT('Ctrl Pts',(1.28411117190556,4.85710381362087,36.05));
#307524=CARTESIAN_POINT('Ctrl Pts',(1.28411117190556,4.85710381362087,36.29));
#307525=CARTESIAN_POINT('Ctrl Pts',(1.32939856317298,4.83218747720399,36.05));
#307526=CARTESIAN_POINT('Ctrl Pts',(1.32939856317298,4.83218747720399,36.29));
#307527=CARTESIAN_POINT('Ctrl Pts',(1.37639471981463,4.81303741070312,36.05));
#307528=CARTESIAN_POINT('Ctrl Pts',(1.37639471981463,4.81303741070312,36.29));
#307529=CARTESIAN_POINT('Ctrl Pts',(1.42508500090371,4.79855444913016,36.05));
#307530=CARTESIAN_POINT('Ctrl Pts',(1.42508500090371,4.79855444913016,36.29));
#307531=CARTESIAN_POINT('Ctrl Pts',(1.47573186595857,4.78994040169141,36.05));
#307532=CARTESIAN_POINT('Ctrl Pts',(1.47573186595857,4.78994040169141,36.29));
#307533=CARTESIAN_POINT('Ctrl Pts',(1.51015384301738,4.789074687262,36.05));
#307534=CARTESIAN_POINT('Ctrl Pts',(1.51015384301738,4.789074687262,36.29));
#307535=CARTESIAN_POINT('Ctrl Pts',(1.52758218344156,4.78863636363636,36.05));
#307536=CARTESIAN_POINT('Ctrl Pts',(1.52758218344156,4.78863636363636,36.29));
#307537=CARTESIAN_POINT('Ctrl Pts',(1.52758218344156,4.78863636363636,36.05));
#307538=CARTESIAN_POINT('Ctrl Pts',(1.51015384301738,4.789074687262,36.05));
#307539=CARTESIAN_POINT('Ctrl Pts',(1.47573186595857,4.78994040169141,36.05));
#307540=CARTESIAN_POINT('Ctrl Pts',(1.42508500090371,4.79855444913016,36.05));
#307541=CARTESIAN_POINT('Ctrl Pts',(1.37639471981463,4.81303741070312,36.05));
#307542=CARTESIAN_POINT('Ctrl Pts',(1.32939856317298,4.83218747720399,36.05));
#307543=CARTESIAN_POINT('Ctrl Pts',(1.28411117190556,4.85710381362087,36.05));
#307544=CARTESIAN_POINT('Ctrl Pts',(1.24122086442875,4.88798983005251,36.05));
#307545=CARTESIAN_POINT('Ctrl Pts',(1.20052382029073,4.9247537203412,36.05));
#307546=CARTESIAN_POINT('Ctrl Pts',(1.16105752958236,4.96538056994282,36.05));
#307547=CARTESIAN_POINT('Ctrl Pts',(1.12612981159753,5.0117585395718,36.05));
#307548=CARTESIAN_POINT('Ctrl Pts',(1.09486612244816,5.06166487648077,36.05));
#307549=CARTESIAN_POINT('Ctrl Pts',(1.06840426337778,5.11515155101266,36.05));
#307550=CARTESIAN_POINT('Ctrl Pts',(1.04731521355877,5.17226185872411,36.05));
#307551=CARTESIAN_POINT('Ctrl Pts',(1.03022528258824,5.23250639408275,36.05));
#307552=CARTESIAN_POINT('Ctrl Pts',(1.01901764419993,5.2966367303295,36.05));
#307553=CARTESIAN_POINT('Ctrl Pts',(1.01175744721102,5.36423939815086,36.05));
#307554=CARTESIAN_POINT('Ctrl Pts',(1.01074437462189,5.41055942108448,36.05));
#307555=CARTESIAN_POINT('Ctrl Pts',(1.01022727272727,5.43420251623377,36.05));
#307556=CARTESIAN_POINT('Ctrl Pts',(1.52758218344156,6.39675324675325,36.05));
#307557=CARTESIAN_POINT('Ctrl Pts',(1.52758218344156,6.39675324675325,36.29));
#307558=CARTESIAN_POINT('Ctrl Pts',(1.55380463951118,6.39823178023093,36.05));
#307559=CARTESIAN_POINT('Ctrl Pts',(1.55380463951118,6.39823178023093,36.29));
#307560=CARTESIAN_POINT('Ctrl Pts',(1.60565316280503,6.40115522024948,36.05));
#307561=CARTESIAN_POINT('Ctrl Pts',(1.60565316280503,6.40115522024948,36.29));
#307562=CARTESIAN_POINT('Ctrl Pts',(1.67939368671106,6.42869442089,36.05));
#307563=CARTESIAN_POINT('Ctrl Pts',(1.67939368671106,6.42869442089,36.29));
#307564=CARTESIAN_POINT('Ctrl Pts',(1.74693138263896,6.47176243493413,36.05));
#307565=CARTESIAN_POINT('Ctrl Pts',(1.74693138263896,6.47176243493413,36.29));
#307566=CARTESIAN_POINT('Ctrl Pts',(1.80622292122723,6.5313545752525,36.05));
#307567=CARTESIAN_POINT('Ctrl Pts',(1.80622292122723,6.5313545752525,36.29));
#307568=CARTESIAN_POINT('Ctrl Pts',(1.85584442820162,6.60421240376617,36.05));
#307569=CARTESIAN_POINT('Ctrl Pts',(1.85584442820162,6.60421240376617,36.29));
#307570=CARTESIAN_POINT('Ctrl Pts',(1.89220381076623,6.68851996626879,36.05));
#307571=CARTESIAN_POINT('Ctrl Pts',(1.89220381076623,6.68851996626879,36.29));
#307572=CARTESIAN_POINT('Ctrl Pts',(1.91369244364984,6.78290098418177,36.05));
#307573=CARTESIAN_POINT('Ctrl Pts',(1.91369244364984,6.78290098418177,36.29));
#307574=CARTESIAN_POINT('Ctrl Pts',(1.91611362687036,6.84892095288905,36.05));
#307575=CARTESIAN_POINT('Ctrl Pts',(1.91611362687036,6.84892095288905,36.29));
#307576=CARTESIAN_POINT('Ctrl Pts',(1.91737012987013,6.88318283279221,36.05));
#307577=CARTESIAN_POINT('Ctrl Pts',(1.91737012987013,6.88318283279221,36.29));
#307578=CARTESIAN_POINT('',(1.52758218344156,6.39675324675325,36.05));
#307579=CARTESIAN_POINT('',(1.52758218344156,6.39675324675325,32.1799631621335));
#307580=CARTESIAN_POINT('',(1.91737012987013,6.88318283279221,36.05));
#307581=CARTESIAN_POINT('Ctrl Pts',(1.91737012987013,6.88318283279221,36.05));
#307582=CARTESIAN_POINT('Ctrl Pts',(1.91611362687036,6.84892095288905,36.05));
#307583=CARTESIAN_POINT('Ctrl Pts',(1.91369244364984,6.78290098418177,36.05));
#307584=CARTESIAN_POINT('Ctrl Pts',(1.89220381076623,6.68851996626879,36.05));
#307585=CARTESIAN_POINT('Ctrl Pts',(1.85584442820162,6.60421240376617,36.05));
#307586=CARTESIAN_POINT('Ctrl Pts',(1.80622292122723,6.5313545752525,36.05));
#307587=CARTESIAN_POINT('Ctrl Pts',(1.74693138263896,6.47176243493413,36.05));
#307588=CARTESIAN_POINT('Ctrl Pts',(1.67939368671106,6.42869442089,36.05));
#307589=CARTESIAN_POINT('Ctrl Pts',(1.60565316280503,6.40115522024948,36.05));
#307590=CARTESIAN_POINT('Ctrl Pts',(1.55380463951118,6.39823178023093,36.05));
#307591=CARTESIAN_POINT('Ctrl Pts',(1.52758218344156,6.39675324675325,36.05));
#307592=CARTESIAN_POINT('',(1.91737012987013,6.88318283279221,32.1799631621335));
#307593=CARTESIAN_POINT('Ctrl Pts',(1.91737012987013,6.88318283279221,36.05));
#307594=CARTESIAN_POINT('Ctrl Pts',(1.91737012987013,6.88318283279221,36.29));
#307595=CARTESIAN_POINT('Ctrl Pts',(1.91616247702613,6.91852455417192,36.05));
#307596=CARTESIAN_POINT('Ctrl Pts',(1.91616247702613,6.91852455417192,36.29));
#307597=CARTESIAN_POINT('Ctrl Pts',(1.91383194746342,6.98672704040914,36.05));
#307598=CARTESIAN_POINT('Ctrl Pts',(1.91383194746342,6.98672704040914,36.29));
#307599=CARTESIAN_POINT('Ctrl Pts',(1.89169657416555,7.08387655284218,36.05));
#307600=CARTESIAN_POINT('Ctrl Pts',(1.89169657416555,7.08387655284218,36.29));
#307601=CARTESIAN_POINT('Ctrl Pts',(1.8545916161061,7.17101343023865,36.05));
#307602=CARTESIAN_POINT('Ctrl Pts',(1.8545916161061,7.17101343023865,36.29));
#307603=CARTESIAN_POINT('Ctrl Pts',(1.80293204922771,7.24570928090529,36.05));
#307604=CARTESIAN_POINT('Ctrl Pts',(1.80293204922771,7.24570928090529,36.29));
#307605=CARTESIAN_POINT('Ctrl Pts',(1.74274241006592,7.30781082924543,36.05));
#307606=CARTESIAN_POINT('Ctrl Pts',(1.74274241006592,7.30781082924543,36.29));
#307607=CARTESIAN_POINT('Ctrl Pts',(1.6749290288411,7.35293658272662,36.05));
#307608=CARTESIAN_POINT('Ctrl Pts',(1.6749290288411,7.35293658272662,36.29));
#307609=CARTESIAN_POINT('Ctrl Pts',(1.60123242933302,7.38129222806274,36.05));
#307610=CARTESIAN_POINT('Ctrl Pts',(1.60123242933302,7.38129222806274,36.29));
#307611=CARTESIAN_POINT('Ctrl Pts',(1.54973345240453,7.38466150198483,36.05));
#307612=CARTESIAN_POINT('Ctrl Pts',(1.54973345240453,7.38466150198483,36.29));
#307613=CARTESIAN_POINT('Ctrl Pts',(1.52371651785715,7.38636363636364,36.05));
#307614=CARTESIAN_POINT('Ctrl Pts',(1.52371651785715,7.38636363636364,36.29));
#307615=CARTESIAN_POINT('',(1.52371651785715,7.38636363636364,36.05));
#307616=CARTESIAN_POINT('Ctrl Pts',(1.52371651785715,7.38636363636364,36.05));
#307617=CARTESIAN_POINT('Ctrl Pts',(1.54973345240453,7.38466150198483,36.05));
#307618=CARTESIAN_POINT('Ctrl Pts',(1.60123242933302,7.38129222806274,36.05));
#307619=CARTESIAN_POINT('Ctrl Pts',(1.6749290288411,7.35293658272662,36.05));
#307620=CARTESIAN_POINT('Ctrl Pts',(1.74274241006592,7.30781082924543,36.05));
#307621=CARTESIAN_POINT('Ctrl Pts',(1.80293204922771,7.24570928090529,36.05));
#307622=CARTESIAN_POINT('Ctrl Pts',(1.8545916161061,7.17101343023865,36.05));
#307623=CARTESIAN_POINT('Ctrl Pts',(1.89169657416555,7.08387655284218,36.05));
#307624=CARTESIAN_POINT('Ctrl Pts',(1.91383194746342,6.98672704040914,36.05));
#307625=CARTESIAN_POINT('Ctrl Pts',(1.91616247702613,6.91852455417192,36.05));
#307626=CARTESIAN_POINT('Ctrl Pts',(1.91737012987013,6.88318283279221,36.05));
#307627=CARTESIAN_POINT('',(1.52371651785715,7.38636363636364,32.1799631621335));
#307628=CARTESIAN_POINT('Ctrl Pts',(1.52371651785715,7.38636363636364,36.05));
#307629=CARTESIAN_POINT('Ctrl Pts',(1.52371651785715,7.38636363636364,36.29));
#307630=CARTESIAN_POINT('Ctrl Pts',(1.49771633107715,7.38486930154146,36.05));
#307631=CARTESIAN_POINT('Ctrl Pts',(1.49771633107715,7.38486930154146,36.29));
#307632=CARTESIAN_POINT('Ctrl Pts',(1.4463007522726,7.38191424239284,36.05));
#307633=CARTESIAN_POINT('Ctrl Pts',(1.4463007522726,7.38191424239284,36.29));
#307634=CARTESIAN_POINT('Ctrl Pts',(1.37265904788325,7.354443366284,36.05));
#307635=CARTESIAN_POINT('Ctrl Pts',(1.37265904788325,7.354443366284,36.29));
#307636=CARTESIAN_POINT('Ctrl Pts',(1.30553944113734,7.30974046602882,36.05));
#307637=CARTESIAN_POINT('Ctrl Pts',(1.30553944113734,7.30974046602882,36.29));
#307638=CARTESIAN_POINT('Ctrl Pts',(1.246166587943,7.24931351323173,36.05));
#307639=CARTESIAN_POINT('Ctrl Pts',(1.246166587943,7.24931351323173,36.29));
#307640=CARTESIAN_POINT('Ctrl Pts',(1.19545283377814,7.17700242184241,36.05));
#307641=CARTESIAN_POINT('Ctrl Pts',(1.19545283377814,7.17700242184241,36.29));
#307642=CARTESIAN_POINT('Ctrl Pts',(1.16034942104761,7.09344714231162,36.05));
#307643=CARTESIAN_POINT('Ctrl Pts',(1.16034942104761,7.09344714231162,36.29));
#307644=CARTESIAN_POINT('Ctrl Pts',(1.13732937915702,7.0018882271475,36.05));
#307645=CARTESIAN_POINT('Ctrl Pts',(1.13732937915702,7.0018882271475,36.29));
#307646=CARTESIAN_POINT('Ctrl Pts',(1.13508801477443,6.93766582705582,36.05));
#307647=CARTESIAN_POINT('Ctrl Pts',(1.13508801477443,6.93766582705582,36.29));
#307648=CARTESIAN_POINT('Ctrl Pts',(1.13392857142857,6.90444399350649,36.05));
#307649=CARTESIAN_POINT('Ctrl Pts',(1.13392857142857,6.90444399350649,36.29));
#307650=CARTESIAN_POINT('',(1.13392857142857,6.9044439935065,36.05));
#307651=CARTESIAN_POINT('Ctrl Pts',(1.13392857142857,6.9044439935065,36.05));
#307652=CARTESIAN_POINT('Ctrl Pts',(1.13508801477443,6.93766582705582,36.05));
#307653=CARTESIAN_POINT('Ctrl Pts',(1.13732937915702,7.0018882271475,36.05));
#307654=CARTESIAN_POINT('Ctrl Pts',(1.16034942104761,7.09344714231162,36.05));
#307655=CARTESIAN_POINT('Ctrl Pts',(1.19545283377814,7.17700242184241,36.05));
#307656=CARTESIAN_POINT('Ctrl Pts',(1.246166587943,7.24931351323173,36.05));
#307657=CARTESIAN_POINT('Ctrl Pts',(1.30553944113734,7.30974046602882,36.05));
#307658=CARTESIAN_POINT('Ctrl Pts',(1.37265904788325,7.354443366284,36.05));
#307659=CARTESIAN_POINT('Ctrl Pts',(1.4463007522726,7.38191424239284,36.05));
#307660=CARTESIAN_POINT('Ctrl Pts',(1.49771633107715,7.38486930154146,36.05));
#307661=CARTESIAN_POINT('Ctrl Pts',(1.52371651785715,7.38636363636364,36.05));
#307662=CARTESIAN_POINT('',(1.13392857142857,6.9044439935065,32.1799631621335));
#307663=CARTESIAN_POINT('Ctrl Pts',(1.13392857142857,6.9044439935065,36.05));
#307664=CARTESIAN_POINT('Ctrl Pts',(1.13392857142857,6.9044439935065,36.29));
#307665=CARTESIAN_POINT('Ctrl Pts',(1.13516721177027,6.8676136615146,36.05));
#307666=CARTESIAN_POINT('Ctrl Pts',(1.13516721177027,6.8676136615146,36.29));
#307667=CARTESIAN_POINT('Ctrl Pts',(1.13753725613477,6.79714161418862,36.05));
#307668=CARTESIAN_POINT('Ctrl Pts',(1.13753725613477,6.79714161418862,36.29));
#307669=CARTESIAN_POINT('Ctrl Pts',(1.15880795207294,6.69694686802566,36.05));
#307670=CARTESIAN_POINT('Ctrl Pts',(1.15880795207294,6.69694686802566,36.29));
#307671=CARTESIAN_POINT('Ctrl Pts',(1.19503681472287,6.60868448959127,36.05));
#307672=CARTESIAN_POINT('Ctrl Pts',(1.19503681472287,6.60868448959127,36.29));
#307673=CARTESIAN_POINT('Ctrl Pts',(1.24462810213434,6.53319043392833,36.05));
#307674=CARTESIAN_POINT('Ctrl Pts',(1.24462810213434,6.53319043392833,36.29));
#307675=CARTESIAN_POINT('Ctrl Pts',(1.30529590544445,6.47327605218271,36.05));
#307676=CARTESIAN_POINT('Ctrl Pts',(1.30529590544445,6.47327605218271,36.29));
#307677=CARTESIAN_POINT('Ctrl Pts',(1.37296075083694,6.42829274914181,36.05));
#307678=CARTESIAN_POINT('Ctrl Pts',(1.37296075083694,6.42829274914181,36.29));
#307679=CARTESIAN_POINT('Ctrl Pts',(1.44831874032179,6.4012532984509,36.05));
#307680=CARTESIAN_POINT('Ctrl Pts',(1.44831874032179,6.4012532984509,36.29));
#307681=CARTESIAN_POINT('Ctrl Pts',(1.50095499802161,6.39826496143831,36.05));
#307682=CARTESIAN_POINT('Ctrl Pts',(1.50095499802161,6.39826496143831,36.29));
#307683=CARTESIAN_POINT('Ctrl Pts',(1.52758218344156,6.39675324675325,36.05));
#307684=CARTESIAN_POINT('Ctrl Pts',(1.52758218344156,6.39675324675325,36.29));
#307685=CARTESIAN_POINT('Ctrl Pts',(1.52758218344156,6.39675324675325,36.05));
#307686=CARTESIAN_POINT('Ctrl Pts',(1.50095499802161,6.39826496143831,36.05));
#307687=CARTESIAN_POINT('Ctrl Pts',(1.44831874032179,6.4012532984509,36.05));
#307688=CARTESIAN_POINT('Ctrl Pts',(1.37296075083694,6.42829274914181,36.05));
#307689=CARTESIAN_POINT('Ctrl Pts',(1.30529590544445,6.47327605218271,36.05));
#307690=CARTESIAN_POINT('Ctrl Pts',(1.24462810213434,6.53319043392833,36.05));
#307691=CARTESIAN_POINT('Ctrl Pts',(1.19503681472287,6.60868448959127,36.05));
#307692=CARTESIAN_POINT('Ctrl Pts',(1.15880795207294,6.69694686802566,36.05));
#307693=CARTESIAN_POINT('Ctrl Pts',(1.13753725613477,6.79714161418862,36.05));
#307694=CARTESIAN_POINT('Ctrl Pts',(1.13516721177027,6.8676136615146,36.05));
#307695=CARTESIAN_POINT('Ctrl Pts',(1.13392857142857,6.9044439935065,36.05));
#307696=CARTESIAN_POINT('Origin',(0.,0.,36.05));
#307697=CARTESIAN_POINT('',(-2.24724025974026,6.89542410714286,36.05));
#307698=CARTESIAN_POINT('',(-1.86131797889611,6.24212662337662,36.05));
#307699=CARTESIAN_POINT('Ctrl Pts',(-2.24724025974026,6.89542410714286,
36.05));
#307700=CARTESIAN_POINT('Ctrl Pts',(-2.24635828463311,6.85667628421743,
36.05));
#307701=CARTESIAN_POINT('Ctrl Pts',(-2.24466128369114,6.78212192154818,
36.05));
#307702=CARTESIAN_POINT('Ctrl Pts',(-2.22526998846174,6.67544579213543,
36.05));
#307703=CARTESIAN_POINT('Ctrl Pts',(-2.19544755091121,6.57824013430206,
36.05));
#307704=CARTESIAN_POINT('Ctrl Pts',(-2.15255407155767,6.49069341485485,
36.05));
#307705=CARTESIAN_POINT('Ctrl Pts',(-2.09711468722833,6.41311300974787,
36.05));
#307706=CARTESIAN_POINT('Ctrl Pts',(-2.02981249733957,6.34542328474194,
36.05));
#307707=CARTESIAN_POINT('Ctrl Pts',(-1.95088478291998,6.28713666449684,
36.05));
#307708=CARTESIAN_POINT('Ctrl Pts',(-1.89166914263337,6.25737900558171,
36.05));
#307709=CARTESIAN_POINT('Ctrl Pts',(-1.86131797889611,6.24212662337662,
36.05));
#307710=CARTESIAN_POINT('',(-2.37094155844156,5.43291396103896,36.05));
#307711=CARTESIAN_POINT('Ctrl Pts',(-1.86131797889611,6.24212662337662,
36.05));
#307712=CARTESIAN_POINT('Ctrl Pts',(-1.88076808190029,6.23557324032603,
36.05));
#307713=CARTESIAN_POINT('Ctrl Pts',(-1.91917711253447,6.22263196745495,
36.05));
#307714=CARTESIAN_POINT('Ctrl Pts',(-1.97432962905344,6.19776979492405,
36.05));
#307715=CARTESIAN_POINT('Ctrl Pts',(-2.02656583006182,6.16910978501208,
36.05));
#307716=CARTESIAN_POINT('Ctrl Pts',(-2.07499444571376,6.1351992195304,36.05));
#307717=CARTESIAN_POINT('Ctrl Pts',(-2.1202782797022,6.09774166415627,36.05));
#307718=CARTESIAN_POINT('Ctrl Pts',(-2.16248925313098,6.05629105732706,
36.05));
#307719=CARTESIAN_POINT('Ctrl Pts',(-2.20124132093025,6.01030469320115,
36.05));
#307720=CARTESIAN_POINT('Ctrl Pts',(-2.23643083441821,5.96019951630268,
36.05));
#307721=CARTESIAN_POINT('Ctrl Pts',(-2.26824051996169,5.90641132135784,
36.05));
#307722=CARTESIAN_POINT('Ctrl Pts',(-2.29590420953425,5.84911895337204,
36.05));
#307723=CARTESIAN_POINT('Ctrl Pts',(-2.31914738800462,5.78833295550162,
36.05));
#307724=CARTESIAN_POINT('Ctrl Pts',(-2.33776644819188,5.72405509656198,
36.05));
#307725=CARTESIAN_POINT('Ctrl Pts',(-2.35252585809151,5.65624108672131,
36.05));
#307726=CARTESIAN_POINT('Ctrl Pts',(-2.36345937406549,5.58482539360676,
36.05));
#307727=CARTESIAN_POINT('Ctrl Pts',(-2.37001876348768,5.50992190470655,
36.05));
#307728=CARTESIAN_POINT('Ctrl Pts',(-2.37063000734488,5.45891313799848,
36.05));
#307729=CARTESIAN_POINT('Ctrl Pts',(-2.37094155844156,5.43291396103896,
36.05));
#307730=CARTESIAN_POINT('',(-1.52371651785714,4.45876623376623,36.05));
#307731=CARTESIAN_POINT('Ctrl Pts',(-2.37094155844156,5.43291396103896,
36.05));
#307732=CARTESIAN_POINT('Ctrl Pts',(-2.37024051692734,5.39744356397404,
36.05));
#307733=CARTESIAN_POINT('Ctrl Pts',(-2.36886427906175,5.32781045016027,
36.05));
#307734=CARTESIAN_POINT('Ctrl Pts',(-2.35686977721559,5.22616336292247,
36.05));
#307735=CARTESIAN_POINT('Ctrl Pts',(-2.33853623055972,5.12949961741785,
36.05));
#307736=CARTESIAN_POINT('Ctrl Pts',(-2.31200320040195,5.03825698338498,
36.05));
#307737=CARTESIAN_POINT('Ctrl Pts',(-2.27806144254569,4.95218254596678,
36.05));
#307738=CARTESIAN_POINT('Ctrl Pts',(-2.2354792856985,4.87186228483585,36.05));
#307739=CARTESIAN_POINT('Ctrl Pts',(-2.18686174567011,4.79599402074389,
36.05));
#307740=CARTESIAN_POINT('Ctrl Pts',(-2.1298438000822,4.72680658155488,36.05));
#307741=CARTESIAN_POINT('Ctrl Pts',(-2.06813219984915,4.66375358613811,
36.05));
#307742=CARTESIAN_POINT('Ctrl Pts',(-2.00109150543013,4.60959489382438,
36.05));
#307743=CARTESIAN_POINT('Ctrl Pts',(-1.93122097549665,4.56241550483758,
36.05));
#307744=CARTESIAN_POINT('Ctrl Pts',(-1.85703181398638,4.52434515927101,
36.05));
#307745=CARTESIAN_POINT('Ctrl Pts',(-1.77882069442911,4.49538915943629,
36.05));
#307746=CARTESIAN_POINT('Ctrl Pts',(-1.69736543838644,4.47372823681752,
36.05));
#307747=CARTESIAN_POINT('Ctrl Pts',(-1.61170021909538,4.46161006986558,
36.05));
#307748=CARTESIAN_POINT('Ctrl Pts',(-1.55338922539081,4.4597253240939,36.05));
#307749=CARTESIAN_POINT('Ctrl Pts',(-1.52371651785714,4.45876623376623,
36.05));
#307750=CARTESIAN_POINT('',(-0.680357142857142,5.42196124188312,36.05));
#307751=CARTESIAN_POINT('Ctrl Pts',(-1.52371651785714,4.45876623376623,
36.05));
#307752=CARTESIAN_POINT('Ctrl Pts',(-1.49447449269809,4.45973608112409,
36.05));
#307753=CARTESIAN_POINT('Ctrl Pts',(-1.43680842361535,4.46164864649648,
36.05));
#307754=CARTESIAN_POINT('Ctrl Pts',(-1.35198241500324,4.47370190759594,
36.05));
#307755=CARTESIAN_POINT('Ctrl Pts',(-1.27102264425494,4.49553589484458,
36.05));
#307756=CARTESIAN_POINT('Ctrl Pts',(-1.19309519794087,4.5241565808727,36.05));
#307757=CARTESIAN_POINT('Ctrl Pts',(-1.11934856150417,4.56264762609262,
36.05));
#307758=CARTESIAN_POINT('Ctrl Pts',(-1.04958738921064,4.60935645208091,
36.05));
#307759=CARTESIAN_POINT('Ctrl Pts',(-0.983169721460654,4.66400945675856,
36.05));
#307760=CARTESIAN_POINT('Ctrl Pts',(-0.921346136582458,4.72672058470318,
36.05));
#307761=CARTESIAN_POINT('Ctrl Pts',(-0.864790653609182,4.79615096254107,
36.05));
#307762=CARTESIAN_POINT('Ctrl Pts',(-0.814894945031659,4.87078209602146,
36.05));
#307763=CARTESIAN_POINT('Ctrl Pts',(-0.773615124031434,4.95095791492866,
36.05));
#307764=CARTESIAN_POINT('Ctrl Pts',(-0.739130657263025,5.03559649057185,
36.05));
#307765=CARTESIAN_POINT('Ctrl Pts',(-0.713135864328774,5.12552781537341,
36.05));
#307766=CARTESIAN_POINT('Ctrl Pts',(-0.693373801633478,5.21999888881734,
36.05));
#307767=CARTESIAN_POINT('Ctrl Pts',(-0.682716393984036,5.31949010994648,
36.05));
#307768=CARTESIAN_POINT('Ctrl Pts',(-0.681153739192598,5.3873620729942,
36.05));
#307769=CARTESIAN_POINT('Ctrl Pts',(-0.680357142857142,5.42196124188312,
36.05));
#307770=CARTESIAN_POINT('',(-1.18611505681818,6.24212662337662,36.05));
#307771=CARTESIAN_POINT('Ctrl Pts',(-0.680357142857142,5.42196124188312,
36.05));
#307772=CARTESIAN_POINT('Ctrl Pts',(-0.680643402753075,5.44731949788714,
36.05));
#307773=CARTESIAN_POINT('Ctrl Pts',(-0.681202359695404,5.4968345485113,
36.05));
#307774=CARTESIAN_POINT('Ctrl Pts',(-0.688060973290405,5.56952358146944,
36.05));
#307775=CARTESIAN_POINT('Ctrl Pts',(-0.698134608146914,5.63904690448481,
36.05));
#307776=CARTESIAN_POINT('Ctrl Pts',(-0.712369756219759,5.70553707456913,
36.05));
#307777=CARTESIAN_POINT('Ctrl Pts',(-0.730130420178432,5.76902496530641,
36.05));
#307778=CARTESIAN_POINT('Ctrl Pts',(-0.753130561450395,5.82909896870107,
36.05));
#307779=CARTESIAN_POINT('Ctrl Pts',(-0.778997347786388,5.88660676946342,
36.05));
#307780=CARTESIAN_POINT('Ctrl Pts',(-0.810449385509135,5.94000771696759,
36.05));
#307781=CARTESIAN_POINT('Ctrl Pts',(-0.844529687053187,5.99064810748104,
36.05));
#307782=CARTESIAN_POINT('Ctrl Pts',(-0.882532948756259,6.03778353402304,
36.05));
#307783=CARTESIAN_POINT('Ctrl Pts',(-0.924520209270103,6.08096773911451,
36.05));
#307784=CARTESIAN_POINT('Ctrl Pts',(-0.969980971511446,6.12033427680283,
36.05));
#307785=CARTESIAN_POINT('Ctrl Pts',(-1.01831785359978,6.15682435284569,
36.05));
#307786=CARTESIAN_POINT('Ctrl Pts',(-1.07097627880842,6.18887731351974,
36.05));
#307787=CARTESIAN_POINT('Ctrl Pts',(-1.12679451037092,6.21812962575334,
36.05));
#307788=CARTESIAN_POINT('Ctrl Pts',(-1.16621033677113,6.23407454786033,
36.05));
#307789=CARTESIAN_POINT('Ctrl Pts',(-1.18611505681818,6.24212662337662,
36.05));
#307790=CARTESIAN_POINT('',(-0.804058441558441,6.88253855519481,36.05));
#307791=CARTESIAN_POINT('Ctrl Pts',(-1.18611505681818,6.24212662337662,
36.05));
#307792=CARTESIAN_POINT('Ctrl Pts',(-1.15549574155667,6.25752314612396,
36.05));
#307793=CARTESIAN_POINT('Ctrl Pts',(-1.09604440098142,6.28741747621295,
36.05));
#307794=CARTESIAN_POINT('Ctrl Pts',(-1.0177935092216,6.34678274879809,36.05));
#307795=CARTESIAN_POINT('Ctrl Pts',(-0.951235352872532,6.41405772296989,
36.05));
#307796=CARTESIAN_POINT('Ctrl Pts',(-0.897038222357849,6.4907436496301,
36.05));
#307797=CARTESIAN_POINT('Ctrl Pts',(-0.854639610807379,6.57608978278239,
36.05));
#307798=CARTESIAN_POINT('Ctrl Pts',(-0.825519260309656,6.6705401244345,
36.05));
#307799=CARTESIAN_POINT('Ctrl Pts',(-0.806813602327297,6.77356208818653,
36.05));
#307800=CARTESIAN_POINT('Ctrl Pts',(-0.804999967272473,6.8452978442089,
36.05));
#307801=CARTESIAN_POINT('Ctrl Pts',(-0.804058441558441,6.88253855519481,
36.05));
#307802=CARTESIAN_POINT('',(-1.52887073863637,7.71623376623377,36.05));
#307803=CARTESIAN_POINT('Ctrl Pts',(-0.804058441558441,6.88253855519481,
36.05));
#307804=CARTESIAN_POINT('Ctrl Pts',(-0.804650124600102,6.91241766550898,
36.05));
#307805=CARTESIAN_POINT('Ctrl Pts',(-0.805811171394462,6.97104879536392,
36.05));
#307806=CARTESIAN_POINT('Ctrl Pts',(-0.815733176885725,7.05701575208482,
36.05));
#307807=CARTESIAN_POINT('Ctrl Pts',(-0.831597303625935,7.13897358699381,
36.05));
#307808=CARTESIAN_POINT('Ctrl Pts',(-0.854229034877609,7.21661236790923,
36.05));
#307809=CARTESIAN_POINT('Ctrl Pts',(-0.883047786444258,7.29002627559583,
36.05));
#307810=CARTESIAN_POINT('Ctrl Pts',(-0.919708538459593,7.35843862911193,
36.05));
#307811=CARTESIAN_POINT('Ctrl Pts',(-0.961621998889034,7.42336185115535,
36.05));
#307812=CARTESIAN_POINT('Ctrl Pts',(-1.00970620194357,7.48362087256877,
36.05));
#307813=CARTESIAN_POINT('Ctrl Pts',(-1.06268331120451,7.53791001729144,
36.05));
#307814=CARTESIAN_POINT('Ctrl Pts',(-1.119447579553,7.58560597597768,36.05));
#307815=CARTESIAN_POINT('Ctrl Pts',(-1.17924186808025,7.62639783586101,
36.05));
#307816=CARTESIAN_POINT('Ctrl Pts',(-1.24280687342643,7.65953041457979,
36.05));
#307817=CARTESIAN_POINT('Ctrl Pts',(-1.30973339831807,7.68468886160549,
36.05));
#307818=CARTESIAN_POINT('Ctrl Pts',(-1.37991458997475,7.7027904588233,36.05));
#307819=CARTESIAN_POINT('Ctrl Pts',(-1.45335117903047,7.71392449956901,
36.05));
#307820=CARTESIAN_POINT('Ctrl Pts',(-1.50349048519761,7.71545767890599,
36.05));
#307821=CARTESIAN_POINT('Ctrl Pts',(-1.52887073863637,7.71623376623377,
36.05));
#307822=CARTESIAN_POINT('Ctrl Pts',(-1.52887073863637,7.71623376623377,
36.05));
#307823=CARTESIAN_POINT('Ctrl Pts',(-1.55402639381368,7.71538504428939,
36.05));
#307824=CARTESIAN_POINT('Ctrl Pts',(-1.60368781725867,7.71370952681349,
36.05));
#307825=CARTESIAN_POINT('Ctrl Pts',(-1.67660001580121,7.7036309678914,36.05));
#307826=CARTESIAN_POINT('Ctrl Pts',(-1.746104953362,7.68533220871074,36.05));
#307827=CARTESIAN_POINT('Ctrl Pts',(-1.81235851864406,7.65993643724945,
36.05));
#307828=CARTESIAN_POINT('Ctrl Pts',(-1.87562432631225,7.62785439831755,
36.05));
#307829=CARTESIAN_POINT('Ctrl Pts',(-1.93532052837525,7.58805917500155,
36.05));
#307830=CARTESIAN_POINT('Ctrl Pts',(-1.99157504243468,7.54133429965825,
36.05));
#307831=CARTESIAN_POINT('Ctrl Pts',(-2.04420697733625,7.48817807892744,
36.05));
#307832=CARTESIAN_POINT('Ctrl Pts',(-2.09163145310384,7.42884662646377,
36.05));
#307833=CARTESIAN_POINT('Ctrl Pts',(-2.13381867185592,7.36527391878087,
36.05));
#307834=CARTESIAN_POINT('Ctrl Pts',(-2.1683837201686,7.29688183752562,36.05));
#307835=CARTESIAN_POINT('Ctrl Pts',(-2.19802765306379,7.22519194306317,
36.05));
#307836=CARTESIAN_POINT('Ctrl Pts',(-2.2194554245458,7.1485092997012,36.05));
#307837=CARTESIAN_POINT('Ctrl Pts',(-2.23564047821614,7.06800054423278,
36.05));
#307838=CARTESIAN_POINT('Ctrl Pts',(-2.24549498801578,6.98307391394772,
36.05));
#307839=CARTESIAN_POINT('Ctrl Pts',(-2.24664961358837,6.92508712200564,
36.05));
#307840=CARTESIAN_POINT('Ctrl Pts',(-2.24724025974026,6.89542410714286,
36.05));
#307841=CARTESIAN_POINT('Origin',(0.,0.,36.05));
#307842=CARTESIAN_POINT('',(0.804058441558442,6.89542410714286,36.05));
#307843=CARTESIAN_POINT('',(1.1899807224026,6.24212662337662,36.05));
#307844=CARTESIAN_POINT('Ctrl Pts',(0.804058441558442,6.89542410714286,
36.05));
#307845=CARTESIAN_POINT('Ctrl Pts',(0.804940416665592,6.85667628421743,
36.05));
#307846=CARTESIAN_POINT('Ctrl Pts',(0.806637417607563,6.78212192154818,
36.05));
#307847=CARTESIAN_POINT('Ctrl Pts',(0.82602871283696,6.67544579213543,36.05));
#307848=CARTESIAN_POINT('Ctrl Pts',(0.855851150387493,6.57824013430206,
36.05));
#307849=CARTESIAN_POINT('Ctrl Pts',(0.898744629741027,6.49069341485485,
36.05));
#307850=CARTESIAN_POINT('Ctrl Pts',(0.954184014070375,6.41311300974787,
36.05));
#307851=CARTESIAN_POINT('Ctrl Pts',(1.02148620395913,6.34542328474194,36.05));
#307852=CARTESIAN_POINT('Ctrl Pts',(1.10041391837872,6.28713666449684,36.05));
#307853=CARTESIAN_POINT('Ctrl Pts',(1.15962955866533,6.25737900558172,36.05));
#307854=CARTESIAN_POINT('Ctrl Pts',(1.1899807224026,6.24212662337662,36.05));
#307855=CARTESIAN_POINT('',(0.680357142857143,5.43291396103896,36.05));
#307856=CARTESIAN_POINT('Ctrl Pts',(1.1899807224026,6.24212662337662,36.05));
#307857=CARTESIAN_POINT('Ctrl Pts',(1.17053061939841,6.23557324032603,36.05));
#307858=CARTESIAN_POINT('Ctrl Pts',(1.13212158876422,6.22263196745495,36.05));
#307859=CARTESIAN_POINT('Ctrl Pts',(1.07696907224526,6.19776979492405,36.05));
#307860=CARTESIAN_POINT('Ctrl Pts',(1.02473287123688,6.16910978501208,36.05));
#307861=CARTESIAN_POINT('Ctrl Pts',(0.976304255584941,6.1351992195304,36.05));
#307862=CARTESIAN_POINT('Ctrl Pts',(0.931020421596495,6.09774166415628,
36.05));
#307863=CARTESIAN_POINT('Ctrl Pts',(0.888809448167726,6.05629105732706,
36.05));
#307864=CARTESIAN_POINT('Ctrl Pts',(0.850057380368458,6.01030469320115,
36.05));
#307865=CARTESIAN_POINT('Ctrl Pts',(0.814867866880491,5.96019951630268,
36.05));
#307866=CARTESIAN_POINT('Ctrl Pts',(0.783058181337012,5.90641132135784,
36.05));
#307867=CARTESIAN_POINT('Ctrl Pts',(0.755394491764458,5.84911895337204,
36.05));
#307868=CARTESIAN_POINT('Ctrl Pts',(0.732151313294084,5.78833295550162,
36.05));
#307869=CARTESIAN_POINT('Ctrl Pts',(0.713532253106825,5.72405509656199,
36.05));
#307870=CARTESIAN_POINT('Ctrl Pts',(0.698772843207189,5.65624108672131,
36.05));
#307871=CARTESIAN_POINT('Ctrl Pts',(0.687839327233214,5.58482539360676,
36.05));
#307872=CARTESIAN_POINT('Ctrl Pts',(0.681279937811019,5.50992190470655,
36.05));
#307873=CARTESIAN_POINT('Ctrl Pts',(0.680668693953829,5.45891313799848,
36.05));
#307874=CARTESIAN_POINT('Ctrl Pts',(0.680357142857143,5.43291396103896,
36.05));
#307875=CARTESIAN_POINT('',(1.52758218344156,4.45876623376623,36.05));
#307876=CARTESIAN_POINT('Ctrl Pts',(0.680357142857143,5.43291396103896,
36.05));
#307877=CARTESIAN_POINT('Ctrl Pts',(0.681058184371366,5.39744356397404,
36.05));
#307878=CARTESIAN_POINT('Ctrl Pts',(0.682434422236949,5.32781045016027,
36.05));
#307879=CARTESIAN_POINT('Ctrl Pts',(0.694428924083107,5.22616336292247,
36.05));
#307880=CARTESIAN_POINT('Ctrl Pts',(0.712762470738981,5.12949961741785,
36.05));
#307881=CARTESIAN_POINT('Ctrl Pts',(0.739295500896744,5.03825698338498,
36.05));
#307882=CARTESIAN_POINT('Ctrl Pts',(0.773237258753005,4.95218254596678,
36.05));
#307883=CARTESIAN_POINT('Ctrl Pts',(0.815819415600203,4.87186228483585,
36.05));
#307884=CARTESIAN_POINT('Ctrl Pts',(0.864436955628593,4.79599402074389,
36.05));
#307885=CARTESIAN_POINT('Ctrl Pts',(0.921454901216499,4.72680658155488,
36.05));
#307886=CARTESIAN_POINT('Ctrl Pts',(0.983166501449546,4.66375358613811,
36.05));
#307887=CARTESIAN_POINT('Ctrl Pts',(1.05020719586857,4.60959489382439,36.05));
#307888=CARTESIAN_POINT('Ctrl Pts',(1.12007772580205,4.56241550483758,36.05));
#307889=CARTESIAN_POINT('Ctrl Pts',(1.19426688731232,4.52434515927101,36.05));
#307890=CARTESIAN_POINT('Ctrl Pts',(1.27247800686959,4.49538915943629,36.05));
#307891=CARTESIAN_POINT('Ctrl Pts',(1.35393326291226,4.47372823681752,36.05));
#307892=CARTESIAN_POINT('Ctrl Pts',(1.43959848220332,4.46161006986558,36.05));
#307893=CARTESIAN_POINT('Ctrl Pts',(1.49790947590789,4.4597253240939,36.05));
#307894=CARTESIAN_POINT('Ctrl Pts',(1.52758218344156,4.45876623376623,36.05));
#307895=CARTESIAN_POINT('',(2.37094155844156,5.42196124188312,36.05));
#307896=CARTESIAN_POINT('Ctrl Pts',(1.52758218344156,4.45876623376623,36.05));
#307897=CARTESIAN_POINT('Ctrl Pts',(1.55682420860062,4.45973608112409,36.05));
#307898=CARTESIAN_POINT('Ctrl Pts',(1.61449027768335,4.46164864649648,36.05));
#307899=CARTESIAN_POINT('Ctrl Pts',(1.69931628629545,4.47370190759594,36.05));
#307900=CARTESIAN_POINT('Ctrl Pts',(1.78027605704376,4.49553589484458,36.05));
#307901=CARTESIAN_POINT('Ctrl Pts',(1.85820350335783,4.5241565808727,36.05));
#307902=CARTESIAN_POINT('Ctrl Pts',(1.93195013979453,4.56264762609262,36.05));
#307903=CARTESIAN_POINT('Ctrl Pts',(2.00171131208806,4.60935645208091,36.05));
#307904=CARTESIAN_POINT('Ctrl Pts',(2.06812897983805,4.66400945675856,36.05));
#307905=CARTESIAN_POINT('Ctrl Pts',(2.12995256471625,4.72672058470318,36.05));
#307906=CARTESIAN_POINT('Ctrl Pts',(2.18650804768952,4.79615096254107,36.05));
#307907=CARTESIAN_POINT('Ctrl Pts',(2.23640375626704,4.87078209602146,36.05));
#307908=CARTESIAN_POINT('Ctrl Pts',(2.27768357726726,4.95095791492866,36.05));
#307909=CARTESIAN_POINT('Ctrl Pts',(2.31216804403568,5.03559649057185,36.05));
#307910=CARTESIAN_POINT('Ctrl Pts',(2.33816283696992,5.12552781537341,36.05));
#307911=CARTESIAN_POINT('Ctrl Pts',(2.35792489966522,5.21999888881734,36.05));
#307912=CARTESIAN_POINT('Ctrl Pts',(2.36858230731467,5.31949010994648,36.05));
#307913=CARTESIAN_POINT('Ctrl Pts',(2.3701449621061,5.3873620729942,36.05));
#307914=CARTESIAN_POINT('Ctrl Pts',(2.37094155844156,5.42196124188312,36.05));
#307915=CARTESIAN_POINT('',(1.86518364448052,6.24212662337662,36.05));
#307916=CARTESIAN_POINT('Ctrl Pts',(2.37094155844156,5.42196124188312,36.05));
#307917=CARTESIAN_POINT('Ctrl Pts',(2.37065529854562,5.44731949788714,36.05));
#307918=CARTESIAN_POINT('Ctrl Pts',(2.3700963416033,5.4968345485113,36.05));
#307919=CARTESIAN_POINT('Ctrl Pts',(2.3632377280083,5.56952358146944,36.05));
#307920=CARTESIAN_POINT('Ctrl Pts',(2.35316409315178,5.63904690448481,36.05));
#307921=CARTESIAN_POINT('Ctrl Pts',(2.33892894507894,5.70553707456913,36.05));
#307922=CARTESIAN_POINT('Ctrl Pts',(2.32116828112027,5.76902496530642,36.05));
#307923=CARTESIAN_POINT('Ctrl Pts',(2.2981681398483,5.82909896870107,36.05));
#307924=CARTESIAN_POINT('Ctrl Pts',(2.27230135351232,5.88660676946342,36.05));
#307925=CARTESIAN_POINT('Ctrl Pts',(2.24084931578957,5.94000771696759,36.05));
#307926=CARTESIAN_POINT('Ctrl Pts',(2.20676901424551,5.99064810748104,36.05));
#307927=CARTESIAN_POINT('Ctrl Pts',(2.16876575254244,6.03778353402304,36.05));
#307928=CARTESIAN_POINT('Ctrl Pts',(2.1267784920286,6.08096773911451,36.05));
#307929=CARTESIAN_POINT('Ctrl Pts',(2.08131772978725,6.12033427680283,36.05));
#307930=CARTESIAN_POINT('Ctrl Pts',(2.03298084769892,6.1568243528457,36.05));
#307931=CARTESIAN_POINT('Ctrl Pts',(1.98032242249028,6.18887731351974,36.05));
#307932=CARTESIAN_POINT('Ctrl Pts',(1.92450419092778,6.21812962575333,36.05));
#307933=CARTESIAN_POINT('Ctrl Pts',(1.88508836452757,6.23407454786033,36.05));
#307934=CARTESIAN_POINT('Ctrl Pts',(1.86518364448052,6.24212662337662,36.05));
#307935=CARTESIAN_POINT('',(2.24724025974026,6.88253855519481,36.05));
#307936=CARTESIAN_POINT('Ctrl Pts',(1.86518364448052,6.24212662337662,36.05));
#307937=CARTESIAN_POINT('Ctrl Pts',(1.89580295974203,6.25752314612396,36.05));
#307938=CARTESIAN_POINT('Ctrl Pts',(1.95525430031729,6.28741747621295,36.05));
#307939=CARTESIAN_POINT('Ctrl Pts',(2.0335051920771,6.34678274879809,36.05));
#307940=CARTESIAN_POINT('Ctrl Pts',(2.10006334842617,6.41405772296989,36.05));
#307941=CARTESIAN_POINT('Ctrl Pts',(2.15426047894085,6.4907436496301,36.05));
#307942=CARTESIAN_POINT('Ctrl Pts',(2.19665909049132,6.57608978278239,36.05));
#307943=CARTESIAN_POINT('Ctrl Pts',(2.22577944098905,6.6705401244345,36.05));
#307944=CARTESIAN_POINT('Ctrl Pts',(2.24448509897141,6.77356208818653,36.05));
#307945=CARTESIAN_POINT('Ctrl Pts',(2.24629873402623,6.8452978442089,36.05));
#307946=CARTESIAN_POINT('Ctrl Pts',(2.24724025974026,6.88253855519481,36.05));
#307947=CARTESIAN_POINT('',(1.52242796266234,7.71623376623377,36.05));
#307948=CARTESIAN_POINT('Ctrl Pts',(2.24724025974026,6.88253855519481,36.05));
#307949=CARTESIAN_POINT('Ctrl Pts',(2.2466485766986,6.91241766550898,36.05));
#307950=CARTESIAN_POINT('Ctrl Pts',(2.24548752990423,6.97104879536392,36.05));
#307951=CARTESIAN_POINT('Ctrl Pts',(2.23556552441298,7.05701575208482,36.05));
#307952=CARTESIAN_POINT('Ctrl Pts',(2.21970139767277,7.13897358699381,36.05));
#307953=CARTESIAN_POINT('Ctrl Pts',(2.19706966642109,7.21661236790923,36.05));
#307954=CARTESIAN_POINT('Ctrl Pts',(2.16825091485445,7.29002627559583,36.05));
#307955=CARTESIAN_POINT('Ctrl Pts',(2.1315901628391,7.35843862911193,36.05));
#307956=CARTESIAN_POINT('Ctrl Pts',(2.08967670240967,7.42336185115535,36.05));
#307957=CARTESIAN_POINT('Ctrl Pts',(2.04159249935513,7.48362087256877,36.05));
#307958=CARTESIAN_POINT('Ctrl Pts',(1.98861539009419,7.53791001729144,36.05));
#307959=CARTESIAN_POINT('Ctrl Pts',(1.9318511217457,7.58560597597768,36.05));
#307960=CARTESIAN_POINT('Ctrl Pts',(1.87205683321845,7.62639783586101,36.05));
#307961=CARTESIAN_POINT('Ctrl Pts',(1.80849182787228,7.65953041457979,36.05));
#307962=CARTESIAN_POINT('Ctrl Pts',(1.74156530298064,7.68468886160549,36.05));
#307963=CARTESIAN_POINT('Ctrl Pts',(1.67138411132394,7.7027904588233,36.05));
#307964=CARTESIAN_POINT('Ctrl Pts',(1.59794752226823,7.71392449956901,36.05));
#307965=CARTESIAN_POINT('Ctrl Pts',(1.54780821610109,7.71545767890599,36.05));
#307966=CARTESIAN_POINT('Ctrl Pts',(1.52242796266234,7.71623376623377,36.05));
#307967=CARTESIAN_POINT('Ctrl Pts',(1.52242796266234,7.71623376623377,36.05));
#307968=CARTESIAN_POINT('Ctrl Pts',(1.49727230748502,7.71538504428939,36.05));
#307969=CARTESIAN_POINT('Ctrl Pts',(1.44761088404003,7.71370952681349,36.05));
#307970=CARTESIAN_POINT('Ctrl Pts',(1.37469868549749,7.7036309678914,36.05));
#307971=CARTESIAN_POINT('Ctrl Pts',(1.3051937479367,7.68533220871074,36.05));
#307972=CARTESIAN_POINT('Ctrl Pts',(1.23894018265463,7.65993643724945,36.05));
#307973=CARTESIAN_POINT('Ctrl Pts',(1.17567437498645,7.62785439831755,36.05));
#307974=CARTESIAN_POINT('Ctrl Pts',(1.11597817292345,7.58805917500155,36.05));
#307975=CARTESIAN_POINT('Ctrl Pts',(1.05972365886402,7.54133429965824,36.05));
#307976=CARTESIAN_POINT('Ctrl Pts',(1.00709172396245,7.48817807892744,36.05));
#307977=CARTESIAN_POINT('Ctrl Pts',(0.959667248194858,7.42884662646377,
36.05));
#307978=CARTESIAN_POINT('Ctrl Pts',(0.917480029442785,7.36527391878087,
36.05));
#307979=CARTESIAN_POINT('Ctrl Pts',(0.882914981130102,7.29688183752562,
36.05));
#307980=CARTESIAN_POINT('Ctrl Pts',(0.853271048234912,7.22519194306317,
36.05));
#307981=CARTESIAN_POINT('Ctrl Pts',(0.831843276752908,7.1485092997012,36.05));
#307982=CARTESIAN_POINT('Ctrl Pts',(0.815658223082562,7.06800054423278,
36.05));
#307983=CARTESIAN_POINT('Ctrl Pts',(0.805803713282925,6.98307391394772,
36.05));
#307984=CARTESIAN_POINT('Ctrl Pts',(0.804649087710329,6.92508712200564,
36.05));
#307985=CARTESIAN_POINT('Ctrl Pts',(0.804058441558442,6.89542410714286,
36.05));
#307986=CARTESIAN_POINT('Origin',(0.,0.,36.05));
#307987=CARTESIAN_POINT('',(-0.185551948051949,4.95357142857143,36.05));
#307988=CARTESIAN_POINT('',(-0.185551948051949,4.5,36.05));
#307989=CARTESIAN_POINT('',(-0.185551948051949,4.5,36.05));
#307990=CARTESIAN_POINT('',(0.144318181818181,4.5,36.05));
#307991=CARTESIAN_POINT('',(0.144318181818181,4.5,36.05));
#307992=CARTESIAN_POINT('',(0.144318181818181,4.95357142857143,36.05));
#307993=CARTESIAN_POINT('',(0.144318181818181,4.95357142857143,36.05));
#307994=CARTESIAN_POINT('',(-0.185551948051949,4.95357142857143,36.05));
#307995=CARTESIAN_POINT('Ctrl Pts',(-1.18611505681818,6.24212662337662,
36.05));
#307996=CARTESIAN_POINT('Ctrl Pts',(-1.18611505681818,6.24212662337662,
36.29));
#307997=CARTESIAN_POINT('Ctrl Pts',(-1.16621033677113,6.23407454786033,
36.05));
#307998=CARTESIAN_POINT('Ctrl Pts',(-1.16621033677113,6.23407454786033,
36.29));
#307999=CARTESIAN_POINT('Ctrl Pts',(-1.12679451037092,6.21812962575334,
36.05));
#308000=CARTESIAN_POINT('Ctrl Pts',(-1.12679451037092,6.21812962575334,
36.29));
#308001=CARTESIAN_POINT('Ctrl Pts',(-1.07097627880842,6.18887731351974,
36.05));
#308002=CARTESIAN_POINT('Ctrl Pts',(-1.07097627880842,6.18887731351974,
36.29));
#308003=CARTESIAN_POINT('Ctrl Pts',(-1.01831785359978,6.15682435284569,
36.05));
#308004=CARTESIAN_POINT('Ctrl Pts',(-1.01831785359978,6.15682435284569,
36.29));
#308005=CARTESIAN_POINT('Ctrl Pts',(-0.969980971511446,6.12033427680283,
36.05));
#308006=CARTESIAN_POINT('Ctrl Pts',(-0.969980971511446,6.12033427680283,
36.29));
#308007=CARTESIAN_POINT('Ctrl Pts',(-0.924520209270103,6.08096773911451,
36.05));
#308008=CARTESIAN_POINT('Ctrl Pts',(-0.924520209270103,6.08096773911451,
36.29));
#308009=CARTESIAN_POINT('Ctrl Pts',(-0.882532948756259,6.03778353402304,
36.05));
#308010=CARTESIAN_POINT('Ctrl Pts',(-0.882532948756259,6.03778353402304,
36.29));
#308011=CARTESIAN_POINT('Ctrl Pts',(-0.844529687053187,5.99064810748104,
36.05));
#308012=CARTESIAN_POINT('Ctrl Pts',(-0.844529687053187,5.99064810748104,
36.29));
#308013=CARTESIAN_POINT('Ctrl Pts',(-0.810449385509135,5.94000771696759,
36.05));
#308014=CARTESIAN_POINT('Ctrl Pts',(-0.810449385509135,5.94000771696759,
36.29));
#308015=CARTESIAN_POINT('Ctrl Pts',(-0.778997347786388,5.88660676946342,
36.05));
#308016=CARTESIAN_POINT('Ctrl Pts',(-0.778997347786388,5.88660676946342,
36.29));
#308017=CARTESIAN_POINT('Ctrl Pts',(-0.753130561450395,5.82909896870107,
36.05));
#308018=CARTESIAN_POINT('Ctrl Pts',(-0.753130561450395,5.82909896870107,
36.29));
#308019=CARTESIAN_POINT('Ctrl Pts',(-0.730130420178432,5.76902496530641,
36.05));
#308020=CARTESIAN_POINT('Ctrl Pts',(-0.730130420178432,5.76902496530641,
36.29));
#308021=CARTESIAN_POINT('Ctrl Pts',(-0.712369756219759,5.70553707456913,
36.05));
#308022=CARTESIAN_POINT('Ctrl Pts',(-0.712369756219759,5.70553707456913,
36.29));
#308023=CARTESIAN_POINT('Ctrl Pts',(-0.698134608146914,5.63904690448481,
36.05));
#308024=CARTESIAN_POINT('Ctrl Pts',(-0.698134608146914,5.63904690448481,
36.29));
#308025=CARTESIAN_POINT('Ctrl Pts',(-0.688060973290405,5.56952358146944,
36.05));
#308026=CARTESIAN_POINT('Ctrl Pts',(-0.688060973290405,5.56952358146944,
36.29));
#308027=CARTESIAN_POINT('Ctrl Pts',(-0.681202359695404,5.4968345485113,
36.05));
#308028=CARTESIAN_POINT('Ctrl Pts',(-0.681202359695404,5.4968345485113,
36.29));
#308029=CARTESIAN_POINT('Ctrl Pts',(-0.680643402753075,5.44731949788714,
36.05));
#308030=CARTESIAN_POINT('Ctrl Pts',(-0.680643402753075,5.44731949788714,
36.29));
#308031=CARTESIAN_POINT('Ctrl Pts',(-0.680357142857142,5.42196124188312,
36.05));
#308032=CARTESIAN_POINT('Ctrl Pts',(-0.680357142857142,5.42196124188312,
36.29));
#308033=CARTESIAN_POINT('',(-1.18611505681818,6.24212662337662,36.25));
#308034=CARTESIAN_POINT('',(-1.18611505681818,6.24212662337662,32.1799631621335));
#308035=CARTESIAN_POINT('',(-0.680357142857142,5.42196124188312,36.25));
#308036=CARTESIAN_POINT('',(-0.680357142857142,5.42196124188312,32.1799631621335));
#308037=CARTESIAN_POINT('Ctrl Pts',(-1.18611505681818,6.24212662337662,
36.25));
#308038=CARTESIAN_POINT('Ctrl Pts',(-1.16621033677113,6.23407454786033,
36.25));
#308039=CARTESIAN_POINT('Ctrl Pts',(-1.12679451037092,6.21812962575334,
36.25));
#308040=CARTESIAN_POINT('Ctrl Pts',(-1.07097627880842,6.18887731351974,
36.25));
#308041=CARTESIAN_POINT('Ctrl Pts',(-1.01831785359978,6.15682435284569,
36.25));
#308042=CARTESIAN_POINT('Ctrl Pts',(-0.969980971511446,6.12033427680283,
36.25));
#308043=CARTESIAN_POINT('Ctrl Pts',(-0.924520209270103,6.08096773911451,
36.25));
#308044=CARTESIAN_POINT('Ctrl Pts',(-0.882532948756259,6.03778353402304,
36.25));
#308045=CARTESIAN_POINT('Ctrl Pts',(-0.844529687053187,5.99064810748104,
36.25));
#308046=CARTESIAN_POINT('Ctrl Pts',(-0.810449385509135,5.94000771696759,
36.25));
#308047=CARTESIAN_POINT('Ctrl Pts',(-0.778997347786388,5.88660676946342,
36.25));
#308048=CARTESIAN_POINT('Ctrl Pts',(-0.753130561450395,5.82909896870107,
36.25));
#308049=CARTESIAN_POINT('Ctrl Pts',(-0.730130420178432,5.76902496530641,
36.25));
#308050=CARTESIAN_POINT('Ctrl Pts',(-0.712369756219759,5.70553707456913,
36.25));
#308051=CARTESIAN_POINT('Ctrl Pts',(-0.698134608146914,5.63904690448481,
36.25));
#308052=CARTESIAN_POINT('Ctrl Pts',(-0.688060973290405,5.56952358146944,
36.25));
#308053=CARTESIAN_POINT('Ctrl Pts',(-0.681202359695404,5.4968345485113,
36.25));
#308054=CARTESIAN_POINT('Ctrl Pts',(-0.680643402753075,5.44731949788714,
36.25));
#308055=CARTESIAN_POINT('Ctrl Pts',(-0.680357142857142,5.42196124188312,
36.25));
#308056=CARTESIAN_POINT('Ctrl Pts',(-0.804058441558441,6.88253855519481,
36.05));
#308057=CARTESIAN_POINT('Ctrl Pts',(-0.804058441558441,6.88253855519481,
36.29));
#308058=CARTESIAN_POINT('Ctrl Pts',(-0.804999967272473,6.8452978442089,
36.05));
#308059=CARTESIAN_POINT('Ctrl Pts',(-0.804999967272473,6.8452978442089,
36.29));
#308060=CARTESIAN_POINT('Ctrl Pts',(-0.806813602327297,6.77356208818653,
36.05));
#308061=CARTESIAN_POINT('Ctrl Pts',(-0.806813602327297,6.77356208818653,
36.29));
#308062=CARTESIAN_POINT('Ctrl Pts',(-0.825519260309656,6.6705401244345,
36.05));
#308063=CARTESIAN_POINT('Ctrl Pts',(-0.825519260309656,6.6705401244345,
36.29));
#308064=CARTESIAN_POINT('Ctrl Pts',(-0.854639610807379,6.57608978278239,
36.05));
#308065=CARTESIAN_POINT('Ctrl Pts',(-0.854639610807379,6.57608978278239,
36.29));
#308066=CARTESIAN_POINT('Ctrl Pts',(-0.897038222357849,6.4907436496301,
36.05));
#308067=CARTESIAN_POINT('Ctrl Pts',(-0.897038222357849,6.4907436496301,
36.29));
#308068=CARTESIAN_POINT('Ctrl Pts',(-0.951235352872532,6.41405772296989,
36.05));
#308069=CARTESIAN_POINT('Ctrl Pts',(-0.951235352872532,6.41405772296989,
36.29));
#308070=CARTESIAN_POINT('Ctrl Pts',(-1.0177935092216,6.34678274879809,36.05));
#308071=CARTESIAN_POINT('Ctrl Pts',(-1.0177935092216,6.34678274879809,36.29));
#308072=CARTESIAN_POINT('Ctrl Pts',(-1.09604440098142,6.28741747621295,
36.05));
#308073=CARTESIAN_POINT('Ctrl Pts',(-1.09604440098142,6.28741747621295,
36.29));
#308074=CARTESIAN_POINT('Ctrl Pts',(-1.15549574155667,6.25752314612396,
36.05));
#308075=CARTESIAN_POINT('Ctrl Pts',(-1.15549574155667,6.25752314612396,
36.29));
#308076=CARTESIAN_POINT('Ctrl Pts',(-1.18611505681818,6.24212662337662,
36.05));
#308077=CARTESIAN_POINT('Ctrl Pts',(-1.18611505681818,6.24212662337662,
36.29));
#308078=CARTESIAN_POINT('',(-0.804058441558441,6.88253855519481,36.25));
#308079=CARTESIAN_POINT('',(-0.804058441558441,6.88253855519481,32.1799631621335));
#308080=CARTESIAN_POINT('Ctrl Pts',(-0.804058441558441,6.88253855519481,
36.25));
#308081=CARTESIAN_POINT('Ctrl Pts',(-0.804999967272473,6.8452978442089,
36.25));
#308082=CARTESIAN_POINT('Ctrl Pts',(-0.806813602327297,6.77356208818653,
36.25));
#308083=CARTESIAN_POINT('Ctrl Pts',(-0.825519260309656,6.6705401244345,
36.25));
#308084=CARTESIAN_POINT('Ctrl Pts',(-0.854639610807379,6.57608978278239,
36.25));
#308085=CARTESIAN_POINT('Ctrl Pts',(-0.897038222357849,6.4907436496301,
36.25));
#308086=CARTESIAN_POINT('Ctrl Pts',(-0.951235352872532,6.41405772296989,
36.25));
#308087=CARTESIAN_POINT('Ctrl Pts',(-1.0177935092216,6.34678274879809,36.25));
#308088=CARTESIAN_POINT('Ctrl Pts',(-1.09604440098142,6.28741747621295,
36.25));
#308089=CARTESIAN_POINT('Ctrl Pts',(-1.15549574155667,6.25752314612396,
36.25));
#308090=CARTESIAN_POINT('Ctrl Pts',(-1.18611505681818,6.24212662337662,
36.25));
#308091=CARTESIAN_POINT('Ctrl Pts',(-1.52887073863637,7.71623376623377,
36.05));
#308092=CARTESIAN_POINT('Ctrl Pts',(-1.52887073863637,7.71623376623377,
36.29));
#308093=CARTESIAN_POINT('Ctrl Pts',(-1.50349048519761,7.71545767890599,
36.05));
#308094=CARTESIAN_POINT('Ctrl Pts',(-1.50349048519761,7.71545767890599,
36.29));
#308095=CARTESIAN_POINT('Ctrl Pts',(-1.45335117903047,7.71392449956901,
36.05));
#308096=CARTESIAN_POINT('Ctrl Pts',(-1.45335117903047,7.71392449956901,
36.29));
#308097=CARTESIAN_POINT('Ctrl Pts',(-1.37991458997475,7.7027904588233,36.05));
#308098=CARTESIAN_POINT('Ctrl Pts',(-1.37991458997475,7.7027904588233,36.29));
#308099=CARTESIAN_POINT('Ctrl Pts',(-1.30973339831807,7.68468886160549,
36.05));
#308100=CARTESIAN_POINT('Ctrl Pts',(-1.30973339831807,7.68468886160549,
36.29));
#308101=CARTESIAN_POINT('Ctrl Pts',(-1.24280687342643,7.65953041457979,
36.05));
#308102=CARTESIAN_POINT('Ctrl Pts',(-1.24280687342643,7.65953041457979,
36.29));
#308103=CARTESIAN_POINT('Ctrl Pts',(-1.17924186808025,7.62639783586101,
36.05));
#308104=CARTESIAN_POINT('Ctrl Pts',(-1.17924186808025,7.62639783586101,
36.29));
#308105=CARTESIAN_POINT('Ctrl Pts',(-1.119447579553,7.58560597597768,36.05));
#308106=CARTESIAN_POINT('Ctrl Pts',(-1.119447579553,7.58560597597768,36.29));
#308107=CARTESIAN_POINT('Ctrl Pts',(-1.06268331120451,7.53791001729144,
36.05));
#308108=CARTESIAN_POINT('Ctrl Pts',(-1.06268331120451,7.53791001729144,
36.29));
#308109=CARTESIAN_POINT('Ctrl Pts',(-1.00970620194357,7.48362087256877,
36.05));
#308110=CARTESIAN_POINT('Ctrl Pts',(-1.00970620194357,7.48362087256877,
36.29));
#308111=CARTESIAN_POINT('Ctrl Pts',(-0.961621998889034,7.42336185115535,
36.05));
#308112=CARTESIAN_POINT('Ctrl Pts',(-0.961621998889034,7.42336185115535,
36.29));
#308113=CARTESIAN_POINT('Ctrl Pts',(-0.919708538459593,7.35843862911193,
36.05));
#308114=CARTESIAN_POINT('Ctrl Pts',(-0.919708538459593,7.35843862911193,
36.29));
#308115=CARTESIAN_POINT('Ctrl Pts',(-0.883047786444258,7.29002627559583,
36.05));
#308116=CARTESIAN_POINT('Ctrl Pts',(-0.883047786444258,7.29002627559583,
36.29));
#308117=CARTESIAN_POINT('Ctrl Pts',(-0.854229034877609,7.21661236790923,
36.05));
#308118=CARTESIAN_POINT('Ctrl Pts',(-0.854229034877609,7.21661236790923,
36.29));
#308119=CARTESIAN_POINT('Ctrl Pts',(-0.831597303625935,7.13897358699381,
36.05));
#308120=CARTESIAN_POINT('Ctrl Pts',(-0.831597303625935,7.13897358699381,
36.29));
#308121=CARTESIAN_POINT('Ctrl Pts',(-0.815733176885725,7.05701575208482,
36.05));
#308122=CARTESIAN_POINT('Ctrl Pts',(-0.815733176885725,7.05701575208482,
36.29));
#308123=CARTESIAN_POINT('Ctrl Pts',(-0.805811171394462,6.97104879536392,
36.05));
#308124=CARTESIAN_POINT('Ctrl Pts',(-0.805811171394462,6.97104879536392,
36.29));
#308125=CARTESIAN_POINT('Ctrl Pts',(-0.804650124600102,6.91241766550898,
36.05));
#308126=CARTESIAN_POINT('Ctrl Pts',(-0.804650124600102,6.91241766550898,
36.29));
#308127=CARTESIAN_POINT('Ctrl Pts',(-0.804058441558441,6.88253855519481,
36.05));
#308128=CARTESIAN_POINT('Ctrl Pts',(-0.804058441558441,6.88253855519481,
36.29));
#308129=CARTESIAN_POINT('',(-1.52887073863637,7.71623376623377,36.25));
#308130=CARTESIAN_POINT('',(-1.52887073863637,7.71623376623377,32.1799631621335));
#308131=CARTESIAN_POINT('Ctrl Pts',(-1.52887073863637,7.71623376623377,
36.25));
#308132=CARTESIAN_POINT('Ctrl Pts',(-1.50349048519761,7.71545767890599,
36.25));
#308133=CARTESIAN_POINT('Ctrl Pts',(-1.45335117903047,7.71392449956901,
36.25));
#308134=CARTESIAN_POINT('Ctrl Pts',(-1.37991458997475,7.7027904588233,36.25));
#308135=CARTESIAN_POINT('Ctrl Pts',(-1.30973339831807,7.68468886160549,
36.25));
#308136=CARTESIAN_POINT('Ctrl Pts',(-1.24280687342643,7.65953041457979,
36.25));
#308137=CARTESIAN_POINT('Ctrl Pts',(-1.17924186808025,7.62639783586101,
36.25));
#308138=CARTESIAN_POINT('Ctrl Pts',(-1.119447579553,7.58560597597768,36.25));
#308139=CARTESIAN_POINT('Ctrl Pts',(-1.06268331120451,7.53791001729144,
36.25));
#308140=CARTESIAN_POINT('Ctrl Pts',(-1.00970620194357,7.48362087256877,
36.25));
#308141=CARTESIAN_POINT('Ctrl Pts',(-0.961621998889034,7.42336185115535,
36.25));
#308142=CARTESIAN_POINT('Ctrl Pts',(-0.919708538459593,7.35843862911193,
36.25));
#308143=CARTESIAN_POINT('Ctrl Pts',(-0.883047786444258,7.29002627559583,
36.25));
#308144=CARTESIAN_POINT('Ctrl Pts',(-0.854229034877609,7.21661236790923,
36.25));
#308145=CARTESIAN_POINT('Ctrl Pts',(-0.831597303625935,7.13897358699381,
36.25));
#308146=CARTESIAN_POINT('Ctrl Pts',(-0.815733176885725,7.05701575208482,
36.25));
#308147=CARTESIAN_POINT('Ctrl Pts',(-0.805811171394462,6.97104879536392,
36.25));
#308148=CARTESIAN_POINT('Ctrl Pts',(-0.804650124600102,6.91241766550898,
36.25));
#308149=CARTESIAN_POINT('Ctrl Pts',(-0.804058441558441,6.88253855519481,
36.25));
#308150=CARTESIAN_POINT('Ctrl Pts',(-2.24724025974026,6.89542410714286,
36.05));
#308151=CARTESIAN_POINT('Ctrl Pts',(-2.24724025974026,6.89542410714286,
36.29));
#308152=CARTESIAN_POINT('Ctrl Pts',(-2.24664961358837,6.92508712200564,
36.05));
#308153=CARTESIAN_POINT('Ctrl Pts',(-2.24664961358837,6.92508712200564,
36.29));
#308154=CARTESIAN_POINT('Ctrl Pts',(-2.24549498801578,6.98307391394772,
36.05));
#308155=CARTESIAN_POINT('Ctrl Pts',(-2.24549498801578,6.98307391394772,
36.29));
#308156=CARTESIAN_POINT('Ctrl Pts',(-2.23564047821614,7.06800054423278,
36.05));
#308157=CARTESIAN_POINT('Ctrl Pts',(-2.23564047821614,7.06800054423278,
36.29));
#308158=CARTESIAN_POINT('Ctrl Pts',(-2.2194554245458,7.1485092997012,36.05));
#308159=CARTESIAN_POINT('Ctrl Pts',(-2.2194554245458,7.1485092997012,36.29));
#308160=CARTESIAN_POINT('Ctrl Pts',(-2.19802765306379,7.22519194306317,
36.05));
#308161=CARTESIAN_POINT('Ctrl Pts',(-2.19802765306379,7.22519194306317,
36.29));
#308162=CARTESIAN_POINT('Ctrl Pts',(-2.1683837201686,7.29688183752562,36.05));
#308163=CARTESIAN_POINT('Ctrl Pts',(-2.1683837201686,7.29688183752562,36.29));
#308164=CARTESIAN_POINT('Ctrl Pts',(-2.13381867185592,7.36527391878087,
36.05));
#308165=CARTESIAN_POINT('Ctrl Pts',(-2.13381867185592,7.36527391878087,
36.29));
#308166=CARTESIAN_POINT('Ctrl Pts',(-2.09163145310384,7.42884662646377,
36.05));
#308167=CARTESIAN_POINT('Ctrl Pts',(-2.09163145310384,7.42884662646377,
36.29));
#308168=CARTESIAN_POINT('Ctrl Pts',(-2.04420697733625,7.48817807892744,
36.05));
#308169=CARTESIAN_POINT('Ctrl Pts',(-2.04420697733625,7.48817807892744,
36.29));
#308170=CARTESIAN_POINT('Ctrl Pts',(-1.99157504243468,7.54133429965825,
36.05));
#308171=CARTESIAN_POINT('Ctrl Pts',(-1.99157504243468,7.54133429965825,
36.29));
#308172=CARTESIAN_POINT('Ctrl Pts',(-1.93532052837525,7.58805917500155,
36.05));
#308173=CARTESIAN_POINT('Ctrl Pts',(-1.93532052837525,7.58805917500155,
36.29));
#308174=CARTESIAN_POINT('Ctrl Pts',(-1.87562432631225,7.62785439831755,
36.05));
#308175=CARTESIAN_POINT('Ctrl Pts',(-1.87562432631225,7.62785439831755,
36.29));
#308176=CARTESIAN_POINT('Ctrl Pts',(-1.81235851864406,7.65993643724945,
36.05));
#308177=CARTESIAN_POINT('Ctrl Pts',(-1.81235851864406,7.65993643724945,
36.29));
#308178=CARTESIAN_POINT('Ctrl Pts',(-1.746104953362,7.68533220871074,36.05));
#308179=CARTESIAN_POINT('Ctrl Pts',(-1.746104953362,7.68533220871074,36.29));
#308180=CARTESIAN_POINT('Ctrl Pts',(-1.67660001580121,7.7036309678914,36.05));
#308181=CARTESIAN_POINT('Ctrl Pts',(-1.67660001580121,7.7036309678914,36.29));
#308182=CARTESIAN_POINT('Ctrl Pts',(-1.60368781725867,7.71370952681349,
36.05));
#308183=CARTESIAN_POINT('Ctrl Pts',(-1.60368781725867,7.71370952681349,
36.29));
#308184=CARTESIAN_POINT('Ctrl Pts',(-1.55402639381368,7.71538504428939,
36.05));
#308185=CARTESIAN_POINT('Ctrl Pts',(-1.55402639381368,7.71538504428939,
36.29));
#308186=CARTESIAN_POINT('Ctrl Pts',(-1.52887073863637,7.71623376623377,
36.05));
#308187=CARTESIAN_POINT('Ctrl Pts',(-1.52887073863637,7.71623376623377,
36.29));
#308188=CARTESIAN_POINT('',(-2.24724025974026,6.89542410714286,36.25));
#308189=CARTESIAN_POINT('',(-2.24724025974026,6.89542410714286,32.1799631621335));
#308190=CARTESIAN_POINT('Ctrl Pts',(-2.24724025974026,6.89542410714286,
36.25));
#308191=CARTESIAN_POINT('Ctrl Pts',(-2.24664961358837,6.92508712200564,
36.25));
#308192=CARTESIAN_POINT('Ctrl Pts',(-2.24549498801578,6.98307391394772,
36.25));
#308193=CARTESIAN_POINT('Ctrl Pts',(-2.23564047821614,7.06800054423278,
36.25));
#308194=CARTESIAN_POINT('Ctrl Pts',(-2.2194554245458,7.1485092997012,36.25));
#308195=CARTESIAN_POINT('Ctrl Pts',(-2.19802765306379,7.22519194306317,
36.25));
#308196=CARTESIAN_POINT('Ctrl Pts',(-2.1683837201686,7.29688183752562,36.25));
#308197=CARTESIAN_POINT('Ctrl Pts',(-2.13381867185592,7.36527391878087,
36.25));
#308198=CARTESIAN_POINT('Ctrl Pts',(-2.09163145310384,7.42884662646377,
36.25));
#308199=CARTESIAN_POINT('Ctrl Pts',(-2.04420697733625,7.48817807892744,
36.25));
#308200=CARTESIAN_POINT('Ctrl Pts',(-1.99157504243468,7.54133429965825,
36.25));
#308201=CARTESIAN_POINT('Ctrl Pts',(-1.93532052837525,7.58805917500155,
36.25));
#308202=CARTESIAN_POINT('Ctrl Pts',(-1.87562432631225,7.62785439831755,
36.25));
#308203=CARTESIAN_POINT('Ctrl Pts',(-1.81235851864406,7.65993643724945,
36.25));
#308204=CARTESIAN_POINT('Ctrl Pts',(-1.746104953362,7.68533220871074,36.25));
#308205=CARTESIAN_POINT('Ctrl Pts',(-1.67660001580121,7.7036309678914,36.25));
#308206=CARTESIAN_POINT('Ctrl Pts',(-1.60368781725867,7.71370952681349,
36.25));
#308207=CARTESIAN_POINT('Ctrl Pts',(-1.55402639381368,7.71538504428939,
36.25));
#308208=CARTESIAN_POINT('Ctrl Pts',(-1.52887073863637,7.71623376623377,
36.25));
#308209=CARTESIAN_POINT('Ctrl Pts',(-1.86131797889611,6.24212662337662,
36.05));
#308210=CARTESIAN_POINT('Ctrl Pts',(-1.86131797889611,6.24212662337662,
36.29));
#308211=CARTESIAN_POINT('Ctrl Pts',(-1.89166914263337,6.25737900558171,
36.05));
#308212=CARTESIAN_POINT('Ctrl Pts',(-1.89166914263337,6.25737900558171,
36.29));
#308213=CARTESIAN_POINT('Ctrl Pts',(-1.95088478291998,6.28713666449684,
36.05));
#308214=CARTESIAN_POINT('Ctrl Pts',(-1.95088478291998,6.28713666449684,
36.29));
#308215=CARTESIAN_POINT('Ctrl Pts',(-2.02981249733957,6.34542328474194,
36.05));
#308216=CARTESIAN_POINT('Ctrl Pts',(-2.02981249733957,6.34542328474194,
36.29));
#308217=CARTESIAN_POINT('Ctrl Pts',(-2.09711468722833,6.41311300974787,
36.05));
#308218=CARTESIAN_POINT('Ctrl Pts',(-2.09711468722833,6.41311300974787,
36.29));
#308219=CARTESIAN_POINT('Ctrl Pts',(-2.15255407155767,6.49069341485485,
36.05));
#308220=CARTESIAN_POINT('Ctrl Pts',(-2.15255407155767,6.49069341485485,
36.29));
#308221=CARTESIAN_POINT('Ctrl Pts',(-2.19544755091121,6.57824013430206,
36.05));
#308222=CARTESIAN_POINT('Ctrl Pts',(-2.19544755091121,6.57824013430206,
36.29));
#308223=CARTESIAN_POINT('Ctrl Pts',(-2.22526998846174,6.67544579213543,
36.05));
#308224=CARTESIAN_POINT('Ctrl Pts',(-2.22526998846174,6.67544579213543,
36.29));
#308225=CARTESIAN_POINT('Ctrl Pts',(-2.24466128369114,6.78212192154818,
36.05));
#308226=CARTESIAN_POINT('Ctrl Pts',(-2.24466128369114,6.78212192154818,
36.29));
#308227=CARTESIAN_POINT('Ctrl Pts',(-2.24635828463311,6.85667628421743,
36.05));
#308228=CARTESIAN_POINT('Ctrl Pts',(-2.24635828463311,6.85667628421743,
36.29));
#308229=CARTESIAN_POINT('Ctrl Pts',(-2.24724025974026,6.89542410714286,
36.05));
#308230=CARTESIAN_POINT('Ctrl Pts',(-2.24724025974026,6.89542410714286,
36.29));
#308231=CARTESIAN_POINT('',(-1.86131797889611,6.24212662337662,36.25));
#308232=CARTESIAN_POINT('',(-1.86131797889611,6.24212662337662,32.1799631621335));
#308233=CARTESIAN_POINT('Ctrl Pts',(-1.86131797889611,6.24212662337662,
36.25));
#308234=CARTESIAN_POINT('Ctrl Pts',(-1.89166914263337,6.25737900558171,
36.25));
#308235=CARTESIAN_POINT('Ctrl Pts',(-1.95088478291998,6.28713666449684,
36.25));
#308236=CARTESIAN_POINT('Ctrl Pts',(-2.02981249733957,6.34542328474194,
36.25));
#308237=CARTESIAN_POINT('Ctrl Pts',(-2.09711468722833,6.41311300974787,
36.25));
#308238=CARTESIAN_POINT('Ctrl Pts',(-2.15255407155767,6.49069341485485,
36.25));
#308239=CARTESIAN_POINT('Ctrl Pts',(-2.19544755091121,6.57824013430206,
36.25));
#308240=CARTESIAN_POINT('Ctrl Pts',(-2.22526998846174,6.67544579213543,
36.25));
#308241=CARTESIAN_POINT('Ctrl Pts',(-2.24466128369114,6.78212192154818,
36.25));
#308242=CARTESIAN_POINT('Ctrl Pts',(-2.24635828463311,6.85667628421743,
36.25));
#308243=CARTESIAN_POINT('Ctrl Pts',(-2.24724025974026,6.89542410714286,
36.25));
#308244=CARTESIAN_POINT('Ctrl Pts',(-2.37094155844156,5.43291396103896,
36.05));
#308245=CARTESIAN_POINT('Ctrl Pts',(-2.37094155844156,5.43291396103896,
36.29));
#308246=CARTESIAN_POINT('Ctrl Pts',(-2.37063000734488,5.45891313799848,
36.05));
#308247=CARTESIAN_POINT('Ctrl Pts',(-2.37063000734488,5.45891313799848,
36.29));
#308248=CARTESIAN_POINT('Ctrl Pts',(-2.37001876348768,5.50992190470655,
36.05));
#308249=CARTESIAN_POINT('Ctrl Pts',(-2.37001876348768,5.50992190470655,
36.29));
#308250=CARTESIAN_POINT('Ctrl Pts',(-2.36345937406549,5.58482539360676,
36.05));
#308251=CARTESIAN_POINT('Ctrl Pts',(-2.36345937406549,5.58482539360676,
36.29));
#308252=CARTESIAN_POINT('Ctrl Pts',(-2.35252585809151,5.65624108672131,
36.05));
#308253=CARTESIAN_POINT('Ctrl Pts',(-2.35252585809151,5.65624108672131,
36.29));
#308254=CARTESIAN_POINT('Ctrl Pts',(-2.33776644819188,5.72405509656198,
36.05));
#308255=CARTESIAN_POINT('Ctrl Pts',(-2.33776644819188,5.72405509656198,
36.29));
#308256=CARTESIAN_POINT('Ctrl Pts',(-2.31914738800462,5.78833295550162,
36.05));
#308257=CARTESIAN_POINT('Ctrl Pts',(-2.31914738800462,5.78833295550162,
36.29));
#308258=CARTESIAN_POINT('Ctrl Pts',(-2.29590420953425,5.84911895337204,
36.05));
#308259=CARTESIAN_POINT('Ctrl Pts',(-2.29590420953425,5.84911895337204,
36.29));
#308260=CARTESIAN_POINT('Ctrl Pts',(-2.26824051996169,5.90641132135784,
36.05));
#308261=CARTESIAN_POINT('Ctrl Pts',(-2.26824051996169,5.90641132135784,
36.29));
#308262=CARTESIAN_POINT('Ctrl Pts',(-2.23643083441821,5.96019951630268,
36.05));
#308263=CARTESIAN_POINT('Ctrl Pts',(-2.23643083441821,5.96019951630268,
36.29));
#308264=CARTESIAN_POINT('Ctrl Pts',(-2.20124132093025,6.01030469320115,
36.05));
#308265=CARTESIAN_POINT('Ctrl Pts',(-2.20124132093025,6.01030469320115,
36.29));
#308266=CARTESIAN_POINT('Ctrl Pts',(-2.16248925313098,6.05629105732706,
36.05));
#308267=CARTESIAN_POINT('Ctrl Pts',(-2.16248925313098,6.05629105732706,
36.29));
#308268=CARTESIAN_POINT('Ctrl Pts',(-2.1202782797022,6.09774166415627,36.05));
#308269=CARTESIAN_POINT('Ctrl Pts',(-2.1202782797022,6.09774166415627,36.29));
#308270=CARTESIAN_POINT('Ctrl Pts',(-2.07499444571376,6.1351992195304,36.05));
#308271=CARTESIAN_POINT('Ctrl Pts',(-2.07499444571376,6.1351992195304,36.29));
#308272=CARTESIAN_POINT('Ctrl Pts',(-2.02656583006182,6.16910978501208,
36.05));
#308273=CARTESIAN_POINT('Ctrl Pts',(-2.02656583006182,6.16910978501208,
36.29));
#308274=CARTESIAN_POINT('Ctrl Pts',(-1.97432962905344,6.19776979492405,
36.05));
#308275=CARTESIAN_POINT('Ctrl Pts',(-1.97432962905344,6.19776979492405,
36.29));
#308276=CARTESIAN_POINT('Ctrl Pts',(-1.91917711253447,6.22263196745495,
36.05));
#308277=CARTESIAN_POINT('Ctrl Pts',(-1.91917711253447,6.22263196745495,
36.29));
#308278=CARTESIAN_POINT('Ctrl Pts',(-1.88076808190029,6.23557324032603,
36.05));
#308279=CARTESIAN_POINT('Ctrl Pts',(-1.88076808190029,6.23557324032603,
36.29));
#308280=CARTESIAN_POINT('Ctrl Pts',(-1.86131797889611,6.24212662337662,
36.05));
#308281=CARTESIAN_POINT('Ctrl Pts',(-1.86131797889611,6.24212662337662,
36.29));
#308282=CARTESIAN_POINT('',(-2.37094155844156,5.43291396103896,36.25));
#308283=CARTESIAN_POINT('',(-2.37094155844156,5.43291396103896,32.1799631621335));
#308284=CARTESIAN_POINT('Ctrl Pts',(-2.37094155844156,5.43291396103896,
36.25));
#308285=CARTESIAN_POINT('Ctrl Pts',(-2.37063000734488,5.45891313799848,
36.25));
#308286=CARTESIAN_POINT('Ctrl Pts',(-2.37001876348768,5.50992190470655,
36.25));
#308287=CARTESIAN_POINT('Ctrl Pts',(-2.36345937406549,5.58482539360676,
36.25));
#308288=CARTESIAN_POINT('Ctrl Pts',(-2.35252585809151,5.65624108672131,
36.25));
#308289=CARTESIAN_POINT('Ctrl Pts',(-2.33776644819188,5.72405509656198,
36.25));
#308290=CARTESIAN_POINT('Ctrl Pts',(-2.31914738800462,5.78833295550162,
36.25));
#308291=CARTESIAN_POINT('Ctrl Pts',(-2.29590420953425,5.84911895337204,
36.25));
#308292=CARTESIAN_POINT('Ctrl Pts',(-2.26824051996169,5.90641132135784,
36.25));
#308293=CARTESIAN_POINT('Ctrl Pts',(-2.23643083441821,5.96019951630268,
36.25));
#308294=CARTESIAN_POINT('Ctrl Pts',(-2.20124132093025,6.01030469320115,
36.25));
#308295=CARTESIAN_POINT('Ctrl Pts',(-2.16248925313098,6.05629105732706,
36.25));
#308296=CARTESIAN_POINT('Ctrl Pts',(-2.1202782797022,6.09774166415627,36.25));
#308297=CARTESIAN_POINT('Ctrl Pts',(-2.07499444571376,6.1351992195304,36.25));
#308298=CARTESIAN_POINT('Ctrl Pts',(-2.02656583006182,6.16910978501208,
36.25));
#308299=CARTESIAN_POINT('Ctrl Pts',(-1.97432962905344,6.19776979492405,
36.25));
#308300=CARTESIAN_POINT('Ctrl Pts',(-1.91917711253447,6.22263196745495,
36.25));
#308301=CARTESIAN_POINT('Ctrl Pts',(-1.88076808190029,6.23557324032603,
36.25));
#308302=CARTESIAN_POINT('Ctrl Pts',(-1.86131797889611,6.24212662337662,
36.25));
#308303=CARTESIAN_POINT('Ctrl Pts',(-1.52371651785714,4.45876623376623,
36.05));
#308304=CARTESIAN_POINT('Ctrl Pts',(-1.52371651785714,4.45876623376623,
36.29));
#308305=CARTESIAN_POINT('Ctrl Pts',(-1.55338922539081,4.4597253240939,36.05));
#308306=CARTESIAN_POINT('Ctrl Pts',(-1.55338922539081,4.4597253240939,36.29));
#308307=CARTESIAN_POINT('Ctrl Pts',(-1.61170021909538,4.46161006986558,
36.05));
#308308=CARTESIAN_POINT('Ctrl Pts',(-1.61170021909538,4.46161006986558,
36.29));
#308309=CARTESIAN_POINT('Ctrl Pts',(-1.69736543838644,4.47372823681752,
36.05));
#308310=CARTESIAN_POINT('Ctrl Pts',(-1.69736543838644,4.47372823681752,
36.29));
#308311=CARTESIAN_POINT('Ctrl Pts',(-1.77882069442911,4.49538915943629,
36.05));
#308312=CARTESIAN_POINT('Ctrl Pts',(-1.77882069442911,4.49538915943629,
36.29));
#308313=CARTESIAN_POINT('Ctrl Pts',(-1.85703181398638,4.52434515927101,
36.05));
#308314=CARTESIAN_POINT('Ctrl Pts',(-1.85703181398638,4.52434515927101,
36.29));
#308315=CARTESIAN_POINT('Ctrl Pts',(-1.93122097549665,4.56241550483758,
36.05));
#308316=CARTESIAN_POINT('Ctrl Pts',(-1.93122097549665,4.56241550483758,
36.29));
#308317=CARTESIAN_POINT('Ctrl Pts',(-2.00109150543013,4.60959489382438,
36.05));
#308318=CARTESIAN_POINT('Ctrl Pts',(-2.00109150543013,4.60959489382438,
36.29));
#308319=CARTESIAN_POINT('Ctrl Pts',(-2.06813219984915,4.66375358613811,
36.05));
#308320=CARTESIAN_POINT('Ctrl Pts',(-2.06813219984915,4.66375358613811,
36.29));
#308321=CARTESIAN_POINT('Ctrl Pts',(-2.1298438000822,4.72680658155488,36.05));
#308322=CARTESIAN_POINT('Ctrl Pts',(-2.1298438000822,4.72680658155488,36.29));
#308323=CARTESIAN_POINT('Ctrl Pts',(-2.18686174567011,4.79599402074389,
36.05));
#308324=CARTESIAN_POINT('Ctrl Pts',(-2.18686174567011,4.79599402074389,
36.29));
#308325=CARTESIAN_POINT('Ctrl Pts',(-2.2354792856985,4.87186228483585,36.05));
#308326=CARTESIAN_POINT('Ctrl Pts',(-2.2354792856985,4.87186228483585,36.29));
#308327=CARTESIAN_POINT('Ctrl Pts',(-2.27806144254569,4.95218254596678,
36.05));
#308328=CARTESIAN_POINT('Ctrl Pts',(-2.27806144254569,4.95218254596678,
36.29));
#308329=CARTESIAN_POINT('Ctrl Pts',(-2.31200320040195,5.03825698338498,
36.05));
#308330=CARTESIAN_POINT('Ctrl Pts',(-2.31200320040195,5.03825698338498,
36.29));
#308331=CARTESIAN_POINT('Ctrl Pts',(-2.33853623055972,5.12949961741785,
36.05));
#308332=CARTESIAN_POINT('Ctrl Pts',(-2.33853623055972,5.12949961741785,
36.29));
#308333=CARTESIAN_POINT('Ctrl Pts',(-2.35686977721559,5.22616336292247,
36.05));
#308334=CARTESIAN_POINT('Ctrl Pts',(-2.35686977721559,5.22616336292247,
36.29));
#308335=CARTESIAN_POINT('Ctrl Pts',(-2.36886427906175,5.32781045016027,
36.05));
#308336=CARTESIAN_POINT('Ctrl Pts',(-2.36886427906175,5.32781045016027,
36.29));
#308337=CARTESIAN_POINT('Ctrl Pts',(-2.37024051692734,5.39744356397404,
36.05));
#308338=CARTESIAN_POINT('Ctrl Pts',(-2.37024051692734,5.39744356397404,
36.29));
#308339=CARTESIAN_POINT('Ctrl Pts',(-2.37094155844156,5.43291396103896,
36.05));
#308340=CARTESIAN_POINT('Ctrl Pts',(-2.37094155844156,5.43291396103896,
36.29));
#308341=CARTESIAN_POINT('',(-1.52371651785714,4.45876623376623,36.25));
#308342=CARTESIAN_POINT('',(-1.52371651785714,4.45876623376623,32.1799631621335));
#308343=CARTESIAN_POINT('Ctrl Pts',(-1.52371651785714,4.45876623376623,
36.25));
#308344=CARTESIAN_POINT('Ctrl Pts',(-1.55338922539081,4.4597253240939,36.25));
#308345=CARTESIAN_POINT('Ctrl Pts',(-1.61170021909538,4.46161006986558,
36.25));
#308346=CARTESIAN_POINT('Ctrl Pts',(-1.69736543838644,4.47372823681752,
36.25));
#308347=CARTESIAN_POINT('Ctrl Pts',(-1.77882069442911,4.49538915943629,
36.25));
#308348=CARTESIAN_POINT('Ctrl Pts',(-1.85703181398638,4.52434515927101,
36.25));
#308349=CARTESIAN_POINT('Ctrl Pts',(-1.93122097549665,4.56241550483758,
36.25));
#308350=CARTESIAN_POINT('Ctrl Pts',(-2.00109150543013,4.60959489382438,
36.25));
#308351=CARTESIAN_POINT('Ctrl Pts',(-2.06813219984915,4.66375358613811,
36.25));
#308352=CARTESIAN_POINT('Ctrl Pts',(-2.1298438000822,4.72680658155488,36.25));
#308353=CARTESIAN_POINT('Ctrl Pts',(-2.18686174567011,4.79599402074389,
36.25));
#308354=CARTESIAN_POINT('Ctrl Pts',(-2.2354792856985,4.87186228483585,36.25));
#308355=CARTESIAN_POINT('Ctrl Pts',(-2.27806144254569,4.95218254596678,
36.25));
#308356=CARTESIAN_POINT('Ctrl Pts',(-2.31200320040195,5.03825698338498,
36.25));
#308357=CARTESIAN_POINT('Ctrl Pts',(-2.33853623055972,5.12949961741785,
36.25));
#308358=CARTESIAN_POINT('Ctrl Pts',(-2.35686977721559,5.22616336292247,
36.25));
#308359=CARTESIAN_POINT('Ctrl Pts',(-2.36886427906175,5.32781045016027,
36.25));
#308360=CARTESIAN_POINT('Ctrl Pts',(-2.37024051692734,5.39744356397404,
36.25));
#308361=CARTESIAN_POINT('Ctrl Pts',(-2.37094155844156,5.43291396103896,
36.25));
#308362=CARTESIAN_POINT('Ctrl Pts',(-0.680357142857142,5.42196124188312,
36.05));
#308363=CARTESIAN_POINT('Ctrl Pts',(-0.680357142857142,5.42196124188312,
36.29));
#308364=CARTESIAN_POINT('Ctrl Pts',(-0.681153739192598,5.3873620729942,
36.05));
#308365=CARTESIAN_POINT('Ctrl Pts',(-0.681153739192598,5.3873620729942,
36.29));
#308366=CARTESIAN_POINT('Ctrl Pts',(-0.682716393984036,5.31949010994648,
36.05));
#308367=CARTESIAN_POINT('Ctrl Pts',(-0.682716393984036,5.31949010994648,
36.29));
#308368=CARTESIAN_POINT('Ctrl Pts',(-0.693373801633478,5.21999888881734,
36.05));
#308369=CARTESIAN_POINT('Ctrl Pts',(-0.693373801633478,5.21999888881734,
36.29));
#308370=CARTESIAN_POINT('Ctrl Pts',(-0.713135864328774,5.12552781537341,
36.05));
#308371=CARTESIAN_POINT('Ctrl Pts',(-0.713135864328774,5.12552781537341,
36.29));
#308372=CARTESIAN_POINT('Ctrl Pts',(-0.739130657263025,5.03559649057185,
36.05));
#308373=CARTESIAN_POINT('Ctrl Pts',(-0.739130657263025,5.03559649057185,
36.29));
#308374=CARTESIAN_POINT('Ctrl Pts',(-0.773615124031434,4.95095791492866,
36.05));
#308375=CARTESIAN_POINT('Ctrl Pts',(-0.773615124031434,4.95095791492866,
36.29));
#308376=CARTESIAN_POINT('Ctrl Pts',(-0.814894945031659,4.87078209602146,
36.05));
#308377=CARTESIAN_POINT('Ctrl Pts',(-0.814894945031659,4.87078209602146,
36.29));
#308378=CARTESIAN_POINT('Ctrl Pts',(-0.864790653609182,4.79615096254107,
36.05));
#308379=CARTESIAN_POINT('Ctrl Pts',(-0.864790653609182,4.79615096254107,
36.29));
#308380=CARTESIAN_POINT('Ctrl Pts',(-0.921346136582458,4.72672058470318,
36.05));
#308381=CARTESIAN_POINT('Ctrl Pts',(-0.921346136582458,4.72672058470318,
36.29));
#308382=CARTESIAN_POINT('Ctrl Pts',(-0.983169721460654,4.66400945675856,
36.05));
#308383=CARTESIAN_POINT('Ctrl Pts',(-0.983169721460654,4.66400945675856,
36.29));
#308384=CARTESIAN_POINT('Ctrl Pts',(-1.04958738921064,4.60935645208091,
36.05));
#308385=CARTESIAN_POINT('Ctrl Pts',(-1.04958738921064,4.60935645208091,
36.29));
#308386=CARTESIAN_POINT('Ctrl Pts',(-1.11934856150417,4.56264762609262,
36.05));
#308387=CARTESIAN_POINT('Ctrl Pts',(-1.11934856150417,4.56264762609262,
36.29));
#308388=CARTESIAN_POINT('Ctrl Pts',(-1.19309519794087,4.5241565808727,36.05));
#308389=CARTESIAN_POINT('Ctrl Pts',(-1.19309519794087,4.5241565808727,36.29));
#308390=CARTESIAN_POINT('Ctrl Pts',(-1.27102264425494,4.49553589484458,
36.05));
#308391=CARTESIAN_POINT('Ctrl Pts',(-1.27102264425494,4.49553589484458,
36.29));
#308392=CARTESIAN_POINT('Ctrl Pts',(-1.35198241500324,4.47370190759594,
36.05));
#308393=CARTESIAN_POINT('Ctrl Pts',(-1.35198241500324,4.47370190759594,
36.29));
#308394=CARTESIAN_POINT('Ctrl Pts',(-1.43680842361535,4.46164864649648,
36.05));
#308395=CARTESIAN_POINT('Ctrl Pts',(-1.43680842361535,4.46164864649648,
36.29));
#308396=CARTESIAN_POINT('Ctrl Pts',(-1.49447449269809,4.45973608112409,
36.05));
#308397=CARTESIAN_POINT('Ctrl Pts',(-1.49447449269809,4.45973608112409,
36.29));
#308398=CARTESIAN_POINT('Ctrl Pts',(-1.52371651785714,4.45876623376623,
36.05));
#308399=CARTESIAN_POINT('Ctrl Pts',(-1.52371651785714,4.45876623376623,
36.29));
#308400=CARTESIAN_POINT('Ctrl Pts',(-0.680357142857142,5.42196124188312,
36.25));
#308401=CARTESIAN_POINT('Ctrl Pts',(-0.681153739192598,5.3873620729942,
36.25));
#308402=CARTESIAN_POINT('Ctrl Pts',(-0.682716393984036,5.31949010994648,
36.25));
#308403=CARTESIAN_POINT('Ctrl Pts',(-0.693373801633478,5.21999888881734,
36.25));
#308404=CARTESIAN_POINT('Ctrl Pts',(-0.713135864328774,5.12552781537341,
36.25));
#308405=CARTESIAN_POINT('Ctrl Pts',(-0.739130657263025,5.03559649057185,
36.25));
#308406=CARTESIAN_POINT('Ctrl Pts',(-0.773615124031434,4.95095791492866,
36.25));
#308407=CARTESIAN_POINT('Ctrl Pts',(-0.814894945031659,4.87078209602146,
36.25));
#308408=CARTESIAN_POINT('Ctrl Pts',(-0.864790653609182,4.79615096254107,
36.25));
#308409=CARTESIAN_POINT('Ctrl Pts',(-0.921346136582458,4.72672058470318,
36.25));
#308410=CARTESIAN_POINT('Ctrl Pts',(-0.983169721460654,4.66400945675856,
36.25));
#308411=CARTESIAN_POINT('Ctrl Pts',(-1.04958738921064,4.60935645208091,
36.25));
#308412=CARTESIAN_POINT('Ctrl Pts',(-1.11934856150417,4.56264762609262,
36.25));
#308413=CARTESIAN_POINT('Ctrl Pts',(-1.19309519794087,4.5241565808727,36.25));
#308414=CARTESIAN_POINT('Ctrl Pts',(-1.27102264425494,4.49553589484458,
36.25));
#308415=CARTESIAN_POINT('Ctrl Pts',(-1.35198241500324,4.47370190759594,
36.25));
#308416=CARTESIAN_POINT('Ctrl Pts',(-1.43680842361535,4.46164864649648,
36.25));
#308417=CARTESIAN_POINT('Ctrl Pts',(-1.49447449269809,4.45973608112409,
36.25));
#308418=CARTESIAN_POINT('Ctrl Pts',(-1.52371651785714,4.45876623376623,
36.25));
#308419=CARTESIAN_POINT('Ctrl Pts',(1.86518364448052,6.24212662337662,36.05));
#308420=CARTESIAN_POINT('Ctrl Pts',(1.86518364448052,6.24212662337662,36.29));
#308421=CARTESIAN_POINT('Ctrl Pts',(1.88508836452757,6.23407454786033,36.05));
#308422=CARTESIAN_POINT('Ctrl Pts',(1.88508836452757,6.23407454786033,36.29));
#308423=CARTESIAN_POINT('Ctrl Pts',(1.92450419092778,6.21812962575333,36.05));
#308424=CARTESIAN_POINT('Ctrl Pts',(1.92450419092778,6.21812962575333,36.29));
#308425=CARTESIAN_POINT('Ctrl Pts',(1.98032242249028,6.18887731351974,36.05));
#308426=CARTESIAN_POINT('Ctrl Pts',(1.98032242249028,6.18887731351974,36.29));
#308427=CARTESIAN_POINT('Ctrl Pts',(2.03298084769892,6.1568243528457,36.05));
#308428=CARTESIAN_POINT('Ctrl Pts',(2.03298084769892,6.1568243528457,36.29));
#308429=CARTESIAN_POINT('Ctrl Pts',(2.08131772978725,6.12033427680283,36.05));
#308430=CARTESIAN_POINT('Ctrl Pts',(2.08131772978725,6.12033427680283,36.29));
#308431=CARTESIAN_POINT('Ctrl Pts',(2.1267784920286,6.08096773911451,36.05));
#308432=CARTESIAN_POINT('Ctrl Pts',(2.1267784920286,6.08096773911451,36.29));
#308433=CARTESIAN_POINT('Ctrl Pts',(2.16876575254244,6.03778353402304,36.05));
#308434=CARTESIAN_POINT('Ctrl Pts',(2.16876575254244,6.03778353402304,36.29));
#308435=CARTESIAN_POINT('Ctrl Pts',(2.20676901424551,5.99064810748104,36.05));
#308436=CARTESIAN_POINT('Ctrl Pts',(2.20676901424551,5.99064810748104,36.29));
#308437=CARTESIAN_POINT('Ctrl Pts',(2.24084931578957,5.94000771696759,36.05));
#308438=CARTESIAN_POINT('Ctrl Pts',(2.24084931578957,5.94000771696759,36.29));
#308439=CARTESIAN_POINT('Ctrl Pts',(2.27230135351232,5.88660676946342,36.05));
#308440=CARTESIAN_POINT('Ctrl Pts',(2.27230135351232,5.88660676946342,36.29));
#308441=CARTESIAN_POINT('Ctrl Pts',(2.2981681398483,5.82909896870107,36.05));
#308442=CARTESIAN_POINT('Ctrl Pts',(2.2981681398483,5.82909896870107,36.29));
#308443=CARTESIAN_POINT('Ctrl Pts',(2.32116828112027,5.76902496530642,36.05));
#308444=CARTESIAN_POINT('Ctrl Pts',(2.32116828112027,5.76902496530642,36.29));
#308445=CARTESIAN_POINT('Ctrl Pts',(2.33892894507894,5.70553707456913,36.05));
#308446=CARTESIAN_POINT('Ctrl Pts',(2.33892894507894,5.70553707456913,36.29));
#308447=CARTESIAN_POINT('Ctrl Pts',(2.35316409315178,5.63904690448481,36.05));
#308448=CARTESIAN_POINT('Ctrl Pts',(2.35316409315178,5.63904690448481,36.29));
#308449=CARTESIAN_POINT('Ctrl Pts',(2.3632377280083,5.56952358146944,36.05));
#308450=CARTESIAN_POINT('Ctrl Pts',(2.3632377280083,5.56952358146944,36.29));
#308451=CARTESIAN_POINT('Ctrl Pts',(2.3700963416033,5.4968345485113,36.05));
#308452=CARTESIAN_POINT('Ctrl Pts',(2.3700963416033,5.4968345485113,36.29));
#308453=CARTESIAN_POINT('Ctrl Pts',(2.37065529854562,5.44731949788714,36.05));
#308454=CARTESIAN_POINT('Ctrl Pts',(2.37065529854562,5.44731949788714,36.29));
#308455=CARTESIAN_POINT('Ctrl Pts',(2.37094155844156,5.42196124188312,36.05));
#308456=CARTESIAN_POINT('Ctrl Pts',(2.37094155844156,5.42196124188312,36.29));
#308457=CARTESIAN_POINT('',(1.86518364448052,6.24212662337662,36.25));
#308458=CARTESIAN_POINT('',(1.86518364448052,6.24212662337662,32.1799631621335));
#308459=CARTESIAN_POINT('',(2.37094155844156,5.42196124188312,36.25));
#308460=CARTESIAN_POINT('',(2.37094155844156,5.42196124188312,32.1799631621335));
#308461=CARTESIAN_POINT('Ctrl Pts',(1.86518364448052,6.24212662337662,36.25));
#308462=CARTESIAN_POINT('Ctrl Pts',(1.88508836452757,6.23407454786033,36.25));
#308463=CARTESIAN_POINT('Ctrl Pts',(1.92450419092778,6.21812962575333,36.25));
#308464=CARTESIAN_POINT('Ctrl Pts',(1.98032242249028,6.18887731351974,36.25));
#308465=CARTESIAN_POINT('Ctrl Pts',(2.03298084769892,6.1568243528457,36.25));
#308466=CARTESIAN_POINT('Ctrl Pts',(2.08131772978725,6.12033427680283,36.25));
#308467=CARTESIAN_POINT('Ctrl Pts',(2.1267784920286,6.08096773911451,36.25));
#308468=CARTESIAN_POINT('Ctrl Pts',(2.16876575254244,6.03778353402304,36.25));
#308469=CARTESIAN_POINT('Ctrl Pts',(2.20676901424551,5.99064810748104,36.25));
#308470=CARTESIAN_POINT('Ctrl Pts',(2.24084931578957,5.94000771696759,36.25));
#308471=CARTESIAN_POINT('Ctrl Pts',(2.27230135351232,5.88660676946342,36.25));
#308472=CARTESIAN_POINT('Ctrl Pts',(2.2981681398483,5.82909896870107,36.25));
#308473=CARTESIAN_POINT('Ctrl Pts',(2.32116828112027,5.76902496530642,36.25));
#308474=CARTESIAN_POINT('Ctrl Pts',(2.33892894507894,5.70553707456913,36.25));
#308475=CARTESIAN_POINT('Ctrl Pts',(2.35316409315178,5.63904690448481,36.25));
#308476=CARTESIAN_POINT('Ctrl Pts',(2.3632377280083,5.56952358146944,36.25));
#308477=CARTESIAN_POINT('Ctrl Pts',(2.3700963416033,5.4968345485113,36.25));
#308478=CARTESIAN_POINT('Ctrl Pts',(2.37065529854562,5.44731949788714,36.25));
#308479=CARTESIAN_POINT('Ctrl Pts',(2.37094155844156,5.42196124188312,36.25));
#308480=CARTESIAN_POINT('Ctrl Pts',(2.24724025974026,6.88253855519481,36.05));
#308481=CARTESIAN_POINT('Ctrl Pts',(2.24724025974026,6.88253855519481,36.29));
#308482=CARTESIAN_POINT('Ctrl Pts',(2.24629873402623,6.8452978442089,36.05));
#308483=CARTESIAN_POINT('Ctrl Pts',(2.24629873402623,6.8452978442089,36.29));
#308484=CARTESIAN_POINT('Ctrl Pts',(2.24448509897141,6.77356208818653,36.05));
#308485=CARTESIAN_POINT('Ctrl Pts',(2.24448509897141,6.77356208818653,36.29));
#308486=CARTESIAN_POINT('Ctrl Pts',(2.22577944098905,6.6705401244345,36.05));
#308487=CARTESIAN_POINT('Ctrl Pts',(2.22577944098905,6.6705401244345,36.29));
#308488=CARTESIAN_POINT('Ctrl Pts',(2.19665909049132,6.57608978278239,36.05));
#308489=CARTESIAN_POINT('Ctrl Pts',(2.19665909049132,6.57608978278239,36.29));
#308490=CARTESIAN_POINT('Ctrl Pts',(2.15426047894085,6.4907436496301,36.05));
#308491=CARTESIAN_POINT('Ctrl Pts',(2.15426047894085,6.4907436496301,36.29));
#308492=CARTESIAN_POINT('Ctrl Pts',(2.10006334842617,6.41405772296989,36.05));
#308493=CARTESIAN_POINT('Ctrl Pts',(2.10006334842617,6.41405772296989,36.29));
#308494=CARTESIAN_POINT('Ctrl Pts',(2.0335051920771,6.34678274879809,36.05));
#308495=CARTESIAN_POINT('Ctrl Pts',(2.0335051920771,6.34678274879809,36.29));
#308496=CARTESIAN_POINT('Ctrl Pts',(1.95525430031729,6.28741747621295,36.05));
#308497=CARTESIAN_POINT('Ctrl Pts',(1.95525430031729,6.28741747621295,36.29));
#308498=CARTESIAN_POINT('Ctrl Pts',(1.89580295974203,6.25752314612396,36.05));
#308499=CARTESIAN_POINT('Ctrl Pts',(1.89580295974203,6.25752314612396,36.29));
#308500=CARTESIAN_POINT('Ctrl Pts',(1.86518364448052,6.24212662337662,36.05));
#308501=CARTESIAN_POINT('Ctrl Pts',(1.86518364448052,6.24212662337662,36.29));
#308502=CARTESIAN_POINT('',(2.24724025974026,6.88253855519481,36.25));
#308503=CARTESIAN_POINT('',(2.24724025974026,6.88253855519481,32.1799631621335));
#308504=CARTESIAN_POINT('Ctrl Pts',(2.24724025974026,6.88253855519481,36.25));
#308505=CARTESIAN_POINT('Ctrl Pts',(2.24629873402623,6.8452978442089,36.25));
#308506=CARTESIAN_POINT('Ctrl Pts',(2.24448509897141,6.77356208818653,36.25));
#308507=CARTESIAN_POINT('Ctrl Pts',(2.22577944098905,6.6705401244345,36.25));
#308508=CARTESIAN_POINT('Ctrl Pts',(2.19665909049132,6.57608978278239,36.25));
#308509=CARTESIAN_POINT('Ctrl Pts',(2.15426047894085,6.4907436496301,36.25));
#308510=CARTESIAN_POINT('Ctrl Pts',(2.10006334842617,6.41405772296989,36.25));
#308511=CARTESIAN_POINT('Ctrl Pts',(2.0335051920771,6.34678274879809,36.25));
#308512=CARTESIAN_POINT('Ctrl Pts',(1.95525430031729,6.28741747621295,36.25));
#308513=CARTESIAN_POINT('Ctrl Pts',(1.89580295974203,6.25752314612396,36.25));
#308514=CARTESIAN_POINT('Ctrl Pts',(1.86518364448052,6.24212662337662,36.25));
#308515=CARTESIAN_POINT('Ctrl Pts',(1.52242796266234,7.71623376623377,36.05));
#308516=CARTESIAN_POINT('Ctrl Pts',(1.52242796266234,7.71623376623377,36.29));
#308517=CARTESIAN_POINT('Ctrl Pts',(1.54780821610109,7.71545767890599,36.05));
#308518=CARTESIAN_POINT('Ctrl Pts',(1.54780821610109,7.71545767890599,36.29));
#308519=CARTESIAN_POINT('Ctrl Pts',(1.59794752226823,7.71392449956901,36.05));
#308520=CARTESIAN_POINT('Ctrl Pts',(1.59794752226823,7.71392449956901,36.29));
#308521=CARTESIAN_POINT('Ctrl Pts',(1.67138411132394,7.7027904588233,36.05));
#308522=CARTESIAN_POINT('Ctrl Pts',(1.67138411132394,7.7027904588233,36.29));
#308523=CARTESIAN_POINT('Ctrl Pts',(1.74156530298064,7.68468886160549,36.05));
#308524=CARTESIAN_POINT('Ctrl Pts',(1.74156530298064,7.68468886160549,36.29));
#308525=CARTESIAN_POINT('Ctrl Pts',(1.80849182787228,7.65953041457979,36.05));
#308526=CARTESIAN_POINT('Ctrl Pts',(1.80849182787228,7.65953041457979,36.29));
#308527=CARTESIAN_POINT('Ctrl Pts',(1.87205683321845,7.62639783586101,36.05));
#308528=CARTESIAN_POINT('Ctrl Pts',(1.87205683321845,7.62639783586101,36.29));
#308529=CARTESIAN_POINT('Ctrl Pts',(1.9318511217457,7.58560597597768,36.05));
#308530=CARTESIAN_POINT('Ctrl Pts',(1.9318511217457,7.58560597597768,36.29));
#308531=CARTESIAN_POINT('Ctrl Pts',(1.98861539009419,7.53791001729144,36.05));
#308532=CARTESIAN_POINT('Ctrl Pts',(1.98861539009419,7.53791001729144,36.29));
#308533=CARTESIAN_POINT('Ctrl Pts',(2.04159249935513,7.48362087256877,36.05));
#308534=CARTESIAN_POINT('Ctrl Pts',(2.04159249935513,7.48362087256877,36.29));
#308535=CARTESIAN_POINT('Ctrl Pts',(2.08967670240967,7.42336185115535,36.05));
#308536=CARTESIAN_POINT('Ctrl Pts',(2.08967670240967,7.42336185115535,36.29));
#308537=CARTESIAN_POINT('Ctrl Pts',(2.1315901628391,7.35843862911193,36.05));
#308538=CARTESIAN_POINT('Ctrl Pts',(2.1315901628391,7.35843862911193,36.29));
#308539=CARTESIAN_POINT('Ctrl Pts',(2.16825091485445,7.29002627559583,36.05));
#308540=CARTESIAN_POINT('Ctrl Pts',(2.16825091485445,7.29002627559583,36.29));
#308541=CARTESIAN_POINT('Ctrl Pts',(2.19706966642109,7.21661236790923,36.05));
#308542=CARTESIAN_POINT('Ctrl Pts',(2.19706966642109,7.21661236790923,36.29));
#308543=CARTESIAN_POINT('Ctrl Pts',(2.21970139767277,7.13897358699381,36.05));
#308544=CARTESIAN_POINT('Ctrl Pts',(2.21970139767277,7.13897358699381,36.29));
#308545=CARTESIAN_POINT('Ctrl Pts',(2.23556552441298,7.05701575208482,36.05));
#308546=CARTESIAN_POINT('Ctrl Pts',(2.23556552441298,7.05701575208482,36.29));
#308547=CARTESIAN_POINT('Ctrl Pts',(2.24548752990423,6.97104879536392,36.05));
#308548=CARTESIAN_POINT('Ctrl Pts',(2.24548752990423,6.97104879536392,36.29));
#308549=CARTESIAN_POINT('Ctrl Pts',(2.2466485766986,6.91241766550898,36.05));
#308550=CARTESIAN_POINT('Ctrl Pts',(2.2466485766986,6.91241766550898,36.29));
#308551=CARTESIAN_POINT('Ctrl Pts',(2.24724025974026,6.88253855519481,36.05));
#308552=CARTESIAN_POINT('Ctrl Pts',(2.24724025974026,6.88253855519481,36.29));
#308553=CARTESIAN_POINT('',(1.52242796266234,7.71623376623377,36.25));
#308554=CARTESIAN_POINT('',(1.52242796266234,7.71623376623377,32.1799631621335));
#308555=CARTESIAN_POINT('Ctrl Pts',(1.52242796266234,7.71623376623377,36.25));
#308556=CARTESIAN_POINT('Ctrl Pts',(1.54780821610109,7.71545767890599,36.25));
#308557=CARTESIAN_POINT('Ctrl Pts',(1.59794752226823,7.71392449956901,36.25));
#308558=CARTESIAN_POINT('Ctrl Pts',(1.67138411132394,7.7027904588233,36.25));
#308559=CARTESIAN_POINT('Ctrl Pts',(1.74156530298064,7.68468886160549,36.25));
#308560=CARTESIAN_POINT('Ctrl Pts',(1.80849182787228,7.65953041457979,36.25));
#308561=CARTESIAN_POINT('Ctrl Pts',(1.87205683321845,7.62639783586101,36.25));
#308562=CARTESIAN_POINT('Ctrl Pts',(1.9318511217457,7.58560597597768,36.25));
#308563=CARTESIAN_POINT('Ctrl Pts',(1.98861539009419,7.53791001729144,36.25));
#308564=CARTESIAN_POINT('Ctrl Pts',(2.04159249935513,7.48362087256877,36.25));
#308565=CARTESIAN_POINT('Ctrl Pts',(2.08967670240967,7.42336185115535,36.25));
#308566=CARTESIAN_POINT('Ctrl Pts',(2.1315901628391,7.35843862911193,36.25));
#308567=CARTESIAN_POINT('Ctrl Pts',(2.16825091485445,7.29002627559583,36.25));
#308568=CARTESIAN_POINT('Ctrl Pts',(2.19706966642109,7.21661236790923,36.25));
#308569=CARTESIAN_POINT('Ctrl Pts',(2.21970139767277,7.13897358699381,36.25));
#308570=CARTESIAN_POINT('Ctrl Pts',(2.23556552441298,7.05701575208482,36.25));
#308571=CARTESIAN_POINT('Ctrl Pts',(2.24548752990423,6.97104879536392,36.25));
#308572=CARTESIAN_POINT('Ctrl Pts',(2.2466485766986,6.91241766550898,36.25));
#308573=CARTESIAN_POINT('Ctrl Pts',(2.24724025974026,6.88253855519481,36.25));
#308574=CARTESIAN_POINT('Ctrl Pts',(0.804058441558442,6.89542410714286,
36.05));
#308575=CARTESIAN_POINT('Ctrl Pts',(0.804058441558442,6.89542410714286,
36.29));
#308576=CARTESIAN_POINT('Ctrl Pts',(0.804649087710329,6.92508712200564,
36.05));
#308577=CARTESIAN_POINT('Ctrl Pts',(0.804649087710329,6.92508712200564,
36.29));
#308578=CARTESIAN_POINT('Ctrl Pts',(0.805803713282925,6.98307391394772,
36.05));
#308579=CARTESIAN_POINT('Ctrl Pts',(0.805803713282925,6.98307391394772,
36.29));
#308580=CARTESIAN_POINT('Ctrl Pts',(0.815658223082562,7.06800054423278,
36.05));
#308581=CARTESIAN_POINT('Ctrl Pts',(0.815658223082562,7.06800054423278,
36.29));
#308582=CARTESIAN_POINT('Ctrl Pts',(0.831843276752908,7.1485092997012,36.05));
#308583=CARTESIAN_POINT('Ctrl Pts',(0.831843276752908,7.1485092997012,36.29));
#308584=CARTESIAN_POINT('Ctrl Pts',(0.853271048234912,7.22519194306317,
36.05));
#308585=CARTESIAN_POINT('Ctrl Pts',(0.853271048234912,7.22519194306317,
36.29));
#308586=CARTESIAN_POINT('Ctrl Pts',(0.882914981130102,7.29688183752562,
36.05));
#308587=CARTESIAN_POINT('Ctrl Pts',(0.882914981130102,7.29688183752562,
36.29));
#308588=CARTESIAN_POINT('Ctrl Pts',(0.917480029442785,7.36527391878087,
36.05));
#308589=CARTESIAN_POINT('Ctrl Pts',(0.917480029442785,7.36527391878087,
36.29));
#308590=CARTESIAN_POINT('Ctrl Pts',(0.959667248194858,7.42884662646377,
36.05));
#308591=CARTESIAN_POINT('Ctrl Pts',(0.959667248194858,7.42884662646377,
36.29));
#308592=CARTESIAN_POINT('Ctrl Pts',(1.00709172396245,7.48817807892744,36.05));
#308593=CARTESIAN_POINT('Ctrl Pts',(1.00709172396245,7.48817807892744,36.29));
#308594=CARTESIAN_POINT('Ctrl Pts',(1.05972365886402,7.54133429965824,36.05));
#308595=CARTESIAN_POINT('Ctrl Pts',(1.05972365886402,7.54133429965824,36.29));
#308596=CARTESIAN_POINT('Ctrl Pts',(1.11597817292345,7.58805917500155,36.05));
#308597=CARTESIAN_POINT('Ctrl Pts',(1.11597817292345,7.58805917500155,36.29));
#308598=CARTESIAN_POINT('Ctrl Pts',(1.17567437498645,7.62785439831755,36.05));
#308599=CARTESIAN_POINT('Ctrl Pts',(1.17567437498645,7.62785439831755,36.29));
#308600=CARTESIAN_POINT('Ctrl Pts',(1.23894018265463,7.65993643724945,36.05));
#308601=CARTESIAN_POINT('Ctrl Pts',(1.23894018265463,7.65993643724945,36.29));
#308602=CARTESIAN_POINT('Ctrl Pts',(1.3051937479367,7.68533220871074,36.05));
#308603=CARTESIAN_POINT('Ctrl Pts',(1.3051937479367,7.68533220871074,36.29));
#308604=CARTESIAN_POINT('Ctrl Pts',(1.37469868549749,7.7036309678914,36.05));
#308605=CARTESIAN_POINT('Ctrl Pts',(1.37469868549749,7.7036309678914,36.29));
#308606=CARTESIAN_POINT('Ctrl Pts',(1.44761088404003,7.71370952681349,36.05));
#308607=CARTESIAN_POINT('Ctrl Pts',(1.44761088404003,7.71370952681349,36.29));
#308608=CARTESIAN_POINT('Ctrl Pts',(1.49727230748502,7.71538504428939,36.05));
#308609=CARTESIAN_POINT('Ctrl Pts',(1.49727230748502,7.71538504428939,36.29));
#308610=CARTESIAN_POINT('Ctrl Pts',(1.52242796266234,7.71623376623377,36.05));
#308611=CARTESIAN_POINT('Ctrl Pts',(1.52242796266234,7.71623376623377,36.29));
#308612=CARTESIAN_POINT('',(0.804058441558442,6.89542410714286,36.25));
#308613=CARTESIAN_POINT('',(0.804058441558442,6.89542410714286,32.1799631621335));
#308614=CARTESIAN_POINT('Ctrl Pts',(0.804058441558442,6.89542410714286,
36.25));
#308615=CARTESIAN_POINT('Ctrl Pts',(0.804649087710329,6.92508712200564,
36.25));
#308616=CARTESIAN_POINT('Ctrl Pts',(0.805803713282925,6.98307391394772,
36.25));
#308617=CARTESIAN_POINT('Ctrl Pts',(0.815658223082562,7.06800054423278,
36.25));
#308618=CARTESIAN_POINT('Ctrl Pts',(0.831843276752908,7.1485092997012,36.25));
#308619=CARTESIAN_POINT('Ctrl Pts',(0.853271048234912,7.22519194306317,
36.25));
#308620=CARTESIAN_POINT('Ctrl Pts',(0.882914981130102,7.29688183752562,
36.25));
#308621=CARTESIAN_POINT('Ctrl Pts',(0.917480029442785,7.36527391878087,
36.25));
#308622=CARTESIAN_POINT('Ctrl Pts',(0.959667248194858,7.42884662646377,
36.25));
#308623=CARTESIAN_POINT('Ctrl Pts',(1.00709172396245,7.48817807892744,36.25));
#308624=CARTESIAN_POINT('Ctrl Pts',(1.05972365886402,7.54133429965824,36.25));
#308625=CARTESIAN_POINT('Ctrl Pts',(1.11597817292345,7.58805917500155,36.25));
#308626=CARTESIAN_POINT('Ctrl Pts',(1.17567437498645,7.62785439831755,36.25));
#308627=CARTESIAN_POINT('Ctrl Pts',(1.23894018265463,7.65993643724945,36.25));
#308628=CARTESIAN_POINT('Ctrl Pts',(1.3051937479367,7.68533220871074,36.25));
#308629=CARTESIAN_POINT('Ctrl Pts',(1.37469868549749,7.7036309678914,36.25));
#308630=CARTESIAN_POINT('Ctrl Pts',(1.44761088404003,7.71370952681349,36.25));
#308631=CARTESIAN_POINT('Ctrl Pts',(1.49727230748502,7.71538504428939,36.25));
#308632=CARTESIAN_POINT('Ctrl Pts',(1.52242796266234,7.71623376623377,36.25));
#308633=CARTESIAN_POINT('Ctrl Pts',(1.1899807224026,6.24212662337662,36.05));
#308634=CARTESIAN_POINT('Ctrl Pts',(1.1899807224026,6.24212662337662,36.29));
#308635=CARTESIAN_POINT('Ctrl Pts',(1.15962955866533,6.25737900558172,36.05));
#308636=CARTESIAN_POINT('Ctrl Pts',(1.15962955866533,6.25737900558172,36.29));
#308637=CARTESIAN_POINT('Ctrl Pts',(1.10041391837872,6.28713666449684,36.05));
#308638=CARTESIAN_POINT('Ctrl Pts',(1.10041391837872,6.28713666449684,36.29));
#308639=CARTESIAN_POINT('Ctrl Pts',(1.02148620395913,6.34542328474194,36.05));
#308640=CARTESIAN_POINT('Ctrl Pts',(1.02148620395913,6.34542328474194,36.29));
#308641=CARTESIAN_POINT('Ctrl Pts',(0.954184014070375,6.41311300974787,
36.05));
#308642=CARTESIAN_POINT('Ctrl Pts',(0.954184014070375,6.41311300974787,
36.29));
#308643=CARTESIAN_POINT('Ctrl Pts',(0.898744629741027,6.49069341485485,
36.05));
#308644=CARTESIAN_POINT('Ctrl Pts',(0.898744629741027,6.49069341485485,
36.29));
#308645=CARTESIAN_POINT('Ctrl Pts',(0.855851150387493,6.57824013430206,
36.05));
#308646=CARTESIAN_POINT('Ctrl Pts',(0.855851150387493,6.57824013430206,
36.29));
#308647=CARTESIAN_POINT('Ctrl Pts',(0.82602871283696,6.67544579213543,36.05));
#308648=CARTESIAN_POINT('Ctrl Pts',(0.82602871283696,6.67544579213543,36.29));
#308649=CARTESIAN_POINT('Ctrl Pts',(0.806637417607563,6.78212192154818,
36.05));
#308650=CARTESIAN_POINT('Ctrl Pts',(0.806637417607563,6.78212192154818,
36.29));
#308651=CARTESIAN_POINT('Ctrl Pts',(0.804940416665592,6.85667628421743,
36.05));
#308652=CARTESIAN_POINT('Ctrl Pts',(0.804940416665592,6.85667628421743,
36.29));
#308653=CARTESIAN_POINT('Ctrl Pts',(0.804058441558442,6.89542410714286,
36.05));
#308654=CARTESIAN_POINT('Ctrl Pts',(0.804058441558442,6.89542410714286,
36.29));
#308655=CARTESIAN_POINT('',(1.1899807224026,6.24212662337662,36.25));
#308656=CARTESIAN_POINT('',(1.1899807224026,6.24212662337662,32.1799631621335));
#308657=CARTESIAN_POINT('Ctrl Pts',(1.1899807224026,6.24212662337662,36.25));
#308658=CARTESIAN_POINT('Ctrl Pts',(1.15962955866533,6.25737900558172,36.25));
#308659=CARTESIAN_POINT('Ctrl Pts',(1.10041391837872,6.28713666449684,36.25));
#308660=CARTESIAN_POINT('Ctrl Pts',(1.02148620395913,6.34542328474194,36.25));
#308661=CARTESIAN_POINT('Ctrl Pts',(0.954184014070375,6.41311300974787,
36.25));
#308662=CARTESIAN_POINT('Ctrl Pts',(0.898744629741027,6.49069341485485,
36.25));
#308663=CARTESIAN_POINT('Ctrl Pts',(0.855851150387493,6.57824013430206,
36.25));
#308664=CARTESIAN_POINT('Ctrl Pts',(0.82602871283696,6.67544579213543,36.25));
#308665=CARTESIAN_POINT('Ctrl Pts',(0.806637417607563,6.78212192154818,
36.25));
#308666=CARTESIAN_POINT('Ctrl Pts',(0.804940416665592,6.85667628421743,
36.25));
#308667=CARTESIAN_POINT('Ctrl Pts',(0.804058441558442,6.89542410714286,
36.25));
#308668=CARTESIAN_POINT('Ctrl Pts',(0.680357142857143,5.43291396103896,
36.05));
#308669=CARTESIAN_POINT('Ctrl Pts',(0.680357142857143,5.43291396103896,
36.29));
#308670=CARTESIAN_POINT('Ctrl Pts',(0.680668693953829,5.45891313799848,
36.05));
#308671=CARTESIAN_POINT('Ctrl Pts',(0.680668693953829,5.45891313799848,
36.29));
#308672=CARTESIAN_POINT('Ctrl Pts',(0.681279937811019,5.50992190470655,
36.05));
#308673=CARTESIAN_POINT('Ctrl Pts',(0.681279937811019,5.50992190470655,
36.29));
#308674=CARTESIAN_POINT('Ctrl Pts',(0.687839327233214,5.58482539360676,
36.05));
#308675=CARTESIAN_POINT('Ctrl Pts',(0.687839327233214,5.58482539360676,
36.29));
#308676=CARTESIAN_POINT('Ctrl Pts',(0.698772843207189,5.65624108672131,
36.05));
#308677=CARTESIAN_POINT('Ctrl Pts',(0.698772843207189,5.65624108672131,
36.29));
#308678=CARTESIAN_POINT('Ctrl Pts',(0.713532253106825,5.72405509656199,
36.05));
#308679=CARTESIAN_POINT('Ctrl Pts',(0.713532253106825,5.72405509656199,
36.29));
#308680=CARTESIAN_POINT('Ctrl Pts',(0.732151313294084,5.78833295550162,
36.05));
#308681=CARTESIAN_POINT('Ctrl Pts',(0.732151313294084,5.78833295550162,
36.29));
#308682=CARTESIAN_POINT('Ctrl Pts',(0.755394491764458,5.84911895337204,
36.05));
#308683=CARTESIAN_POINT('Ctrl Pts',(0.755394491764458,5.84911895337204,
36.29));
#308684=CARTESIAN_POINT('Ctrl Pts',(0.783058181337012,5.90641132135784,
36.05));
#308685=CARTESIAN_POINT('Ctrl Pts',(0.783058181337012,5.90641132135784,
36.29));
#308686=CARTESIAN_POINT('Ctrl Pts',(0.814867866880491,5.96019951630268,
36.05));
#308687=CARTESIAN_POINT('Ctrl Pts',(0.814867866880491,5.96019951630268,
36.29));
#308688=CARTESIAN_POINT('Ctrl Pts',(0.850057380368458,6.01030469320115,
36.05));
#308689=CARTESIAN_POINT('Ctrl Pts',(0.850057380368458,6.01030469320115,
36.29));
#308690=CARTESIAN_POINT('Ctrl Pts',(0.888809448167726,6.05629105732706,
36.05));
#308691=CARTESIAN_POINT('Ctrl Pts',(0.888809448167726,6.05629105732706,
36.29));
#308692=CARTESIAN_POINT('Ctrl Pts',(0.931020421596495,6.09774166415628,
36.05));
#308693=CARTESIAN_POINT('Ctrl Pts',(0.931020421596495,6.09774166415628,
36.29));
#308694=CARTESIAN_POINT('Ctrl Pts',(0.976304255584941,6.1351992195304,36.05));
#308695=CARTESIAN_POINT('Ctrl Pts',(0.976304255584941,6.1351992195304,36.29));
#308696=CARTESIAN_POINT('Ctrl Pts',(1.02473287123688,6.16910978501208,36.05));
#308697=CARTESIAN_POINT('Ctrl Pts',(1.02473287123688,6.16910978501208,36.29));
#308698=CARTESIAN_POINT('Ctrl Pts',(1.07696907224526,6.19776979492405,36.05));
#308699=CARTESIAN_POINT('Ctrl Pts',(1.07696907224526,6.19776979492405,36.29));
#308700=CARTESIAN_POINT('Ctrl Pts',(1.13212158876422,6.22263196745495,36.05));
#308701=CARTESIAN_POINT('Ctrl Pts',(1.13212158876422,6.22263196745495,36.29));
#308702=CARTESIAN_POINT('Ctrl Pts',(1.17053061939841,6.23557324032603,36.05));
#308703=CARTESIAN_POINT('Ctrl Pts',(1.17053061939841,6.23557324032603,36.29));
#308704=CARTESIAN_POINT('Ctrl Pts',(1.1899807224026,6.24212662337662,36.05));
#308705=CARTESIAN_POINT('Ctrl Pts',(1.1899807224026,6.24212662337662,36.29));
#308706=CARTESIAN_POINT('',(0.680357142857143,5.43291396103896,36.25));
#308707=CARTESIAN_POINT('',(0.680357142857143,5.43291396103896,32.1799631621335));
#308708=CARTESIAN_POINT('Ctrl Pts',(0.680357142857143,5.43291396103896,
36.25));
#308709=CARTESIAN_POINT('Ctrl Pts',(0.680668693953829,5.45891313799848,
36.25));
#308710=CARTESIAN_POINT('Ctrl Pts',(0.681279937811019,5.50992190470655,
36.25));
#308711=CARTESIAN_POINT('Ctrl Pts',(0.687839327233214,5.58482539360676,
36.25));
#308712=CARTESIAN_POINT('Ctrl Pts',(0.698772843207189,5.65624108672131,
36.25));
#308713=CARTESIAN_POINT('Ctrl Pts',(0.713532253106825,5.72405509656199,
36.25));
#308714=CARTESIAN_POINT('Ctrl Pts',(0.732151313294084,5.78833295550162,
36.25));
#308715=CARTESIAN_POINT('Ctrl Pts',(0.755394491764458,5.84911895337204,
36.25));
#308716=CARTESIAN_POINT('Ctrl Pts',(0.783058181337012,5.90641132135784,
36.25));
#308717=CARTESIAN_POINT('Ctrl Pts',(0.814867866880491,5.96019951630268,
36.25));
#308718=CARTESIAN_POINT('Ctrl Pts',(0.850057380368458,6.01030469320115,
36.25));
#308719=CARTESIAN_POINT('Ctrl Pts',(0.888809448167726,6.05629105732706,
36.25));
#308720=CARTESIAN_POINT('Ctrl Pts',(0.931020421596495,6.09774166415628,
36.25));
#308721=CARTESIAN_POINT('Ctrl Pts',(0.976304255584941,6.1351992195304,36.25));
#308722=CARTESIAN_POINT('Ctrl Pts',(1.02473287123688,6.16910978501208,36.25));
#308723=CARTESIAN_POINT('Ctrl Pts',(1.07696907224526,6.19776979492405,36.25));
#308724=CARTESIAN_POINT('Ctrl Pts',(1.13212158876422,6.22263196745495,36.25));
#308725=CARTESIAN_POINT('Ctrl Pts',(1.17053061939841,6.23557324032603,36.25));
#308726=CARTESIAN_POINT('Ctrl Pts',(1.1899807224026,6.24212662337662,36.25));
#308727=CARTESIAN_POINT('Ctrl Pts',(1.52758218344156,4.45876623376623,36.05));
#308728=CARTESIAN_POINT('Ctrl Pts',(1.52758218344156,4.45876623376623,36.29));
#308729=CARTESIAN_POINT('Ctrl Pts',(1.49790947590789,4.4597253240939,36.05));
#308730=CARTESIAN_POINT('Ctrl Pts',(1.49790947590789,4.4597253240939,36.29));
#308731=CARTESIAN_POINT('Ctrl Pts',(1.43959848220332,4.46161006986558,36.05));
#308732=CARTESIAN_POINT('Ctrl Pts',(1.43959848220332,4.46161006986558,36.29));
#308733=CARTESIAN_POINT('Ctrl Pts',(1.35393326291226,4.47372823681752,36.05));
#308734=CARTESIAN_POINT('Ctrl Pts',(1.35393326291226,4.47372823681752,36.29));
#308735=CARTESIAN_POINT('Ctrl Pts',(1.27247800686959,4.49538915943629,36.05));
#308736=CARTESIAN_POINT('Ctrl Pts',(1.27247800686959,4.49538915943629,36.29));
#308737=CARTESIAN_POINT('Ctrl Pts',(1.19426688731232,4.52434515927101,36.05));
#308738=CARTESIAN_POINT('Ctrl Pts',(1.19426688731232,4.52434515927101,36.29));
#308739=CARTESIAN_POINT('Ctrl Pts',(1.12007772580205,4.56241550483758,36.05));
#308740=CARTESIAN_POINT('Ctrl Pts',(1.12007772580205,4.56241550483758,36.29));
#308741=CARTESIAN_POINT('Ctrl Pts',(1.05020719586857,4.60959489382439,36.05));
#308742=CARTESIAN_POINT('Ctrl Pts',(1.05020719586857,4.60959489382439,36.29));
#308743=CARTESIAN_POINT('Ctrl Pts',(0.983166501449546,4.66375358613811,
36.05));
#308744=CARTESIAN_POINT('Ctrl Pts',(0.983166501449546,4.66375358613811,
36.29));
#308745=CARTESIAN_POINT('Ctrl Pts',(0.921454901216499,4.72680658155488,
36.05));
#308746=CARTESIAN_POINT('Ctrl Pts',(0.921454901216499,4.72680658155488,
36.29));
#308747=CARTESIAN_POINT('Ctrl Pts',(0.864436955628593,4.79599402074389,
36.05));
#308748=CARTESIAN_POINT('Ctrl Pts',(0.864436955628593,4.79599402074389,
36.29));
#308749=CARTESIAN_POINT('Ctrl Pts',(0.815819415600203,4.87186228483585,
36.05));
#308750=CARTESIAN_POINT('Ctrl Pts',(0.815819415600203,4.87186228483585,
36.29));
#308751=CARTESIAN_POINT('Ctrl Pts',(0.773237258753005,4.95218254596678,
36.05));
#308752=CARTESIAN_POINT('Ctrl Pts',(0.773237258753005,4.95218254596678,
36.29));
#308753=CARTESIAN_POINT('Ctrl Pts',(0.739295500896744,5.03825698338498,
36.05));
#308754=CARTESIAN_POINT('Ctrl Pts',(0.739295500896744,5.03825698338498,
36.29));
#308755=CARTESIAN_POINT('Ctrl Pts',(0.712762470738981,5.12949961741785,
36.05));
#308756=CARTESIAN_POINT('Ctrl Pts',(0.712762470738981,5.12949961741785,
36.29));
#308757=CARTESIAN_POINT('Ctrl Pts',(0.694428924083107,5.22616336292247,
36.05));
#308758=CARTESIAN_POINT('Ctrl Pts',(0.694428924083107,5.22616336292247,
36.29));
#308759=CARTESIAN_POINT('Ctrl Pts',(0.682434422236949,5.32781045016027,
36.05));
#308760=CARTESIAN_POINT('Ctrl Pts',(0.682434422236949,5.32781045016027,
36.29));
#308761=CARTESIAN_POINT('Ctrl Pts',(0.681058184371366,5.39744356397404,
36.05));
#308762=CARTESIAN_POINT('Ctrl Pts',(0.681058184371366,5.39744356397404,
36.29));
#308763=CARTESIAN_POINT('Ctrl Pts',(0.680357142857143,5.43291396103896,
36.05));
#308764=CARTESIAN_POINT('Ctrl Pts',(0.680357142857143,5.43291396103896,
36.29));
#308765=CARTESIAN_POINT('',(1.52758218344156,4.45876623376623,36.25));
#308766=CARTESIAN_POINT('',(1.52758218344156,4.45876623376623,32.1799631621335));
#308767=CARTESIAN_POINT('Ctrl Pts',(1.52758218344156,4.45876623376623,36.25));
#308768=CARTESIAN_POINT('Ctrl Pts',(1.49790947590789,4.4597253240939,36.25));
#308769=CARTESIAN_POINT('Ctrl Pts',(1.43959848220332,4.46161006986558,36.25));
#308770=CARTESIAN_POINT('Ctrl Pts',(1.35393326291226,4.47372823681752,36.25));
#308771=CARTESIAN_POINT('Ctrl Pts',(1.27247800686959,4.49538915943629,36.25));
#308772=CARTESIAN_POINT('Ctrl Pts',(1.19426688731232,4.52434515927101,36.25));
#308773=CARTESIAN_POINT('Ctrl Pts',(1.12007772580205,4.56241550483758,36.25));
#308774=CARTESIAN_POINT('Ctrl Pts',(1.05020719586857,4.60959489382439,36.25));
#308775=CARTESIAN_POINT('Ctrl Pts',(0.983166501449546,4.66375358613811,
36.25));
#308776=CARTESIAN_POINT('Ctrl Pts',(0.921454901216499,4.72680658155488,
36.25));
#308777=CARTESIAN_POINT('Ctrl Pts',(0.864436955628593,4.79599402074389,
36.25));
#308778=CARTESIAN_POINT('Ctrl Pts',(0.815819415600203,4.87186228483585,
36.25));
#308779=CARTESIAN_POINT('Ctrl Pts',(0.773237258753005,4.95218254596678,
36.25));
#308780=CARTESIAN_POINT('Ctrl Pts',(0.739295500896744,5.03825698338498,
36.25));
#308781=CARTESIAN_POINT('Ctrl Pts',(0.712762470738981,5.12949961741785,
36.25));
#308782=CARTESIAN_POINT('Ctrl Pts',(0.694428924083107,5.22616336292247,
36.25));
#308783=CARTESIAN_POINT('Ctrl Pts',(0.682434422236949,5.32781045016027,
36.25));
#308784=CARTESIAN_POINT('Ctrl Pts',(0.681058184371366,5.39744356397404,
36.25));
#308785=CARTESIAN_POINT('Ctrl Pts',(0.680357142857143,5.43291396103896,
36.25));
#308786=CARTESIAN_POINT('Ctrl Pts',(2.37094155844156,5.42196124188312,36.05));
#308787=CARTESIAN_POINT('Ctrl Pts',(2.37094155844156,5.42196124188312,36.29));
#308788=CARTESIAN_POINT('Ctrl Pts',(2.3701449621061,5.3873620729942,36.05));
#308789=CARTESIAN_POINT('Ctrl Pts',(2.3701449621061,5.3873620729942,36.29));
#308790=CARTESIAN_POINT('Ctrl Pts',(2.36858230731467,5.31949010994648,36.05));
#308791=CARTESIAN_POINT('Ctrl Pts',(2.36858230731467,5.31949010994648,36.29));
#308792=CARTESIAN_POINT('Ctrl Pts',(2.35792489966522,5.21999888881734,36.05));
#308793=CARTESIAN_POINT('Ctrl Pts',(2.35792489966522,5.21999888881734,36.29));
#308794=CARTESIAN_POINT('Ctrl Pts',(2.33816283696992,5.12552781537341,36.05));
#308795=CARTESIAN_POINT('Ctrl Pts',(2.33816283696992,5.12552781537341,36.29));
#308796=CARTESIAN_POINT('Ctrl Pts',(2.31216804403568,5.03559649057185,36.05));
#308797=CARTESIAN_POINT('Ctrl Pts',(2.31216804403568,5.03559649057185,36.29));
#308798=CARTESIAN_POINT('Ctrl Pts',(2.27768357726726,4.95095791492866,36.05));
#308799=CARTESIAN_POINT('Ctrl Pts',(2.27768357726726,4.95095791492866,36.29));
#308800=CARTESIAN_POINT('Ctrl Pts',(2.23640375626704,4.87078209602146,36.05));
#308801=CARTESIAN_POINT('Ctrl Pts',(2.23640375626704,4.87078209602146,36.29));
#308802=CARTESIAN_POINT('Ctrl Pts',(2.18650804768952,4.79615096254107,36.05));
#308803=CARTESIAN_POINT('Ctrl Pts',(2.18650804768952,4.79615096254107,36.29));
#308804=CARTESIAN_POINT('Ctrl Pts',(2.12995256471625,4.72672058470318,36.05));
#308805=CARTESIAN_POINT('Ctrl Pts',(2.12995256471625,4.72672058470318,36.29));
#308806=CARTESIAN_POINT('Ctrl Pts',(2.06812897983805,4.66400945675856,36.05));
#308807=CARTESIAN_POINT('Ctrl Pts',(2.06812897983805,4.66400945675856,36.29));
#308808=CARTESIAN_POINT('Ctrl Pts',(2.00171131208806,4.60935645208091,36.05));
#308809=CARTESIAN_POINT('Ctrl Pts',(2.00171131208806,4.60935645208091,36.29));
#308810=CARTESIAN_POINT('Ctrl Pts',(1.93195013979453,4.56264762609262,36.05));
#308811=CARTESIAN_POINT('Ctrl Pts',(1.93195013979453,4.56264762609262,36.29));
#308812=CARTESIAN_POINT('Ctrl Pts',(1.85820350335783,4.5241565808727,36.05));
#308813=CARTESIAN_POINT('Ctrl Pts',(1.85820350335783,4.5241565808727,36.29));
#308814=CARTESIAN_POINT('Ctrl Pts',(1.78027605704376,4.49553589484458,36.05));
#308815=CARTESIAN_POINT('Ctrl Pts',(1.78027605704376,4.49553589484458,36.29));
#308816=CARTESIAN_POINT('Ctrl Pts',(1.69931628629545,4.47370190759594,36.05));
#308817=CARTESIAN_POINT('Ctrl Pts',(1.69931628629545,4.47370190759594,36.29));
#308818=CARTESIAN_POINT('Ctrl Pts',(1.61449027768335,4.46164864649648,36.05));
#308819=CARTESIAN_POINT('Ctrl Pts',(1.61449027768335,4.46164864649648,36.29));
#308820=CARTESIAN_POINT('Ctrl Pts',(1.55682420860062,4.45973608112409,36.05));
#308821=CARTESIAN_POINT('Ctrl Pts',(1.55682420860062,4.45973608112409,36.29));
#308822=CARTESIAN_POINT('Ctrl Pts',(1.52758218344156,4.45876623376623,36.05));
#308823=CARTESIAN_POINT('Ctrl Pts',(1.52758218344156,4.45876623376623,36.29));
#308824=CARTESIAN_POINT('Ctrl Pts',(2.37094155844156,5.42196124188312,36.25));
#308825=CARTESIAN_POINT('Ctrl Pts',(2.3701449621061,5.3873620729942,36.25));
#308826=CARTESIAN_POINT('Ctrl Pts',(2.36858230731467,5.31949010994648,36.25));
#308827=CARTESIAN_POINT('Ctrl Pts',(2.35792489966522,5.21999888881734,36.25));
#308828=CARTESIAN_POINT('Ctrl Pts',(2.33816283696992,5.12552781537341,36.25));
#308829=CARTESIAN_POINT('Ctrl Pts',(2.31216804403568,5.03559649057185,36.25));
#308830=CARTESIAN_POINT('Ctrl Pts',(2.27768357726726,4.95095791492866,36.25));
#308831=CARTESIAN_POINT('Ctrl Pts',(2.23640375626704,4.87078209602146,36.25));
#308832=CARTESIAN_POINT('Ctrl Pts',(2.18650804768952,4.79615096254107,36.25));
#308833=CARTESIAN_POINT('Ctrl Pts',(2.12995256471625,4.72672058470318,36.25));
#308834=CARTESIAN_POINT('Ctrl Pts',(2.06812897983805,4.66400945675856,36.25));
#308835=CARTESIAN_POINT('Ctrl Pts',(2.00171131208806,4.60935645208091,36.25));
#308836=CARTESIAN_POINT('Ctrl Pts',(1.93195013979453,4.56264762609262,36.25));
#308837=CARTESIAN_POINT('Ctrl Pts',(1.85820350335783,4.5241565808727,36.25));
#308838=CARTESIAN_POINT('Ctrl Pts',(1.78027605704376,4.49553589484458,36.25));
#308839=CARTESIAN_POINT('Ctrl Pts',(1.69931628629545,4.47370190759594,36.25));
#308840=CARTESIAN_POINT('Ctrl Pts',(1.61449027768335,4.46164864649648,36.25));
#308841=CARTESIAN_POINT('Ctrl Pts',(1.55682420860062,4.45973608112409,36.25));
#308842=CARTESIAN_POINT('Ctrl Pts',(1.52758218344156,4.45876623376623,36.25));
#308843=CARTESIAN_POINT('Origin',(-0.185551948051949,4.5,32.1799631621335));
#308844=CARTESIAN_POINT('',(-0.185551948051949,4.5,36.25));
#308845=CARTESIAN_POINT('',(-0.185551948051949,4.5,32.1799631621335));
#308846=CARTESIAN_POINT('',(-0.185551948051949,4.95357142857143,36.25));
#308847=CARTESIAN_POINT('',(-0.185551948051949,4.95357142857143,32.1799631621335));
#308848=CARTESIAN_POINT('',(-0.185551948051949,0.,36.25));
#308849=CARTESIAN_POINT('Origin',(0.144318181818181,4.5,32.1799631621335));
#308850=CARTESIAN_POINT('',(0.144318181818181,4.5,36.25));
#308851=CARTESIAN_POINT('',(0.144318181818181,4.5,32.1799631621335));
#308852=CARTESIAN_POINT('',(0.,4.5,36.25));
#308853=CARTESIAN_POINT('Origin',(0.144318181818181,4.95357142857143,32.1799631621335));
#308854=CARTESIAN_POINT('',(0.144318181818181,4.95357142857143,36.25));
#308855=CARTESIAN_POINT('',(0.144318181818181,4.95357142857143,32.1799631621335));
#308856=CARTESIAN_POINT('',(0.144318181818181,0.,36.25));
#308857=CARTESIAN_POINT('Origin',(-0.185551948051949,4.95357142857143,32.1799631621335));
#308858=CARTESIAN_POINT('',(0.,4.95357142857143,36.25));
#308859=CARTESIAN_POINT('Origin',(0.,0.,36.25));
#308860=CARTESIAN_POINT('',(4.75,-8.22724133595217,36.25));
#308861=CARTESIAN_POINT('',(9.5,0.,36.25));
#308862=CARTESIAN_POINT('Origin',(0.,0.,36.25));
#308863=CARTESIAN_POINT('',(4.75,8.22724133595217,36.25));
#308864=CARTESIAN_POINT('Origin',(0.,0.,36.25));
#308865=CARTESIAN_POINT('',(-4.75,8.22724133595217,36.25));
#308866=CARTESIAN_POINT('Origin',(0.,0.,36.25));
#308867=CARTESIAN_POINT('',(-9.5,-1.50231459873716E-15,36.25));
#308868=CARTESIAN_POINT('Origin',(0.,0.,36.25));
#308869=CARTESIAN_POINT('',(-4.75,-8.22724133595217,36.25));
#308870=CARTESIAN_POINT('Origin',(0.,0.,36.25));
#308871=CARTESIAN_POINT('Origin',(0.,0.,36.25));
#308872=CARTESIAN_POINT('Origin',(0.,0.,36.25));
#308873=CARTESIAN_POINT('',(-2.91010732950533E-15,-10.9696551146029,35.4014942239681));
#308874=CARTESIAN_POINT('Ctrl Pts',(-4.74999999999998,-8.22724133595217,
36.25));
#308875=CARTESIAN_POINT('Ctrl Pts',(-2.54551732809356,-9.50000000000121,
36.25));
#308876=CARTESIAN_POINT('Ctrl Pts',(5.22468907019947E-12,-10.9696551146059,
35.4014942239664));
#308877=CARTESIAN_POINT('Ctrl Pts',(-5.2327759896147E-12,-10.9696551146059,
35.4014942239664));
#308878=CARTESIAN_POINT('Ctrl Pts',(2.54551732809357,-9.50000000000122,
36.25));
#308879=CARTESIAN_POINT('Ctrl Pts',(4.75000000000001,-8.22724133595218,
36.25));
#308880=CARTESIAN_POINT('Origin',(0.,0.,36.25));
#308881=CARTESIAN_POINT('',(9.5,-5.48482755730145,35.4014942239681));
#308882=CARTESIAN_POINT('Ctrl Pts',(4.75000000000001,-8.22724133595218,
36.25));
#308883=CARTESIAN_POINT('Ctrl Pts',(6.95448267190644,-6.95448267190313,
36.25));
#308884=CARTESIAN_POINT('Ctrl Pts',(9.50000000000523,-5.48482755729844,
35.4014942239664));
#308885=CARTESIAN_POINT('Ctrl Pts',(9.5,-5.48482755730749,35.4014942239664));
#308886=CARTESIAN_POINT('Ctrl Pts',(9.5,-2.54551732809809,36.25));
#308887=CARTESIAN_POINT('Ctrl Pts',(9.5,1.60134500782782E-14,36.25));
#308888=CARTESIAN_POINT('Origin',(0.,0.,36.25));
#308889=CARTESIAN_POINT('',(9.5,5.48482755730145,35.4014942239681));
#308890=CARTESIAN_POINT('Ctrl Pts',(9.5,1.60134500782782E-14,36.25));
#308891=CARTESIAN_POINT('Ctrl Pts',(9.5,2.5455173280981,36.25));
#308892=CARTESIAN_POINT('Ctrl Pts',(9.5,5.48482755730748,35.4014942239664));
#308893=CARTESIAN_POINT('Ctrl Pts',(9.50000000000522,5.48482755729844,35.4014942239664));
#308894=CARTESIAN_POINT('Ctrl Pts',(6.95448267190642,6.95448267190313,36.25));
#308895=CARTESIAN_POINT('Ctrl Pts',(4.74999999999998,8.22724133595218,36.25));
#308896=CARTESIAN_POINT('Origin',(0.,0.,36.25));
#308897=CARTESIAN_POINT('',(-4.96520474180093E-16,10.9696551146029,35.4014942239681));
#308898=CARTESIAN_POINT('Ctrl Pts',(4.74999999999998,8.22724133595218,36.25));
#308899=CARTESIAN_POINT('Ctrl Pts',(2.54551732809355,9.50000000000122,36.25));
#308900=CARTESIAN_POINT('Ctrl Pts',(-5.2257673261215E-12,10.9696551146059,
35.4014942239664));
#308901=CARTESIAN_POINT('Ctrl Pts',(5.23169773369267E-12,10.9696551146059,
35.4014942239664));
#308902=CARTESIAN_POINT('Ctrl Pts',(-2.54551732809357,9.50000000000122,
36.25));
#308903=CARTESIAN_POINT('Ctrl Pts',(-4.75,8.22724133595218,36.25));
#308904=CARTESIAN_POINT('Origin',(0.,0.,36.25));
#308905=CARTESIAN_POINT('',(-9.5,-5.48482755730144,35.4014942239681));
#308906=CARTESIAN_POINT('Ctrl Pts',(-9.5,-1.40117688184935E-14,36.25));
#308907=CARTESIAN_POINT('Ctrl Pts',(-9.5,-2.54551732809809,36.25));
#308908=CARTESIAN_POINT('Ctrl Pts',(-9.5,-5.48482755730747,35.4014942239664));
#308909=CARTESIAN_POINT('Ctrl Pts',(-9.50000000000523,-5.48482755729841,
35.4014942239664));
#308910=CARTESIAN_POINT('Ctrl Pts',(-6.95448267190643,-6.95448267190312,
36.25));
#308911=CARTESIAN_POINT('Ctrl Pts',(-4.74999999999998,-8.22724133595217,
36.25));
#308912=CARTESIAN_POINT('Origin',(0.,0.,36.25));
#308913=CARTESIAN_POINT('',(-9.5,5.48482755730145,35.4014942239681));
#308914=CARTESIAN_POINT('Ctrl Pts',(-9.5,5.48482755730747,35.4014942239664));
#308915=CARTESIAN_POINT('Ctrl Pts',(-9.5,2.54551732809808,36.25));
#308916=CARTESIAN_POINT('Ctrl Pts',(-9.5,-1.40117688184935E-14,36.25));
#308917=CARTESIAN_POINT('Ctrl Pts',(-4.75,8.22724133595218,36.25));
#308918=CARTESIAN_POINT('Ctrl Pts',(-6.95448267190644,6.95448267190313,
36.25));
#308919=CARTESIAN_POINT('Ctrl Pts',(-9.50000000000522,5.48482755729844,
35.4014942239664));
#308920=CARTESIAN_POINT('Origin',(-9.5,-5.48482755730144,36.25));
#308921=CARTESIAN_POINT('',(-9.5,-5.48482755730144,28.75));
#308922=CARTESIAN_POINT('',(-9.5,-5.48482755730144,36.25));
#308923=CARTESIAN_POINT('',(-2.51906757195928E-15,-10.9696551146029,28.75));
#308924=CARTESIAN_POINT('',(-9.5,-5.48482755730144,28.75));
#308925=CARTESIAN_POINT('',(-2.51906757195928E-15,-10.9696551146029,36.25));
#308926=CARTESIAN_POINT('Origin',(-2.51906757195928E-15,-10.9696551146029,
36.25));
#308927=CARTESIAN_POINT('',(9.5,-5.48482755730145,28.75));
#308928=CARTESIAN_POINT('',(-2.51906757195928E-15,-10.9696551146029,28.75));
#308929=CARTESIAN_POINT('',(9.5,-5.48482755730145,36.25));
#308930=CARTESIAN_POINT('Origin',(9.5,-5.48482755730145,36.25));
#308931=CARTESIAN_POINT('',(9.5,5.48482755730145,28.75));
#308932=CARTESIAN_POINT('',(9.5,-5.48482755730145,28.75));
#308933=CARTESIAN_POINT('',(9.5,5.48482755730145,36.25));
#308934=CARTESIAN_POINT('Origin',(9.5,5.48482755730145,36.25));
#308935=CARTESIAN_POINT('',(-1.81887649324012E-16,10.9696551146029,28.75));
#308936=CARTESIAN_POINT('',(9.5,5.48482755730145,28.75));
#308937=CARTESIAN_POINT('',(-1.81887649324012E-16,10.9696551146029,36.25));
#308938=CARTESIAN_POINT('Origin',(-1.81887649324012E-16,10.9696551146029,
36.25));
#308939=CARTESIAN_POINT('',(-9.5,5.48482755730145,28.75));
#308940=CARTESIAN_POINT('',(-1.81887649324012E-16,10.9696551146029,28.75));
#308941=CARTESIAN_POINT('',(-9.5,5.48482755730145,36.25));
#308942=CARTESIAN_POINT('Origin',(-9.5,5.48482755730145,36.25));
#308943=CARTESIAN_POINT('',(-9.5,5.48482755730145,28.75));
#308944=CARTESIAN_POINT('Origin',(0.,0.,28.75));
#308945=CARTESIAN_POINT('Origin',(0.,5.28128932132296E-15,28.75));
#308946=CARTESIAN_POINT('Origin',(0.,0.,-6.25));
#310599=UNCERTAINTY_MEASURE_WITH_UNIT(LENGTH_MEASURE(0.01),#310624,
'DISTANCE_ACCURACY_VALUE',
'Maximum model space distance between geometric entities at asserted c
onnectivities');
#310601=UNCERTAINTY_MEASURE_WITH_UNIT(LENGTH_MEASURE(0.01),#310624,
'DISTANCE_ACCURACY_VALUE',
'Maximum model space distance between geometric entities at asserted c
onnectivities');
#310621=(
GEOMETRIC_REPRESENTATION_CONTEXT(3)
GLOBAL_UNCERTAINTY_ASSIGNED_CONTEXT((#310599))
GLOBAL_UNIT_ASSIGNED_CONTEXT((#310624,#310626,#310627))
REPRESENTATION_CONTEXT('','3D')
);
#310623=(
GEOMETRIC_REPRESENTATION_CONTEXT(3)
GLOBAL_UNCERTAINTY_ASSIGNED_CONTEXT((#310601))
GLOBAL_UNIT_ASSIGNED_CONTEXT((#310624,#310626,#310627))
REPRESENTATION_CONTEXT('','3D')
);
#310624=(
LENGTH_UNIT()
NAMED_UNIT(*)
SI_UNIT(.MILLI.,.METRE.)
);
#310626=(
NAMED_UNIT(*)
PLANE_ANGLE_UNIT()
SI_UNIT($,.RADIAN.)
);
#310627=(
NAMED_UNIT(*)
SI_UNIT($,.STERADIAN.)
SOLID_ANGLE_UNIT()
);
#310647=SHAPE_DEFINITION_REPRESENTATION(#310808,#310912);
#310808=PRODUCT_DEFINITION_SHAPE('',$,#310934);
#310912=SHAPE_REPRESENTATION('',(#104637),#310621);
#310914=PRODUCT_DEFINITION_CONTEXT('part definition',#310979,'design');
#310934=PRODUCT_DEFINITION('Class 8.8 Steel Hex Head Screw',
'Class 8.8 Steel Hex Head Screw',#310955,#310914);
#310955=PRODUCT_DEFINITION_FORMATION('',$,#311000);
#310979=APPLICATION_CONTEXT(
'Core Data for Automotive Mechanical Design Process');
#310980=PRODUCT_CONTEXT('part definition',#310979,'mechanical');
#311000=PRODUCT('Class 8.8 Steel Hex Head Screw',
'Class 8.8 Steel Hex Head Screw',$,(#310980));
#311008=PRESENTATION_STYLE_ASSIGNMENT((#311015));
#311015=SURFACE_STYLE_USAGE(.BOTH.,#311022);
#311022=SURFACE_SIDE_STYLE('',(#311029));
#311029=SURFACE_STYLE_FILL_AREA(#311036);
#311036=FILL_AREA_STYLE('Opaque(31,36,43)',(#311043));
#311043=FILL_AREA_STYLE_COLOUR('Opaque(31,36,43)',#311050);
#311050=COLOUR_RGB('Opaque(31,36,43)',0.12156862745098,0.141176470588235,
0.168627450980392);
ENDSEC;
END-ISO-10303-21;
